ISO-10303-21;
HEADER;
FILE_DESCRIPTION (('STEP AP214'),
    '1' );
FILE_NAME ('pinion.step',
    '2026-10-27T17:59:55',
    ( '' ),
    ( '' ),
    'SwSTEP 2.0',
    'SolidWorks 2025',
    '' );
FILE_SCHEMA (( 'AUTOMOTIVE_DESIGN' ));
ENDSEC;

DATA;
#1=EDGE_LOOP ( 'NONE', ( #10472, #7018, #25272, #25137 ) ) ;
#6=DIRECTION ( 'NONE',  ( -1.000000000000000000, 6.938893903907226837E-18, -1.734723475976806709E-18 ) ) ;
#14=CARTESIAN_POINT ( 'NONE',  ( -12.82751273423877514, -44.03362901246993744, 21.21958768041844579 ) ) ;
#18=EDGE_CURVE ( 'NONE', #18004, #25022, #27276, .T. ) ;
#31=EDGE_CURVE ( 'NONE', #25314, #21344, #6914, .T. ) ;
#34=CARTESIAN_POINT ( 'NONE',  ( -1.019300379054419947, -44.15350047934390432, 12.21833869579511500 ) ) ;
#37=CARTESIAN_POINT ( 'NONE',  ( -20.57838717382308147, -16.28767523336102130, 25.16001208503123365 ) ) ;
#45=CARTESIAN_POINT ( 'NONE',  ( -1.050230346682696103, 37.05264119692688496, -26.91946103437118509 ) ) ;
#47=VECTOR ( 'NONE', #2248, 999.9999999999998863 ) ;
#48=ORIENTED_EDGE ( 'NONE', *, *, #19991, .T. ) ;
#50=DIRECTION ( 'NONE',  ( 0.000000000000000000, 5.223019709707975211E-21, -1.000000000000000000 ) ) ;
#55=CARTESIAN_POINT ( 'NONE',  ( -8.786685647604890903, -52.67761315067293282, -9.545808661480407409 ) ) ;
#56=EDGE_LOOP ( 'NONE', ( #3504, #20915, #25986, #8058 ) ) ;
#58=EDGE_CURVE ( 'NONE', #28126, #17270, #1739, .T. ) ;
#61=FACE_OUTER_BOUND ( 'NONE', #13204, .T. ) ;
#77=( BOUNDED_SURFACE ( )  B_SPLINE_SURFACE ( 3, 1, ( 
 ( #18368, #537 ),
 ( #2696, #7179 ),
 ( #16223, #3130 ),
 ( #25029, #14055 ) ),
 .UNSPECIFIED., .F., .F., .F. ) 
 B_SPLINE_SURFACE_WITH_KNOTS ( ( 4, 4 ),
 ( 2, 2 ),
 ( 0.000000000000000000, 1.000000000000000000 ),
 ( 0.000000000000000000, 1.000000000000000000 ),
 .UNSPECIFIED. ) 
 GEOMETRIC_REPRESENTATION_ITEM ( )  RATIONAL_B_SPLINE_SURFACE ( (
 ( 1.000000000000000000, 1.000000000000000000),
 ( 0.7789835883360576307, 0.9689951854195403280),
 ( 0.7789835883360576307, 0.9689951854195403280),
 ( 1.000000000000000000, 1.000000000000000000) ) ) 
 REPRESENTATION_ITEM ( '' )  SURFACE ( )  );
#82=B_SPLINE_CURVE_WITH_KNOTS ( 'NONE', 3,
 ( #16407, #22468, #25063, #2733, #11511, #18128 ),
 .UNSPECIFIED., .F., .F.,
 ( 4, 2, 4 ),
 ( 4.906538933386797396E-18, 0.0004335151646191543395, 0.0008670303292383036917 ),
 .UNSPECIFIED. ) ;
#83=CARTESIAN_POINT ( 'NONE',  ( -1.583189561560256253, 11.94859433442902130, -44.83405390829675952 ) ) ;
#85=B_SPLINE_CURVE_WITH_KNOTS ( 'NONE', 3,
 ( #11291, #16435, #20350, #18180, #12122, #2499 ),
 .UNSPECIFIED., .F., .F.,
 ( 4, 2, 4 ),
 ( 3.525929482785130599E-16, 0.003576372551511158761, 0.007152745103021965374 ),
 .UNSPECIFIED. ) ;
#87=CARTESIAN_POINT ( 'NONE',  ( -24.53237795827004319, 33.71192251888839309, -3.868415699415555853 ) ) ;
#98=CARTESIAN_POINT ( 'NONE',  ( -55.24390624410018802, 0.009374879212967415429, 0.004572280736702902422 ) ) ;
#108=CIRCLE ( 'NONE', #9760, 53.53553390275978785 ) ;
#109=CARTESIAN_POINT ( 'NONE',  ( -1.464342487929870096, 35.90631960086420094, -29.09292098541673965 ) ) ;
#115=EDGE_LOOP ( 'NONE', ( #6839, #637, #24909, #28009 ) ) ;
#117=CARTESIAN_POINT ( 'NONE',  ( -16.86833981943422600, -7.884812276281804699, 43.51541671545733436 ) ) ;
#122=ORIENTED_EDGE ( 'NONE', *, *, #1235, .F. ) ;
#123=CARTESIAN_POINT ( 'NONE',  ( -1.048996300304493312, -27.53442103413720332, -36.59642367107734628 ) ) ;
#129=ORIENTED_EDGE ( 'NONE', *, *, #24590, .F. ) ;
#130=CARTESIAN_POINT ( 'NONE',  ( -4.178947244162636743, 48.81675275154077553, -3.367451375481286036 ) ) ;
#131=CARTESIAN_POINT ( 'NONE',  ( -23.79248802219731118, 28.61009539422409631, 16.82188324679449565 ) ) ;
#132=CARTESIAN_POINT ( 'NONE',  ( -1.050229599974486616, -36.90196321294315140, -27.12684363859242254 ) ) ;
#138=CIRCLE ( 'NONE', #7979, 34.60786435723138510 ) ;
#143=B_SPLINE_CURVE_WITH_KNOTS ( 'NONE', 3,
 ( #16043, #26973, #20213, #20507, #7279, #22545, #24997 ),
 .UNSPECIFIED., .F., .F.,
 ( 4, 3, 4 ),
 ( 1.105886215935214523E-17, 0.0007657099931970557912, 0.001530725384384964971 ),
 .UNSPECIFIED. ) ;
#147=CARTESIAN_POINT ( 'NONE',  ( -1.056502255334264895, 45.80535052436397336, -0.5104472526221494055 ) ) ;
#151=CARTESIAN_POINT ( 'NONE',  ( -55.25297051322618813, 0.007247191603129411047, -0.01306918787467283537 ) ) ;
#153=EDGE_CURVE ( 'NONE', #12676, #6634, #10682, .T. ) ;
#155=CARTESIAN_POINT ( 'NONE',  ( -1.583189561560253589, 36.01941156322789084, -29.24830400313178558 ) ) ;
#159=CARTESIAN_POINT ( 'NONE',  ( 60.46576798286869803, -4.195655488513964285E-16, 1.048913872128491071E-16 ) ) ;
#161=CARTESIAN_POINT ( 'NONE',  ( -1.031422197589716205, -43.06660437151298026, 15.60268798220682562 ) ) ;
#164=ADVANCED_FACE ( 'NONE', ( #4090 ), #17761, .F. ) ;
#165=CARTESIAN_POINT ( 'NONE',  ( -55.25719721206881729, -0.004044147484877910065, -0.01041086141212526316 ) ) ;
#169=B_SPLINE_CURVE_WITH_KNOTS ( 'NONE', 3,
 ( #9089, #24504, #26632, #13540, #23032, #14, #6943 ),
 .UNSPECIFIED., .F., .F.,
 ( 4, 3, 4 ),
 ( 0.000000000000000000, 0.006568092053401781462, 0.02506242213020847681 ),
 .UNSPECIFIED. ) ;
#176=FACE_OUTER_BOUND ( 'NONE', #3047, .T. ) ;
#179=ORIENTED_EDGE ( 'NONE', *, *, #12730, .F. ) ;
#183=FACE_OUTER_BOUND ( 'NONE', #401, .T. ) ;
#202=ORIENTED_EDGE ( 'NONE', *, *, #27365, .T. ) ;
#203=CARTESIAN_POINT ( 'NONE',  ( -55.24300891470650754, -0.002702093572892964434, 0.009439835024158798812 ) ) ;
#204=ORIENTED_EDGE ( 'NONE', *, *, #22614, .T. ) ;
#205=CARTESIAN_POINT ( 'NONE',  ( -1.046936909428695328, 43.14407378092994350, -15.35929614323679893 ) ) ;
#206=CARTESIAN_POINT ( 'NONE',  ( -25.21435515916043713, -4.655591116594118617, 34.29329011225960500 ) ) ;
#209=B_SPLINE_CURVE_WITH_KNOTS ( 'NONE', 3,
 ( #19495, #4231, #17048, #26252, #19767, #28124, #6140, #6547 ),
 .UNSPECIFIED., .F., .F.,
 ( 4, 2, 2, 4 ),
 ( 0.000000000000000000, 0.002761524886576660620, 0.005523049773153321240, 0.01104609954630662513 ),
 .UNSPECIFIED. ) ;
#211=VERTEX_POINT ( 'NONE', #55 ) ;
#217=CARTESIAN_POINT ( 'NONE',  ( -1.050230346682673677, -14.15203301556463167, -43.55772679531845881 ) ) ;
#234=CARTESIAN_POINT ( 'NONE',  ( -1.044557008772713180, 15.70482370518816495, -43.01636061108991527 ) ) ;
#241=CARTESIAN_POINT ( 'NONE',  ( -23.79248802219723302, -33.03370827286728684, 3.207402715357496881 ) ) ;
#243=VERTEX_POINT ( 'NONE', #11283 ) ;
#249=CARTESIAN_POINT ( 'NONE',  ( -20.20700224038492010, -16.58740185276728241, -24.51628800869040958 ) ) ;
#250=CARTESIAN_POINT ( 'NONE',  ( -20.47566338032515532, 28.85746366088581283, 7.708089572830123082 ) ) ;
#251=FACE_OUTER_BOUND ( 'NONE', #25592, .T. ) ;
#255=B_SPLINE_CURVE_WITH_KNOTS ( 'NONE', 3,
 ( #24853, #22407, #7154, #15914, #800, #7433, #27419 ),
 .UNSPECIFIED., .F., .F.,
 ( 4, 3, 4 ),
 ( 0.000000000000000000, 0.006568092053401802279, 0.02506242213020847681 ),
 .UNSPECIFIED. ) ;
#264=CARTESIAN_POINT ( 'NONE',  ( -1.048171036023509917, -26.08692787913895472, -37.64178826568597458 ) ) ;
#265=CARTESIAN_POINT ( 'NONE',  ( -1.019300379054419947, 45.76814864815091255, 2.023851374322834573 ) ) ;
#280=ORIENTED_EDGE ( 'NONE', *, *, #15755, .F. ) ;
#286=CARTESIAN_POINT ( 'NONE',  ( -55.24390624410018802, 0.01027195578987812573, -0.001811362924359468263 ) ) ;
#289=ORIENTED_EDGE ( 'NONE', *, *, #8409, .F. ) ;
#291=EDGE_LOOP ( 'NONE', ( #9552, #9379, #25852, #8534 ) ) ;
#294=CARTESIAN_POINT ( 'NONE',  ( -8.786685647604855376, -7.199674155859337787, -53.04920435127184675 ) ) ;
#300=CARTESIAN_POINT ( 'NONE',  ( -9.156249394959713683, -48.78605533024723684, 24.29252099376542517 ) ) ;
#311=ORIENTED_EDGE ( 'NONE', *, *, #19586, .T. ) ;
#319=CARTESIAN_POINT ( 'NONE',  ( -1.050231094221198536, 43.63617436699759367, 13.91061116148147292 ) ) ;
#326=EDGE_LOOP ( 'NONE', ( #25366, #7082, #18538, #9597 ) ) ;
#328=CARTESIAN_POINT ( 'NONE',  ( -55.24198130335446422, -0.008310594958152726572, 0.004163123460802491127 ) ) ;
#329=CARTESIAN_POINT ( 'NONE',  ( -55.24198130335446422, 0.001516807524704581441, 0.009170435128245077103 ) ) ;
#333=ORIENTED_EDGE ( 'NONE', *, *, #2698, .T. ) ;
#336=CARTESIAN_POINT ( 'NONE',  ( -6.574463467970648622, -20.55340846381166742, -47.03022655117394635 ) ) ;
#338=ORIENTED_EDGE ( 'NONE', *, *, #13237, .T. ) ;
#341=CARTESIAN_POINT ( 'NONE',  ( -1.045287976400362417, -28.14015102489855735, -36.12803364096578207 ) ) ;
#345=ORIENTED_EDGE ( 'NONE', *, *, #8746, .T. ) ;
#346=CARTESIAN_POINT ( 'NONE',  ( -20.57838717382308147, 16.28767523336121315, -25.16001208503110931 ) ) ;
#350=EDGE_CURVE ( 'NONE', #18707, #4229, #24424, .T. ) ;
#351=CARTESIAN_POINT ( 'NONE',  ( -55.24300891470650754, -0.009225237711100996510, 0.003362556190412404646 ) ) ;
#361=FACE_OUTER_BOUND ( 'NONE', #15013, .T. ) ;
#367=CARTESIAN_POINT ( 'NONE',  ( -1.155001620486262759, 16.13799328198422245, -42.97366440495917317 ) ) ;
#376=CARTESIAN_POINT ( 'NONE',  ( -8.786685647604885574, 6.096987947571466530E-17, -1.524246986892866633E-17 ) ) ;
#381=ORIENTED_EDGE ( 'NONE', *, *, #6506, .T. ) ;
#395=CARTESIAN_POINT ( 'NONE',  ( -55.25297051322618813, -0.01019003092403672657, 0.01093108995495161231 ) ) ;
#399=ORIENTED_EDGE ( 'NONE', *, *, #9408, .F. ) ;
#401=EDGE_LOOP ( 'NONE', ( #6763, #21380, #8242, #7080 ) ) ;
#406=CARTESIAN_POINT ( 'NONE',  ( -55.24390624410018802, 0.009374879212971231821, -0.004572280736701976080 ) ) ;
#414=VERTEX_POINT ( 'NONE', #12558 ) ;
#423=EDGE_CURVE ( 'NONE', #4272, #25436, #20279, .T. ) ;
#440=LINE ( 'NONE', #9227, #24777 ) ;
#444=CARTESIAN_POINT ( 'NONE',  ( -7.078251931573406708, -47.71415099571790108, 20.86696228105274997 ) ) ;
#446=CARTESIAN_POINT ( 'NONE',  ( -55.24271866751342941, -0.001545935011626541761, -0.009369360294294543784 ) ) ;
#453=CARTESIAN_POINT ( 'NONE',  ( -1.019300379054419947, -28.53917295602871818, 35.83762006677432055 ) ) ;
#457=VERTEX_POINT ( 'NONE', #12411 ) ;
#458=CARTESIAN_POINT ( 'NONE',  ( -55.24271866751342941, 0.001545935011631000867, -0.009369360294295843092 ) ) ;
#461=AXIS2_PLACEMENT_3D ( 'NONE', #8171, #27874, #16935 ) ;
#463=CARTESIAN_POINT ( 'NONE',  ( -55.24198130335446422, 0.009190321388309335635, 0.001391250620105184774 ) ) ;
#466=CARTESIAN_POINT ( 'NONE',  ( -7.078251931573400491, 5.101176922830666705, -51.82710018979476274 ) ) ;
#467=CARTESIAN_POINT ( 'NONE',  ( -20.20700224038492010, 24.51628800869071867, 16.58740185276683832 ) ) ;
#471=CARTESIAN_POINT ( 'NONE',  ( -8.786685647604896232, 25.35688121747570278, 47.14957014837326454 ) ) ;
#473=AXIS2_PLACEMENT_3D ( 'NONE', #13879, #26834, #13590 ) ;
#480=ORIENTED_EDGE ( 'NONE', *, *, #423, .T. ) ;
#483=CARTESIAN_POINT ( 'NONE',  ( -1.048172774974303278, 43.23017713506524728, -15.11899685083838030 ) ) ;
#487=CARTESIAN_POINT ( 'NONE',  ( -1.619063947482197729, -29.22875152547781852, -35.99532424477369830 ) ) ;
#491=EDGE_CURVE ( 'NONE', #21106, #21028, #26123, .T. ) ;
#498=CARTESIAN_POINT ( 'NONE',  ( -1.049817751779873687, -13.66628317065018017, -43.71287583013722156 ) ) ;
#500=CIRCLE ( 'NONE', #6062, 34.60786435723138510 ) ;
#504=CARTESIAN_POINT ( 'NONE',  ( -28.41354790283022069, 1.249099604787076601, -23.16239616762931064 ) ) ;
#506=CARTESIAN_POINT ( 'NONE',  ( -1.113427685306999759, -1.967672929087495470, -45.82016658690750432 ) ) ;
#508=CARTESIAN_POINT ( 'NONE',  ( -20.90916690077964901, -18.74041620980142753, 34.84883504600970383 ) ) ;
#510=CARTESIAN_POINT ( 'NONE',  ( -1.019300379054419947, -38.21680004809145714, 25.26451264419685572 ) ) ;
#530=CARTESIAN_POINT ( 'NONE',  ( -21.41430102051751660, -28.68859753627386766, 11.22990201072307137 ) ) ;
#532=CARTESIAN_POINT ( 'NONE',  ( -20.24399999263414784, 28.55700515887720670, -7.930419334766287243 ) ) ;
#535=B_SPLINE_CURVE_WITH_KNOTS ( 'NONE', 3,
 ( #21357, #5971, #23537, #25826, #16620, #12292, #12840 ),
 .UNSPECIFIED., .F., .F.,
 ( 4, 3, 4 ),
 ( 0.000000000000000000, 0.006568092053401830901, 0.02506242213020847681 ),
 .UNSPECIFIED. ) ;
#537=CARTESIAN_POINT ( 'NONE',  ( -1.583189561560253589, 16.68617981233763814, 43.29471907393723029 ) ) ;
#548=FACE_OUTER_BOUND ( 'NONE', #7468, .T. ) ;
#550=CARTESIAN_POINT ( 'NONE',  ( -8.786685647604890903, -37.00619870957905277, 38.68584556812340480 ) ) ;
#558=CARTESIAN_POINT ( 'NONE',  ( -1.583189561560256253, -38.94740041318311796, -25.21827308671218404 ) ) ;
#559=CARTESIAN_POINT ( 'NONE',  ( -25.21435515916043713, 15.02493970636190745, 31.17620025257570759 ) ) ;
#560=CARTESIAN_POINT ( 'NONE',  ( 14.74894986621300319, -1.023413983156987147E-16, 2.558534957892467869E-17 ) ) ;
#566=CARTESIAN_POINT ( 'NONE',  ( -20.38016308990358638, 29.73560196176844528, -1.509191766064308382 ) ) ;
#567=CARTESIAN_POINT ( 'NONE',  ( -20.20700224038492010, -0.9908225410476447781, 29.58392382092673500 ) ) ;
#570=ORIENTED_EDGE ( 'NONE', *, *, #4414, .T. ) ;
#578=CARTESIAN_POINT ( 'NONE',  ( -22.23226125620942284, 11.82389163795251541, 29.33577758406437042 ) ) ;
#580=ORIENTED_EDGE ( 'NONE', *, *, #26933, .T. ) ;
#581=EDGE_CURVE ( 'NONE', #23740, #22045, #4854, .T. ) ;
#586=CARTESIAN_POINT ( 'NONE',  ( -55.24271866751342941, -0.006671293903667678896, -0.006757859501010191408 ) ) ;
#589=CIRCLE ( 'NONE', #19894, 12.50000000000000000 ) ;
#596=FACE_OUTER_BOUND ( 'NONE', #16790, .T. ) ;
#597=CARTESIAN_POINT ( 'NONE',  ( -4.162674018437132695, -41.48630000627035486, 25.90909455705156006 ) ) ;
#608=DIRECTION ( 'NONE',  ( 0.000000000000000000, 5.223019709707975211E-21, -1.000000000000000000 ) ) ;
#611=CARTESIAN_POINT ( 'NONE',  ( -55.24271866751342941, 0.009388511352200527849, -0.001425019990779188969 ) ) ;
#620=B_SPLINE_CURVE_WITH_KNOTS ( 'NONE', 3,
 ( #10934, #14824, #28333, #23637, #19426, #23909, #17396, #19697, #14681, #26184, #16985, #24049, #3750 ),
 .UNSPECIFIED., .F., .F.,
 ( 4, 3, 3, 3, 4 ),
 ( 9.813077866773594792E-18, 0.0007657099931970658743, 0.001531419946797928045, 0.002296279302920156435, 0.003061450627205745956 ),
 .UNSPECIFIED. ) ;
#629=CARTESIAN_POINT ( 'NONE',  ( -55.24271866751342941, -0.004365563123939050251, 0.008433070970613824532 ) ) ;
#637=ORIENTED_EDGE ( 'NONE', *, *, #19856, .F. ) ;
#638=CARTESIAN_POINT ( 'NONE',  ( -1.539760825549682410, -29.16712717142786460, -35.94320866319479535 ) ) ;
#641=ORIENTED_EDGE ( 'NONE', *, *, #26722, .T. ) ;
#643=CYLINDRICAL_SURFACE ( 'NONE', #10147, 12.50000000000000000 ) ;
#645=LINE ( 'NONE', #22976, #13807 ) ;
#654=VERTEX_POINT ( 'NONE', #3441 ) ;
#655=CARTESIAN_POINT ( 'NONE',  ( -16.86833981943426153, -20.94590537750580239, 38.94907963570745579 ) ) ;
#669=CARTESIAN_POINT ( 'NONE',  ( -22.23342874802670011, -31.55488258420090375, -2.180636882146402833 ) ) ;
#679=DIRECTION ( 'NONE',  ( 1.000000000000000000, -6.938893903907226837E-18, 1.734723475976806709E-18 ) ) ;
#681=EDGE_CURVE ( 'NONE', #27239, #7066, #7645, .T. ) ;
#683=ADVANCED_FACE ( 'NONE', ( #1966 ), #21971, .F. ) ;
#684=CARTESIAN_POINT ( 'NONE',  ( -20.57838717382308147, -7.715628353033481268, 28.96176188950225949 ) ) ;
#693=CARTESIAN_POINT ( 'NONE',  ( -55.24198130335446422, -0.008310594958150379491, -0.004163123460805868634 ) ) ;
#696=CARTESIAN_POINT ( 'NONE',  ( -7.733045908741326357, -51.44704017882769875, 10.42750254442592706 ) ) ;
#699=CARTESIAN_POINT ( 'NONE',  ( -1.259972190295303385, -16.33417789844404666, -43.01178231151323672 ) ) ;
#723=CARTESIAN_POINT ( 'NONE',  ( -1.045287976400365970, -45.76855895860947498, -1.530335034933654859 ) ) ;
#728=CARTESIAN_POINT ( 'NONE',  ( -20.57838717382308147, 16.28767523336157552, 25.16001208503087838 ) ) ;
#736=CARTESIAN_POINT ( 'NONE',  ( -1.239374126674604337, -16.50008610789269170, 42.99367564261294206 ) ) ;
#744=VERTEX_POINT ( 'NONE', #16956 ) ;
#747=SHAPE_REPRESENTATION ( 'pinion', ( #27263 ), #6137 ) ;
#760=CARTESIAN_POINT ( 'NONE',  ( -12.94347594948480662, 35.22469990145658159, 33.69581619287838947 ) ) ;
#763=CARTESIAN_POINT ( 'NONE',  ( -18.41936578851709072, 7.566034416291376630, 41.75701384111728487 ) ) ;
#765=FACE_OUTER_BOUND ( 'NONE', #8133, .T. ) ;
#766=CARTESIAN_POINT ( 'NONE',  ( -1.046936909428682672, -36.28616897897433091, 27.93981068760662012 ) ) ;
#785=CARTESIAN_POINT ( 'NONE',  ( -1.049819825607592794, -14.63675055554412374, -43.39756533277876827 ) ) ;
#786=CARTESIAN_POINT ( 'NONE',  ( -8.259864102781680373, 47.98931516265592734, -22.52209142944943565 ) ) ;
#797=CARTESIAN_POINT ( 'NONE',  ( -1.239374126674604337, -35.79060836339833429, -28.97829083655425819 ) ) ;
#798=LINE ( 'NONE', #7286, #16006 ) ;
#800=CARTESIAN_POINT ( 'NONE',  ( -16.86833981943424376, -43.82216161736207738, 5.948101187262031964 ) ) ;
#802=ORIENTED_EDGE ( 'NONE', *, *, #17983, .T. ) ;
#804=B_SPLINE_CURVE_WITH_KNOTS ( 'NONE', 3,
 ( #21480, #25810, #25951, #14578, #4198, #14991 ),
 .UNSPECIFIED., .F., .F.,
 ( 4, 2, 4 ),
 ( 1.396102177145585797E-16, 0.003570751334075631788, 0.007141502668151123931 ),
 .UNSPECIFIED. ) ;
#817=EDGE_LOOP ( 'NONE', ( #4201, #23942, #19669, #10493 ) ) ;
#820=B_SPLINE_CURVE_WITH_KNOTS ( 'NONE', 3,
 ( #26367, #13402, #6669, #22352, #26505, #15555 ),
 .UNSPECIFIED., .F., .F.,
 ( 4, 2, 4 ),
 ( 0.000000000000000000, 0.0004335184443140219679, 0.0008670368886280439358 ),
 .UNSPECIFIED. ) ;
#829=ORIENTED_EDGE ( 'NONE', *, *, #16054, .F. ) ;
#836=DIRECTION ( 'NONE',  ( 0.7563875759206388771, -0.5078650950445684487, -0.4122509917856733708 ) ) ;
#838=CARTESIAN_POINT ( 'NONE',  ( -2.265401668238153032, -45.46007138824032978, 11.98901689611089516 ) ) ;
#841=CARTESIAN_POINT ( 'NONE',  ( -1.031422197589711987, -37.93675465142491277, -25.67058493451428802 ) ) ;
#842=CARTESIAN_POINT ( 'NONE',  ( -1.045287976400351981, 12.68782741917293855, -44.00138577190654132 ) ) ;
#848=CARTESIAN_POINT ( 'NONE',  ( -12.94347594948482971, 47.96504705787755540, -8.691477019903484091 ) ) ;
#849=B_SPLINE_CURVE_WITH_KNOTS ( 'NONE', 3,
 ( #13988, #5213, #7380, #18743, #3201, #14264 ),
 .UNSPECIFIED., .F., .F.,
 ( 4, 2, 4 ),
 ( 1.512296865354101973E-16, 0.003570751334075637860, 0.007141502668151123931 ),
 .UNSPECIFIED. ) ;
#850=FACE_OUTER_BOUND ( 'NONE', #1927, .T. ) ;
#854=EDGE_LOOP ( 'NONE', ( #27943, #8561, #14969, #11566 ) ) ;
#855=CARTESIAN_POINT ( 'NONE',  ( -1.050230346682680560, 45.79907861045643358, 0.0006945978177289460027 ) ) ;
#859=CARTESIAN_POINT ( 'NONE',  ( -20.20612092514784308, 24.59769888281557471, 16.46550332780499559 ) ) ;
#863=CARTESIAN_POINT ( 'NONE',  ( -28.13707043255157103, 22.00298671236740233, -6.342158660427079653 ) ) ;
#864=VERTEX_POINT ( 'NONE', #18350 ) ;
#865=ORIENTED_EDGE ( 'NONE', *, *, #5403, .T. ) ;
#881=ORIENTED_EDGE ( 'NONE', *, *, #1372, .T. ) ;
#882=ADVANCED_FACE ( 'NONE', ( #22853 ), #3615, .T. ) ;
#890=CARTESIAN_POINT ( 'NONE',  ( -1.239374126674604337, -35.79060836339793639, 28.97829083655478399 ) ) ;
#894=CARTESIAN_POINT ( 'NONE',  ( -25.21435515916043002, 4.655591116594353984, -34.29329011225956947 ) ) ;
#895=EDGE_LOOP ( 'NONE', ( #11336, #3517, #24492, #9208 ) ) ;
#896=DIRECTION ( 'NONE',  ( 1.000000000000000000, -6.938893903907226837E-18, 1.734723475976806709E-18 ) ) ;
#898=B_SPLINE_CURVE_WITH_KNOTS ( 'NONE', 3,
 ( #12919, #4423, #19967, #6193, #23893, #22132, #21854, #13195, #28315, #8480 ),
 .UNSPECIFIED., .F., .F.,
 ( 4, 2, 2, 2, 4 ),
 ( 1.563658610346375379E-18, 0.0003346267210630944644, 0.0006692534421261873024, 0.001003880163189280195, 0.001338506884252373087 ),
 .UNSPECIFIED. ) ;
#900=CARTESIAN_POINT ( 'NONE',  ( -20.20700224038492365, -8.199606986804534259, -28.44216453106533748 ) ) ;
#901=CARTESIAN_POINT ( 'NONE',  ( -8.786685647604894456, 37.00619870957989832, 38.68584556812258768 ) ) ;
#905=CARTESIAN_POINT ( 'NONE',  ( -9.156249394959713683, -25.18996226954579498, 48.32878616081037393 ) ) ;
#929=LINE ( 'NONE', #3380, #25774 ) ;
#936=ORIENTED_EDGE ( 'NONE', *, *, #17252, .F. ) ;
#950=ORIENTED_EDGE ( 'NONE', *, *, #18124, .T. ) ;
#955=CARTESIAN_POINT ( 'NONE',  ( -1.058473599757824735, 1.755404039370064950, 45.77379534793241334 ) ) ;
#961=( BOUNDED_SURFACE ( )  B_SPLINE_SURFACE ( 3, 1, ( 
 ( #5989, #12724 ),
 ( #25708, #23410 ),
 ( #21373, #8153 ),
 ( #5708, #5847 ) ),
 .UNSPECIFIED., .F., .F., .F. ) 
 B_SPLINE_SURFACE_WITH_KNOTS ( ( 4, 4 ),
 ( 2, 2 ),
 ( 0.000000000000000000, 1.000000000000000000 ),
 ( 0.000000000000000000, 1.000000000000000000 ),
 .UNSPECIFIED. ) 
 GEOMETRIC_REPRESENTATION_ITEM ( )  RATIONAL_B_SPLINE_SURFACE ( (
 ( 1.000000000000000000, 1.000000000000000000),
 ( 0.7789835883360576307, 0.9689951854195403280),
 ( 0.7789835883360576307, 0.9689951854195403280),
 ( 1.000000000000000000, 1.000000000000000000) ) ) 
 REPRESENTATION_ITEM ( '' )  SURFACE ( )  );
#962=ORIENTED_EDGE ( 'NONE', *, *, #8677, .F. ) ;
#965=( NAMED_UNIT ( * ) PLANE_ANGLE_UNIT ( ) SI_UNIT ( $, .RADIAN. ) );
#967=CARTESIAN_POINT ( 'NONE',  ( -1.048172774974287069, 15.11899685083884393, 43.23017713506509097 ) ) ;
#975=VECTOR ( 'NONE', #24764, 1000.000000000000000 ) ;
#976=VERTEX_POINT ( 'NONE', #7085 ) ;
#980=ADVANCED_FACE ( 'NONE', ( #26487 ), #2904, .F. ) ;
#985=CARTESIAN_POINT ( 'NONE',  ( -20.20700224038492010, -18.19058640100240254, -23.35150625415651859 ) ) ;
#987=VERTEX_POINT ( 'NONE', #728 ) ;
#990=CARTESIAN_POINT ( 'NONE',  ( -1.058473599757832062, 44.07591602137171094, 12.47539220917817815 ) ) ;
#992=EDGE_CURVE ( 'NONE', #14085, #11759, #7270, .T. ) ;
#993=CARTESIAN_POINT ( 'NONE',  ( -20.47566338032516597, -27.87687989047309145, 10.72601609985058957 ) ) ;
#1004=ORIENTED_EDGE ( 'NONE', *, *, #3036, .F. ) ;
#1005=CARTESIAN_POINT ( 'NONE',  ( -1.048994561756802169, -14.87838255483227101, 43.31369460697990803 ) ) ;
#1013=CARTESIAN_POINT ( 'NONE',  ( -20.57838717382308147, -27.96569011373093971, -10.78122205916989529 ) ) ;
#1016=CARTESIAN_POINT ( 'NONE',  ( -55.25719721206881729, 0.0006290797159235729736, 0.01115102788683339750 ) ) ;
#1018=EDGE_CURVE ( 'NONE', #18216, #9135, #11027, .T. ) ;
#1026=LINE ( 'NONE', #12112, #16910 ) ;
#1031=CARTESIAN_POINT ( 'NONE',  ( -7.733045908741322805, -45.70676731105703539, 25.81515396910911875 ) ) ;
#1033=CARTESIAN_POINT ( 'NONE',  ( -1.259972190295298500, 38.49631882650683679, 25.19627397134255986 ) ) ;
#1038=EDGE_LOOP ( 'NONE', ( #13079, #8094, #11343, #21519 ) ) ;
#1039=ORIENTED_EDGE ( 'NONE', *, *, #17983, .F. ) ;
#1042=PRODUCT_DEFINITION_CONTEXT ( 'detailed design', #27763, 'design' ) ;
#1046=EDGE_CURVE ( 'NONE', #8158, #19215, #440, .T. ) ;
#1050=EDGE_CURVE ( 'NONE', #17941, #7710, #9660, .T. ) ;
#1056=CARTESIAN_POINT ( 'NONE',  ( -20.20700224038492721, -23.35150625415671755, -18.19058640100215385 ) ) ;
#1059=CARTESIAN_POINT ( 'NONE',  ( -20.47566262905010248, 29.82700878811083811, 1.586617686065662447 ) ) ;
#1064=CARTESIAN_POINT ( 'NONE',  ( -1.048171036023507252, 43.86077206077069235, -13.17819047681618372 ) ) ;
#1069=VECTOR ( 'NONE', #13291, 1000.000000000000114 ) ;
#1079=CARTESIAN_POINT ( 'NONE',  ( -1.056502255334265339, 26.51074901220557933, 37.35734037467605617 ) ) ;
#1082=CARTESIAN_POINT ( 'NONE',  ( -20.20612092514784663, 10.22177639105900226, 27.77903665678154255 ) ) ;
#1085=VECTOR ( 'NONE', #3210, 999.9999999999998863 ) ;
#1086=VERTEX_POINT ( 'NONE', #14540 ) ;
#1089=CARTESIAN_POINT ( 'NONE',  ( -23.79223135445720061, 13.25822371132295352, -30.42557260166815780 ) ) ;
#1100=CARTESIAN_POINT ( 'NONE',  ( -28.13707043255157103, 21.52861750560949972, 7.802116958608778852 ) ) ;
#1106=ORIENTED_EDGE ( 'NONE', *, *, #3667, .F. ) ;
#1114=DIRECTION ( 'NONE',  ( 0.7563875759206387661, -0.6320336713238486892, 0.1685564395263406956 ) ) ;
#1115=DIRECTION ( 'NONE',  ( -0.7637818620346801257, 0.3965875333584876761, 0.5092696688508626668 ) ) ;
#1123=ORIENTED_EDGE ( 'NONE', *, *, #14062, .T. ) ;
#1128=CARTESIAN_POINT ( 'NONE',  ( -55.24271866751342941, 0.006671293903668397071, 0.006757859501010046559 ) ) ;
#1129=CARTESIAN_POINT ( 'NONE',  ( -1.058197053496160667, -12.47644286888545828, -44.07533330186785037 ) ) ;
#1134=CARTESIAN_POINT ( 'NONE',  ( -4.780792508754322157, 42.16805077400959334, -25.98388465890095489 ) ) ;
#1146=CARTESIAN_POINT ( 'NONE',  ( -55.24390624410018802, -0.004572280736701530256, -0.009374879212970928244 ) ) ;
#1147=B_SPLINE_CURVE_WITH_KNOTS ( 'NONE', 3,
 ( #28328, #10655, #16980, #17256, #28191, #14819, #8493, #1996, #25772, #8360 ),
 .UNSPECIFIED., .F., .F.,
 ( 4, 2, 2, 2, 4 ),
 ( 1.301042606982605128E-18, 0.0003346267210630945186, 0.0006692534421261877361, 0.001003880163189281062, 0.001338506884252374171 ),
 .UNSPECIFIED. ) ;
#1153=ORIENTED_EDGE ( 'NONE', *, *, #11866, .T. ) ;
#1154=CARTESIAN_POINT ( 'NONE',  ( -22.23226125620943705, -11.82389163795231468, -29.33577758406444858 ) ) ;
#1155=EDGE_CURVE ( 'NONE', #22965, #4951, #14176, .T. ) ;
#1157=CARTESIAN_POINT ( 'NONE',  ( -8.786685647604890903, 52.67761315067286176, -9.545808661480789326 ) ) ;
#1173=CARTESIAN_POINT ( 'NONE',  ( -28.41354790283022069, 22.41474081378001060, -5.969609727608100158 ) ) ;
#1178=B_SPLINE_CURVE_WITH_KNOTS ( 'NONE', 3,
 ( #4774, #26495, #24660, #13542, #6801, #20160, #9236 ),
 .UNSPECIFIED., .F., .F.,
 ( 4, 3, 4 ),
 ( 0.000000000000000000, 0.006568092053401771921, 0.02506242213020852885 ),
 .UNSPECIFIED. ) ;
#1194=CARTESIAN_POINT ( 'NONE',  ( -25.21435515916042647, 25.00736669481023355, -23.92354251275945742 ) ) ;
#1200=CARTESIAN_POINT ( 'NONE',  ( -1.056502255334264895, -45.80535052436396626, 0.5104472526224692608 ) ) ;
#1202=ORIENTED_EDGE ( 'NONE', *, *, #26611, .F. ) ;
#1208=EDGE_CURVE ( 'NONE', #25606, #12851, #25348, .T. ) ;
#1215=CARTESIAN_POINT ( 'NONE',  ( -1.031422197589716205, 28.14735071801795740, 36.13727897780097464 ) ) ;
#1219=CARTESIAN_POINT ( 'NONE',  ( -4.162674018437132695, -45.34593312138897403, -18.33413805792422124 ) ) ;
#1224=DIRECTION ( 'NONE',  ( -0.7637818620346800147, 0.3617919495470713898, -0.5345501402766312804 ) ) ;
#1230=CARTESIAN_POINT ( 'NONE',  ( -1.113548883309550375, 35.91246368318242332, 28.52482525634906096 ) ) ;
#1234=CARTESIAN_POINT ( 'NONE',  ( -1.259972190295306715, -38.49631882650665204, -25.19627397134285474 ) ) ;
#1235=EDGE_CURVE ( 'NONE', #5518, #15303, #12658, .T. ) ;
#1245=LINE ( 'NONE', #10043, #19404 ) ;
#1250=CARTESIAN_POINT ( 'NONE',  ( -25.21435515916025594, 1.749597353048488237E-16, -4.373993382621220594E-17 ) ) ;
#1252=ORIENTED_EDGE ( 'NONE', *, *, #4451, .F. ) ;
#1265=CARTESIAN_POINT ( 'NONE',  ( -20.20612091757422846, -29.57813639663779526, -1.137293889216260512 ) ) ;
#1268=EDGE_CURVE ( 'NONE', #14951, #7509, #6412, .T. ) ;
#1275=CARTESIAN_POINT ( 'NONE',  ( -20.20700224038492721, -16.58740185276692358, 24.51628800869065827 ) ) ;
#1280=CARTESIAN_POINT ( 'NONE',  ( -1.058197053496165552, -1.754224732379234153, 45.77356582045592859 ) ) ;
#1281=DIRECTION ( 'NONE',  ( 1.000000000000000000, -6.938893903907226837E-18, 1.734723475976806709E-18 ) ) ;
#1283=CARTESIAN_POINT ( 'NONE',  ( -1.045287976400362417, -44.00138577190658395, -12.68782741917276446 ) ) ;
#1295=CARTESIAN_POINT ( 'NONE',  ( -20.57838717382308147, -10.78122205917020437, -27.96569011373082603 ) ) ;
#1301=VERTEX_POINT ( 'NONE', #15503 ) ;
#1303=CARTESIAN_POINT ( 'NONE',  ( -1.048172774974290178, -1.020161070261438097, -45.78636862970792265 ) ) ;
#1311=ADVANCED_FACE ( 'NONE', ( #24462 ), #27356, .F. ) ;
#1319=B_SPLINE_CURVE_WITH_KNOTS ( 'NONE', 3,
 ( #27351, #7664, #14399, #7361, #5191, #16423, #3046, #3324, #23209, #25207 ),
 .UNSPECIFIED., .F., .F.,
 ( 4, 2, 2, 2, 4 ),
 ( 2.877728285596781101E-16, 0.0003346187017559061659, 0.0006692374035115240425, 0.001003856105267141811, 0.001338474807022759687 ),
 .UNSPECIFIED. ) ;
#1320=B_SPLINE_CURVE_WITH_KNOTS ( 'NONE', 3,
 ( #1056, #9415, #18168, #24823 ),
 .UNSPECIFIED., .F., .F.,
 ( 4, 4 ),
 ( 1.956780383866537384E-16, 0.001982023823822938111 ),
 .UNSPECIFIED. ) ;
#1328=CARTESIAN_POINT ( 'NONE',  ( -20.20700224038492721, 24.51628800869048419, -16.58740185276719359 ) ) ;
#1332=ADVANCED_FACE ( 'NONE', ( #15945 ), #26418, .F. ) ;
#1337=ORIENTED_EDGE ( 'NONE', *, *, #26697, .F. ) ;
#1339=ORIENTED_EDGE ( 'NONE', *, *, #15826, .F. ) ;
#1344=ORIENTED_EDGE ( 'NONE', *, *, #7073, .T. ) ;
#1346=ORIENTED_EDGE ( 'NONE', *, *, #9836, .F. ) ;
#1347=EDGE_LOOP ( 'NONE', ( #5434, #21722, #24363, #12048 ) ) ;
#1363=DIRECTION ( 'NONE',  ( 0.000000000000000000, 5.223019709708190374E-21, -1.000000000000000000 ) ) ;
#1364=CARTESIAN_POINT ( 'NONE',  ( -55.25297051322618813, 0.01306918787467630481, -0.007247191603131783282 ) ) ;
#1366=ORIENTED_EDGE ( 'NONE', *, *, #5235, .T. ) ;
#1367=LINE ( 'NONE', #12307, #28094 ) ;
#1368=AXIS2_PLACEMENT_3D ( 'NONE', #560, #24901, #18110 ) ;
#1372=EDGE_CURVE ( 'NONE', #7217, #13229, #23622, .T. ) ;
#1373=CARTESIAN_POINT ( 'NONE',  ( -1.113427685307002424, -38.22586258295212502, -25.34053733836516642 ) ) ;
#1395=ORIENTED_EDGE ( 'NONE', *, *, #16762, .F. ) ;
#1396=ORIENTED_EDGE ( 'NONE', *, *, #581, .F. ) ;
#1397=CARTESIAN_POINT ( 'NONE',  ( -2.911734481061388990, -47.57875121082950898, 2.802366807346684308 ) ) ;
#1408=CARTESIAN_POINT ( 'NONE',  ( -1.048996300304495310, 13.42280206896976757, -43.78665266739842110 ) ) ;
#1411=CARTESIAN_POINT ( 'NONE',  ( -55.24390624410018802, -0.01027195578987734684, 0.001811362924359352471 ) ) ;
#1415=AXIS2_PLACEMENT_3D ( 'NONE', #17030, #21631, #21494 ) ;
#1422=CARTESIAN_POINT ( 'NONE',  ( -1.583189561560252701, -11.94859433442933394, -44.83405390829668136 ) ) ;
#1423=VERTEX_POINT ( 'NONE', #18543 ) ;
#1441=CARTESIAN_POINT ( 'NONE',  ( -16.86833981943423666, 43.51541671545732726, 7.884812276281646604 ) ) ;
#1450=CARTESIAN_POINT ( 'NONE',  ( -1.019300379054419947, -45.76814864815092676, -2.023851374322514829 ) ) ;
#1452=B_SPLINE_CURVE_WITH_KNOTS ( 'NONE', 3,
 ( #16150, #24955, #5215, #13989, #22799, #20610, #894 ),
 .UNSPECIFIED., .F., .F.,
 ( 4, 3, 4 ),
 ( 2.299948302575412283E-16, 0.009512539173626367167, 0.02506242213020821313 ),
 .UNSPECIFIED. ) ;
#1453=CARTESIAN_POINT ( 'NONE',  ( -20.57838717382308147, -25.16001208503117326, -16.28767523336112433 ) ) ;
#1456=AXIS2_PLACEMENT_3D ( 'NONE', #12266, #5805, #12682 ) ;
#1477=CONICAL_SURFACE ( 'NONE', #24938, 34.60786435723138510, 0.8559913436420825139 ) ;
#1480=PLANE ( 'NONE',  #4389 ) ;
#1484=VERTEX_POINT ( 'NONE', #10762 ) ;
#1492=VECTOR ( 'NONE', #28184, 1000.000000000000114 ) ;
#1494=CARTESIAN_POINT ( 'NONE',  ( -20.38016308990357217, 16.25718651464982045, -24.94368798801356490 ) ) ;
#1495=DIRECTION ( 'NONE',  ( -1.000000000000000000, 6.938893903907226837E-18, -1.734723475976806709E-18 ) ) ;
#1500=CARTESIAN_POINT ( 'NONE',  ( -55.25297051322618813, 0.001818774723749745246, 0.01483298743814625079 ) ) ;
#1503=VERTEX_POINT ( 'NONE', #9304 ) ;
#1505=CARTESIAN_POINT ( 'NONE',  ( -6.588769196390771299, 11.07780292579764847, 50.13301368233286581 ) ) ;
#1512=CONICAL_SURFACE ( 'NONE', #26330, 34.60786435723138510, 0.8559913436420825139 ) ;
#1516=CONICAL_SURFACE ( 'NONE', #12542, 34.60786435723138510, 0.8559913436420825139 ) ;
#1531=CARTESIAN_POINT ( 'NONE',  ( -1.045287976400379737, 44.00138577190644185, -12.68782741917337198 ) ) ;
#1533=EDGE_CURVE ( 'NONE', #6666, #21211, #6780, .T. ) ;
#1536=EDGE_CURVE ( 'NONE', #18316, #12676, #798, .T. ) ;
#1543=CARTESIAN_POINT ( 'NONE',  ( -12.94347594948482083, -33.69581619287849605, 35.22469990145643948 ) ) ;
#1566=DIRECTION ( 'NONE',  ( 0.7637818620346800147, -0.1788995134688871336, -0.6201872550346648749 ) ) ;
#1570=CARTESIAN_POINT ( 'NONE',  ( -1.464342487929843006, -11.94843286121887438, 44.64187261869788870 ) ) ;
#1571=CARTESIAN_POINT ( 'NONE',  ( -1.049817751779889008, -43.39729912094389874, -14.63752841325032250 ) ) ;
#1573=CARTESIAN_POINT ( 'NONE',  ( -21.41427618760446450, 1.815001260755841450, -30.75468365310879193 ) ) ;
#1578=CARTESIAN_POINT ( 'NONE',  ( -1.058197053496163109, -28.32422455455050425, 36.00048521498983689 ) ) ;
#1581=VERTEX_POINT ( 'NONE', #5113 ) ;
#1586=CARTESIAN_POINT ( 'NONE',  ( -1.113427685307000203, 12.28784199929934751, -44.18561238466741514 ) ) ;
#1587=CARTESIAN_POINT ( 'NONE',  ( -1.155001620486242553, 42.97366440495935080, 16.13799328198379257 ) ) ;
#1590=EDGE_LOOP ( 'NONE', ( #5054, #21491, #20191, #21560 ) ) ;
#1592=CARTESIAN_POINT ( 'NONE',  ( -55.24340739397742084, 0.0007387096945740994529, -0.01010924026184336841 ) ) ;
#1593=CARTESIAN_POINT ( 'NONE',  ( -1.463510566862833207, -25.15876608740840936, -38.76366072687767428 ) ) ;
#1604=EDGE_CURVE ( 'NONE', #15835, #16671, #25426, .T. ) ;
#1608=CARTESIAN_POINT ( 'NONE',  ( -1.031422197589711764, 12.69107518035563587, 44.01264471863832739 ) ) ;
#1619=FACE_OUTER_BOUND ( 'NONE', #12979, .T. ) ;
#1625=ORIENTED_EDGE ( 'NONE', *, *, #10400, .F. ) ;
#1629=EDGE_LOOP ( 'NONE', ( #27024, #6614, #11939, #20985 ) ) ;
#1632=EDGE_CURVE ( 'NONE', #13229, #18707, #8018, .T. ) ;
#1643=CARTESIAN_POINT ( 'NONE',  ( -21.81686047589429833, -6.867757412720954413, -37.90526371014254892 ) ) ;
#1651=ORIENTED_EDGE ( 'NONE', *, *, #11503, .F. ) ;
#1652=ORIENTED_EDGE ( 'NONE', *, *, #17166, .F. ) ;
#1653=ADVANCED_FACE ( 'NONE', ( #15015, #8421 ), #23548, .F. ) ;
#1654=CARTESIAN_POINT ( 'NONE',  ( -1.058473599757826511, -38.06357893967446415, -25.48501014712384816 ) ) ;
#1661=CARTESIAN_POINT ( 'NONE',  ( -1.031422197589711987, 15.60268798220698727, 43.06660437151290211 ) ) ;
#1670=CARTESIAN_POINT ( 'NONE',  ( -1.619063947482197729, 44.80407745103800465, 11.94059994246113021 ) ) ;
#1678=FACE_OUTER_BOUND ( 'NONE', #5902, .T. ) ;
#1680=CARTESIAN_POINT ( 'NONE',  ( -22.34422965417125440, -16.46028608106132651, -34.15536449444082479 ) ) ;
#1692=B_SPLINE_CURVE_WITH_KNOTS ( 'NONE', 3,
 ( #11741, #26695, #24576, #4833, #7726, #1505, #12973, #12300 ),
 .UNSPECIFIED., .F., .F.,
 ( 4, 2, 2, 4 ),
 ( 2.237231151233565423E-16, 0.002761568181852865501, 0.005523136363705507222, 0.01104627272741080454 ),
 .UNSPECIFIED. ) ;
#1698=CARTESIAN_POINT ( 'NONE',  ( -55.25297051322618813, 0.01354497706059544504, -0.006313402748432239003 ) ) ;
#1700=CARTESIAN_POINT ( 'NONE',  ( -25.21435515916043713, -4.655591116594118617, 34.29329011225960500 ) ) ;
#1701=CARTESIAN_POINT ( 'NONE',  ( -1.619063947482197729, -11.94059994246129008, 44.80407745103795492 ) ) ;
#1703=CARTESIAN_POINT ( 'NONE',  ( -1.044556982611274831, 36.05793013899099719, -28.22896456560681600 ) ) ;
#1705=CARTESIAN_POINT ( 'NONE',  ( -4.473127245936431073, 41.70021447285055416, -26.34600523034553277 ) ) ;
#1712=( BOUNDED_SURFACE ( )  B_SPLINE_SURFACE ( 3, 1, ( 
 ( #8468, #17503 ),
 ( #19664, #19956 ),
 ( #24147, #4548 ),
 ( #21973, #3991 ) ),
 .UNSPECIFIED., .F., .F., .F. ) 
 B_SPLINE_SURFACE_WITH_KNOTS ( ( 4, 4 ),
 ( 2, 2 ),
 ( 0.000000000000000000, 1.000000000000000000 ),
 ( 0.000000000000000000, 1.000000000000000000 ),
 .UNSPECIFIED. ) 
 GEOMETRIC_REPRESENTATION_ITEM ( )  RATIONAL_B_SPLINE_SURFACE ( (
 ( 1.000000000000000000, 1.000000000000000000),
 ( 0.9934239774497838349, 0.8357310067453913582),
 ( 0.9934239774497838349, 0.8357310067453913582),
 ( 1.000000000000000000, 1.000000000000000000) ) ) 
 REPRESENTATION_ITEM ( '' )  SURFACE ( )  );
#1718=CARTESIAN_POINT ( 'NONE',  ( -1.619063947482201282, 43.26576862488434472, -16.67502769180576649 ) ) ;
#1721=ORIENTED_EDGE ( 'NONE', *, *, #6154, .T. ) ;
#1723=CARTESIAN_POINT ( 'NONE',  ( -55.24390624410018802, 0.001811362924362862900, -0.01027195578988028025 ) ) ;
#1725=B_SPLINE_CURVE_WITH_KNOTS ( 'NONE', 3,
 ( #7037, #2842, #24879, #15795, #27150, #5141 ),
 .UNSPECIFIED., .F., .F.,
 ( 4, 2, 4 ),
 ( 0.000000000000000000, 0.003570751334075635691, 0.007141502668151271382 ),
 .UNSPECIFIED. ) ;
#1730=CARTESIAN_POINT ( 'NONE',  ( -7.733045908741324581, 35.49239760110675945, -38.67583825854160295 ) ) ;
#1735=ORIENTED_EDGE ( 'NONE', *, *, #27850, .T. ) ;
#1739=B_SPLINE_CURVE_WITH_KNOTS ( 'NONE', 3,
 ( #25007, #26980, #22552, #22703, #14316, #20941 ),
 .UNSPECIFIED., .F., .F.,
 ( 4, 2, 4 ),
 ( 4.653458371169123007E-16, 0.003576372551511270217, 0.007152745103022075529 ),
 .UNSPECIFIED. ) ;
#1746=CARTESIAN_POINT ( 'NONE',  ( -1.048172774974279076, 45.78636862970795107, -1.020161070261278224 ) ) ;
#1759=EDGE_LOOP ( 'NONE', ( #21545, #6302, #17364, #18495 ) ) ;
#1762=CARTESIAN_POINT ( 'NONE',  ( -20.57838717382308147, -7.715628353033481268, 28.96176188950225949 ) ) ;
#1763=CARTESIAN_POINT ( 'NONE',  ( -1.619063947482197729, -43.26576862488421682, 16.67502769180607203 ) ) ;
#1770=ADVANCED_FACE ( 'NONE', ( #22513 ), #16698, .F. ) ;
#1775=ORIENTED_EDGE ( 'NONE', *, *, #12128, .F. ) ;
#1777=CARTESIAN_POINT ( 'NONE',  ( -2.911734481061364566, -40.13920818157090054, -25.69892591260251535 ) ) ;
#1781=CARTESIAN_POINT ( 'NONE',  ( -20.20612092514784308, -16.46550332780508796, 24.59769888281551786 ) ) ;
#1782=ORIENTED_EDGE ( 'NONE', *, *, #5338, .F. ) ;
#1786=CARTESIAN_POINT ( 'NONE',  ( -55.24271866751342941, 0.001425019990779439203, 0.009388511352200054269 ) ) ;
#1787=ORIENTED_EDGE ( 'NONE', *, *, #8404, .F. ) ;
#1788=VERTEX_POINT ( 'NONE', #4371 ) ;
#1801=EDGE_CURVE ( 'NONE', #211, #8086, #12986, .T. ) ;
#1802=B_SPLINE_CURVE_WITH_KNOTS ( 'NONE', 3,
 ( #12381, #16568, #5636, #14404, #10104, #8097 ),
 .UNSPECIFIED., .F., .F.,
 ( 4, 2, 4 ),
 ( 4.906538933386797396E-18, 0.0004335151646191519543, 0.0008670303292382989212 ),
 .UNSPECIFIED. ) ;
#1810=CARTESIAN_POINT ( 'NONE',  ( -1.539763995773685945, 25.17088606276602647, 38.84665165401036546 ) ) ;
#1830=B_SPLINE_CURVE_WITH_KNOTS ( 'NONE', 3,
 ( #3651, #21635, #25696, #10712, #4073, #6386 ),
 .UNSPECIFIED., .F., .F.,
 ( 4, 2, 4 ),
 ( 1.734723475976807094E-18, 0.0004335184443140231605, 0.0008670368886280445863 ),
 .UNSPECIFIED. ) ;
#1836=LINE ( 'NONE', #8344, #47 ) ;
#1837=FACE_OUTER_BOUND ( 'NONE', #20975, .T. ) ;
#1846=EDGE_CURVE ( 'NONE', #12851, #15769, #22664, .T. ) ;
#1854=CARTESIAN_POINT ( 'NONE',  ( -20.57838717382308502, 27.96569011373086866, -10.78122205917010135 ) ) ;
#1855=CARTESIAN_POINT ( 'NONE',  ( -55.24340739397742794, 0.009842732675349290250, 0.002421372372456403153 ) ) ;
#1858=ORIENTED_EDGE ( 'NONE', *, *, #9631, .F. ) ;
#1860=CARTESIAN_POINT ( 'NONE',  ( -1.056502255334264895, -13.66916755949820583, 43.72121397317236102 ) ) ;
#1862=CARTESIAN_POINT ( 'NONE',  ( -1.048996300304505747, -37.49570739463903379, -26.29666317565288480 ) ) ;
#1863=B_SPLINE_CURVE_WITH_KNOTS ( 'NONE', 3,
 ( #471, #5221, #27080, #13419, #17871, #13564, #7255 ),
 .UNSPECIFIED., .F., .F.,
 ( 4, 3, 4 ),
 ( 1.430489624538199204E-17, 0.009512539173626433087, 0.02506242213020844906 ),
 .UNSPECIFIED. ) ;
#1866=CARTESIAN_POINT ( 'NONE',  ( -4.780792508754315051, -37.74278713234418348, -32.07473752860764904 ) ) ;
#1872=VECTOR ( 'NONE', #11255, 1000.000000000000114 ) ;
#1879=CARTESIAN_POINT ( 'NONE',  ( -1.031422197589716205, -36.13727897780147202, -28.14735071801731792 ) ) ;
#1883=EDGE_CURVE ( 'NONE', #20968, #8074, #1320, .T. ) ;
#1899=CARTESIAN_POINT ( 'NONE',  ( -1.045287976400365970, 15.59869763335156101, 43.05558670614217931 ) ) ;
#1904=EDGE_LOOP ( 'NONE', ( #15098, #13288, #13142, #27561 ) ) ;
#1909=CARTESIAN_POINT ( 'NONE',  ( -1.046936909428682672, 43.93225665392633061, 12.93351869073227611 ) ) ;
#1911=CARTESIAN_POINT ( 'NONE',  ( -12.82751273423880711, 35.32125660155448088, -33.78816682541299343 ) ) ;
#1912=CARTESIAN_POINT ( 'NONE',  ( -7.733045908741344121, 38.67583825854200086, 35.49239760110631181 ) ) ;
#1915=CARTESIAN_POINT ( 'NONE',  ( -1.050231094221226291, 36.90262059116464854, -27.12595454131517769 ) ) ;
#1921=CARTESIAN_POINT ( 'NONE',  ( -1.583189561560253589, 29.24830400313217638, 36.01941156322755688 ) ) ;
#1924=CARTESIAN_POINT ( 'NONE',  ( -4.178947244162637631, -31.41809272265950170, -37.51424432987639079 ) ) ;
#1927=EDGE_LOOP ( 'NONE', ( #17824, #15062, #17328, #17776 ) ) ;
#1929=B_SPLINE_CURVE_WITH_KNOTS ( 'NONE', 3,
 ( #27527, #5508, #5814, #8116 ),
 .UNSPECIFIED., .F., .F.,
 ( 4, 4 ),
 ( 0.0009910334943225120648, 0.001982023823822943315 ),
 .UNSPECIFIED. ) ;
#1934=CONICAL_SURFACE ( 'NONE', #18012, 34.60786435723138510, 0.8559913436420825139 ) ;
#1936=CARTESIAN_POINT ( 'NONE',  ( -20.20700224038492721, 0.9908225410482660589, 29.58392382092671724 ) ) ;
#1940=CARTESIAN_POINT ( 'NONE',  ( -55.24340739397742794, -0.009386184976284812215, 0.003826481709800012669 ) ) ;
#1943=CARTESIAN_POINT ( 'NONE',  ( -55.24271866751342941, 0.008488649505346579707, -0.004256484107793386679 ) ) ;
#1952=( BOUNDED_SURFACE ( )  B_SPLINE_SURFACE ( 3, 1, ( 
 ( #11016, #6280 ),
 ( #10744, #17553 ),
 ( #13661, #9210 ),
 ( #26476, #6781 ) ),
 .UNSPECIFIED., .F., .F., .F. ) 
 B_SPLINE_SURFACE_WITH_KNOTS ( ( 4, 4 ),
 ( 2, 2 ),
 ( 0.000000000000000000, 1.000000000000000000 ),
 ( 0.000000000000000000, 1.000000000000000000 ),
 .UNSPECIFIED. ) 
 GEOMETRIC_REPRESENTATION_ITEM ( )  RATIONAL_B_SPLINE_SURFACE ( (
 ( 1.000000000000000000, 1.000000000000000000),
 ( 0.9934239774497837239, 0.8357310067453919133),
 ( 0.9934239774497837239, 0.8357310067453919133),
 ( 1.000000000000000000, 1.000000000000000000) ) ) 
 REPRESENTATION_ITEM ( '' )  SURFACE ( )  );
#1956=CARTESIAN_POINT ( 'NONE',  ( -15.02187109954783217, 40.82269973458240031, -21.95370994985588098 ) ) ;
#1961=CARTESIAN_POINT ( 'NONE',  ( -20.21097721712959938, 9.464413111084745367, -28.05863618200111986 ) ) ;
#1962=ORIENTED_EDGE ( 'NONE', *, *, #19230, .F. ) ;
#1966=FACE_OUTER_BOUND ( 'NONE', #27353, .T. ) ;
#1968=B_SPLINE_CURVE_WITH_KNOTS ( 'NONE', 3,
 ( #15373, #20261, #7052, #11070, #9351, #6762, #17811 ),
 .UNSPECIFIED., .F., .F.,
 ( 4, 3, 4 ),
 ( 0.000000000000000000, 0.006568092053401806615, 0.02506242213020846293 ),
 .UNSPECIFIED. ) ;
#1972=CONICAL_SURFACE ( 'NONE', #4276, 34.60786435723138510, 0.8559913436420825139 ) ;
#1976=EDGE_CURVE ( 'NONE', #27143, #8890, #4314, .T. ) ;
#1978=CARTESIAN_POINT ( 'NONE',  ( -28.41354790283022069, 1.249099604787400564, 23.16239616762929288 ) ) ;
#1982=EDGE_CURVE ( 'NONE', #17730, #13364, #17120, .T. ) ;
#1990=DIRECTION ( 'NONE',  ( 1.000000000000000000, -6.938893903907226837E-18, 1.734723475976806709E-18 ) ) ;
#1995=CARTESIAN_POINT ( 'NONE',  ( -1.045287976400383290, -44.00138577190632816, 12.68782741917368106 ) ) ;
#1996=CARTESIAN_POINT ( 'NONE',  ( -1.058473599757814521, 15.81436910992580991, 42.99101666105212161 ) ) ;
#1997=CARTESIAN_POINT ( 'NONE',  ( -2.904412668506649808, -30.27712468694961956, 36.79926976721486653 ) ) ;
#1998=CARTESIAN_POINT ( 'NONE',  ( -8.786685647604890903, -52.67761315067279781, 9.545808661481174795 ) ) ;
#1999=CARTESIAN_POINT ( 'NONE',  ( -1.044556982611281493, 43.01635920718349126, -15.70482750345250267 ) ) ;
#2006=CARTESIAN_POINT ( 'NONE',  ( -1.058473599757810746, -42.99101666105219977, 15.81436910992565004 ) ) ;
#2008=EDGE_LOOP ( 'NONE', ( #17015, #9500, #22791, #8704 ) ) ;
#2010=CARTESIAN_POINT ( 'NONE',  ( -1.049817751779889008, 0.5106138415326839652, -45.79652915392414769 ) ) ;
#2021=CARTESIAN_POINT ( 'NONE',  ( -55.24300891470648622, -0.007734635432132420246, -0.006048736206180634067 ) ) ;
#2022=ORIENTED_EDGE ( 'NONE', *, *, #13546, .T. ) ;
#2027=CARTESIAN_POINT ( 'NONE',  ( -25.21435515916043357, 6.169479169075458458, -34.05351380035335751 ) ) ;
#2030=CARTESIAN_POINT ( 'NONE',  ( -1.113548883309563253, -44.18588492042580640, 12.28732181966563886 ) ) ;
#2037=ORIENTED_EDGE ( 'NONE', *, *, #16578, .T. ) ;
#2042=EDGE_CURVE ( 'NONE', #7528, #10527, #3721, .T. ) ;
#2047=CARTESIAN_POINT ( 'NONE',  ( -1.048996300304498419, 43.78665266739856321, 13.42280206896931638 ) ) ;
#2050=CARTESIAN_POINT ( 'NONE',  ( -23.77929240705206482, 17.17389748746964173, -31.93650644494346835 ) ) ;
#2055=LINE ( 'NONE', #10858, #3816 ) ;
#2056=CARTESIAN_POINT ( 'NONE',  ( -28.41354790283022069, -5.969609727608182759, -22.41474081377998218 ) ) ;
#2062=CARTESIAN_POINT ( 'NONE',  ( -8.259864102781671491, -36.24929574824938783, -38.68084189741935575 ) ) ;
#2064=ORIENTED_EDGE ( 'NONE', *, *, #7038, .F. ) ;
#2073=( BOUNDED_SURFACE ( )  B_SPLINE_SURFACE ( 3, 1, ( 
 ( #17109, #12781 ),
 ( #8348, #25905 ),
 ( #15490, #21570 ),
 ( #12922, #13198 ) ),
 .UNSPECIFIED., .F., .F., .F. ) 
 B_SPLINE_SURFACE_WITH_KNOTS ( ( 4, 4 ),
 ( 2, 2 ),
 ( 0.000000000000000000, 1.000000000000000000 ),
 ( 0.000000000000000000, 1.000000000000000000 ),
 .UNSPECIFIED. ) 
 GEOMETRIC_REPRESENTATION_ITEM ( )  RATIONAL_B_SPLINE_SURFACE ( (
 ( 1.000000000000000000, 1.000000000000000000),
 ( 0.7789835883360576307, 0.9689951854195403280),
 ( 0.7789835883360576307, 0.9689951854195403280),
 ( 1.000000000000000000, 1.000000000000000000) ) ) 
 REPRESENTATION_ITEM ( '' )  SURFACE ( )  );
#2080=ADVANCED_FACE ( 'NONE', ( #7332, #24624 ), #16096, .T. ) ;
#2087=VERTEX_POINT ( 'NONE', #26890 ) ;
#2092=CARTESIAN_POINT ( 'NONE',  ( -6.574463467970653063, -47.03022655117387529, 20.55340846381182018 ) ) ;
#2094=CARTESIAN_POINT ( 'NONE',  ( -2.904412668506665351, 17.42365698954698061, -44.35433137608945486 ) ) ;
#2098=CARTESIAN_POINT ( 'NONE',  ( -4.780792508754321268, 25.98388465890140964, 42.16805077400930202 ) ) ;
#2104=CARTESIAN_POINT ( 'NONE',  ( -8.786685647604890903, -9.545808661480982948, -52.67761315067281913 ) ) ;
#2115=CARTESIAN_POINT ( 'NONE',  ( -1.046935749539985583, -1.275486069320154847, 45.77872888003168583 ) ) ;
#2127=DIRECTION ( 'NONE',  ( 0.7637818620346801257, 0.02150485345384395286, -0.6451161201712182214 ) ) ;
#2128=CARTESIAN_POINT ( 'NONE',  ( -21.41427618760457463, -23.81423075802597111, -19.54551635498120277 ) ) ;
#2139=CARTESIAN_POINT ( 'NONE',  ( -20.20700224038492721, 18.19058640100257662, 23.35150625415638714 ) ) ;
#2150=ORIENTED_EDGE ( 'NONE', *, *, #14062, .F. ) ;
#2155=EDGE_CURVE ( 'NONE', #4790, #27931, #5601, .T. ) ;
#2159=CARTESIAN_POINT ( 'NONE',  ( -1.619063947482197729, -2.489035965910479486, -46.30105812165547974 ) ) ;
#2160=CARTESIAN_POINT ( 'NONE',  ( -55.24390624410018802, 0.007503127514282199352, -0.007245494385991655198 ) ) ;
#2179=CARTESIAN_POINT ( 'NONE',  ( -55.25297051322618813, 0.01483298743814672610, -0.001818774723749509541 ) ) ;
#2184=CARTESIAN_POINT ( 'NONE',  ( -1.050230346682680560, 26.91946103437159721, 37.05264119692660785 ) ) ;
#2189=CARTESIAN_POINT ( 'NONE',  ( -25.21435515916025594, 1.749597353048488237E-16, -4.373993382621220594E-17 ) ) ;
#2200=ORIENTED_EDGE ( 'NONE', *, *, #13155, .F. ) ;
#2201=B_SPLINE_CURVE_WITH_KNOTS ( 'NONE', 3,
 ( #24292, #26709, #17652, #241, #7019, #26432 ),
 .UNSPECIFIED., .F., .F.,
 ( 4, 2, 4 ),
 ( 0.000000000000000000, 0.003570751334075635691, 0.007141502668151271382 ),
 .UNSPECIFIED. ) ;
#2204=ORIENTED_EDGE ( 'NONE', *, *, #8746, .F. ) ;
#2205=CARTESIAN_POINT ( 'NONE',  ( -22.23342874802667879, -2.180636882146296696, 31.55488258420093572 ) ) ;
#2208=CARTESIAN_POINT ( 'NONE',  ( -22.23226125620943705, 16.78323347921918796, -26.80886670319641851 ) ) ;
#2212=CARTESIAN_POINT ( 'NONE',  ( -28.41354790283022069, -19.47297445639558333, -12.60397206714825558 ) ) ;
#2214=CARTESIAN_POINT ( 'NONE',  ( -1.048171036023497704, 13.17819047681665090, 43.86077206077055735 ) ) ;
#2215=FACE_OUTER_BOUND ( 'NONE', #13923, .T. ) ;
#2221=CARTESIAN_POINT ( 'NONE',  ( -1.583189561560255143, 38.94740041318295454, -25.21827308671246470 ) ) ;
#2224=DIRECTION ( 'NONE',  ( 0.000000000000000000, 5.223019709707975211E-21, -1.000000000000000000 ) ) ;
#2230=CARTESIAN_POINT ( 'NONE',  ( -55.24390624410018802, -0.009209468562450790971, 0.004896917417127758312 ) ) ;
#2235=ORIENTED_EDGE ( 'NONE', *, *, #12128, .T. ) ;
#2248=DIRECTION ( 'NONE',  ( 0.7563875759206388771, 0.1685564395263429993, 0.6320336713238481341 ) ) ;
#2261=CARTESIAN_POINT ( 'NONE',  ( -20.57838717382308147, -29.92853265176830746, 1.611677988432673070 ) ) ;
#2262=CARTESIAN_POINT ( 'NONE',  ( -1.583189561560252701, -25.21827308671259615, -38.94740041318285506 ) ) ;
#2263=CARTESIAN_POINT ( 'NONE',  ( -55.25719721206881729, -0.01079965405819840671, -0.002847566758682798602 ) ) ;
#2270=LINE ( 'NONE', #17400, #10620 ) ;
#2281=CARTESIAN_POINT ( 'NONE',  ( -20.21097721712958872, 28.26295595852185727, -8.835581498567558256 ) ) ;
#2290=B_SPLINE_CURVE_WITH_KNOTS ( 'NONE', 3,
 ( #24397, #26533, #22522, #24551, #4814, #16171 ),
 .UNSPECIFIED., .F., .F.,
 ( 4, 2, 4 ),
 ( 3.469446951953613804E-18, 0.0004335184443139973023, 0.0008670368886279911352 ),
 .UNSPECIFIED. ) ;
#2292=ORIENTED_EDGE ( 'NONE', *, *, #6506, .F. ) ;
#2293=CARTESIAN_POINT ( 'NONE',  ( -21.41427618760446094, 30.75468365310879193, 1.815001260755948254 ) ) ;
#2306=VERTEX_POINT ( 'NONE', #22086 ) ;
#2307=FACE_OUTER_BOUND ( 'NONE', #25115, .T. ) ;
#2312=VECTOR ( 'NONE', #7939, 1000.000000000000000 ) ;
#2314=ORIENTED_EDGE ( 'NONE', *, *, #27127, .T. ) ;
#2317=ADVANCED_FACE ( 'NONE', ( #6559 ), #1952, .F. ) ;
#2331=CARTESIAN_POINT ( 'NONE',  ( -1.048171036023513247, 26.08692787913922473, 37.64178826568577563 ) ) ;
#2336=CARTESIAN_POINT ( 'NONE',  ( -1.056502255334265339, 37.35734037467636171, -26.51074901220517432 ) ) ;
#2339=CARTESIAN_POINT ( 'NONE',  ( -1.031422197589716205, -36.13727897780108123, 28.14735071801782951 ) ) ;
#2343=DIRECTION ( 'NONE',  ( 0.000000000000000000, 5.223019709708233256E-21, -1.000000000000000000 ) ) ;
#2353=CARTESIAN_POINT ( 'NONE',  ( -1.583189561560256253, 43.29471907393742924, -16.68617981233717273 ) ) ;
#2357=CARTESIAN_POINT ( 'NONE',  ( -1.583189561560256253, 16.68617981233763459, 43.29471907393723029 ) ) ;
#2358=CARTESIAN_POINT ( 'NONE',  ( -1.239374126674604337, 25.08410696974242882, -38.61989855450947573 ) ) ;
#2360=CARTESIAN_POINT ( 'NONE',  ( -2.911734481061396540, 12.03743348210780439, -46.11606034418766598 ) ) ;
#2368=ORIENTED_EDGE ( 'NONE', *, *, #28417, .T. ) ;
#2374=CARTESIAN_POINT ( 'NONE',  ( -1.259920593601984162, 16.33409644610551581, -43.01175804832013938 ) ) ;
#2378=B_SPLINE_CURVE_WITH_KNOTS ( 'NONE', 3,
 ( #2494, #18035, #18176, #336, #22672, #7266, #2643, #15888 ),
 .UNSPECIFIED., .F., .F.,
 ( 4, 2, 2, 4 ),
 ( 0.000000000000000000, 0.002761524886576648043, 0.005523049773153296087, 0.01104609954630659217 ),
 .UNSPECIFIED. ) ;
#2383=CARTESIAN_POINT ( 'NONE',  ( -1.464342487929861214, -35.90631960086394514, 29.09292098541700611 ) ) ;
#2403=CARTESIAN_POINT ( 'NONE',  ( -20.20997486282892552, 3.551351076220724598E-15, -29.60348406988233450 ) ) ;
#2412=CARTESIAN_POINT ( 'NONE',  ( -8.786685647604890903, -53.04920435127188938, -7.199674155858766689 ) ) ;
#2413=EDGE_CURVE ( 'NONE', #3326, #5301, #16411, .T. ) ;
#2418=CARTESIAN_POINT ( 'NONE',  ( -1.619063947482197729, -11.94059994246129008, 44.80407745103795492 ) ) ;
#2420=CARTESIAN_POINT ( 'NONE',  ( -8.786685647604890903, 23.24040270374391426, -48.22796981442777309 ) ) ;
#2424=( BOUNDED_SURFACE ( )  B_SPLINE_SURFACE ( 3, 1, ( 
 ( #17347, #2221 ),
 ( #15598, #6715 ),
 ( #21681, #17634 ),
 ( #24416, #8721 ) ),
 .UNSPECIFIED., .F., .F., .F. ) 
 B_SPLINE_SURFACE_WITH_KNOTS ( ( 4, 4 ),
 ( 2, 2 ),
 ( 0.000000000000000000, 1.000000000000000000 ),
 ( 0.000000000000000000, 1.000000000000000000 ),
 .UNSPECIFIED. ) 
 GEOMETRIC_REPRESENTATION_ITEM ( )  RATIONAL_B_SPLINE_SURFACE ( (
 ( 1.000000000000000000, 1.000000000000000000),
 ( 0.9934239774497837239, 0.8357310067453919133),
 ( 0.9934239774497837239, 0.8357310067453919133),
 ( 1.000000000000000000, 1.000000000000000000) ) ) 
 REPRESENTATION_ITEM ( '' )  SURFACE ( )  );
#2425=ADVANCED_FACE ( 'NONE', ( #6497 ), #7879, .F. ) ;
#2439=FACE_OUTER_BOUND ( 'NONE', #3040, .T. ) ;
#2455=CARTESIAN_POINT ( 'NONE',  ( -55.24728320129491266, 0.008013189884952347936, 0.01214321324517130159 ) ) ;
#2466=B_SPLINE_CURVE_WITH_KNOTS ( 'NONE', 3,
 ( #23195, #3585, #8201, #27779, #23468, #6052, #12364, #14807, #3878, #1005, #5463, #9799, #27336 ),
 .UNSPECIFIED., .F., .F.,
 ( 4, 3, 3, 3, 4 ),
 ( 6.938893903907227607E-18, 0.0007657099931970539480, 0.001531419946797919806, 0.002296279302920154267, 0.003061450627205759834 ),
 .UNSPECIFIED. ) ;
#2468=EDGE_CURVE ( 'NONE', #28211, #20564, #27509, .T. ) ;
#2470=ORIENTED_EDGE ( 'NONE', *, *, #5642, .T. ) ;
#2471=CARTESIAN_POINT ( 'NONE',  ( -55.24198130335446422, -0.004276389980775889554, -0.008252882783650218948 ) ) ;
#2473=CARTESIAN_POINT ( 'NONE',  ( -55.24390624410018802, 0.004572280736703349113, -0.009374879212967143077 ) ) ;
#2475=CARTESIAN_POINT ( 'NONE',  ( -1.048994561756796839, 43.31369460697995777, 14.87838255483211469 ) ) ;
#2478=CARTESIAN_POINT ( 'NONE',  ( -20.21097721650787449, 24.14932365326977148, 17.13687097598110398 ) ) ;
#2479=CARTESIAN_POINT ( 'NONE',  ( -8.786685647604890903, 25.35688121747502066, -47.14957014837363403 ) ) ;
#2486=CARTESIAN_POINT ( 'NONE',  ( -8.786685647604890903, -52.67761315067293282, -9.545808661480407409 ) ) ;
#2487=CARTESIAN_POINT ( 'NONE',  ( 14.74894986621300319, -1.023413983156987147E-16, 2.558534957892467869E-17 ) ) ;
#2488=CARTESIAN_POINT ( 'NONE',  ( -1.056502255334264895, -36.75727364034712963, 27.33667001641208572 ) ) ;
#2494=CARTESIAN_POINT ( 'NONE',  ( -8.786685647604890903, -23.24040270374424466, -48.22796981442760256 ) ) ;
#2499=CARTESIAN_POINT ( 'NONE',  ( -20.57838717382308147, -27.96569011373093971, -10.78122205916989529 ) ) ;
#2500=EDGE_CURVE ( 'NONE', #1301, #9661, #22172, .T. ) ;
#2507=CARTESIAN_POINT ( 'NONE',  ( -55.24340739397742084, -0.009842732675351817742, 0.002421372372454084262 ) ) ;
#2508=CARTESIAN_POINT ( 'NONE',  ( -7.711401346138389457, 10.36923727626120773, -51.42722225669425740 ) ) ;
#2514=EDGE_CURVE ( 'NONE', #24670, #4384, #18393, .T. ) ;
#2515=ORIENTED_EDGE ( 'NONE', *, *, #26003, .T. ) ;
#2516=CARTESIAN_POINT ( 'NONE',  ( -1.583189561560255143, -2.490696082059541627, 46.33203782964464068 ) ) ;
#2519=CARTESIAN_POINT ( 'NONE',  ( -55.24340739397742794, 0.002421372372456844640, -0.009842732675349010960 ) ) ;
#2522=CARTESIAN_POINT ( 'NONE',  ( -24.53237795827027412, -22.94498492516361310, -24.99972053297897290 ) ) ;
#2524=CARTESIAN_POINT ( 'NONE',  ( -1.463510566862822770, 11.94877850058565727, 44.64091840826476698 ) ) ;
#2529=CARTESIAN_POINT ( 'NONE',  ( 14.74894986621300319, -5.136656239696338858E-17, 37.50000000000001421 ) ) ;
#2535=LINE ( 'NONE', #4552, #19780 ) ;
#2537=ORIENTED_EDGE ( 'NONE', *, *, #12546, .T. ) ;
#2542=CARTESIAN_POINT ( 'NONE',  ( -24.53239521893650377, -22.94500969220219488, 24.99972072650167476 ) ) ;
#2547=CIRCLE ( 'NONE', #17718, 44.74884827092600403 ) ;
#2554=CARTESIAN_POINT ( 'NONE',  ( -1.045287976400379737, -25.66401692420040703, -37.92705037016734337 ) ) ;
#2556=CARTESIAN_POINT ( 'NONE',  ( -1.031422197589711764, 45.78027046666443312, 1.530725436377622817 ) ) ;
#2568=EDGE_CURVE ( 'NONE', #27540, #24434, #24947, .T. ) ;
#2570=ADVANCED_FACE ( 'NONE', ( #15723 ), #5461, .T. ) ;
#2595=CARTESIAN_POINT ( 'NONE',  ( -8.259864102781634188, -6.590267880897305197, -52.60025989855206063 ) ) ;
#2599=CARTESIAN_POINT ( 'NONE',  ( -4.473127245936434626, 3.196405119334491562, 49.22197550883364414 ) ) ;
#2600=CARTESIAN_POINT ( 'NONE',  ( -8.786685647604887350, -25.35688121747534751, -47.14957014837345639 ) ) ;
#2601=ADVANCED_FACE ( 'NONE', ( #17448 ), #19450, .F. ) ;
#2605=CARTESIAN_POINT ( 'NONE',  ( -55.24271866751342941, 0.008488649505343330570, 0.004256484107795472684 ) ) ;
#2606=CARTESIAN_POINT ( 'NONE',  ( -1.058473599757810746, 38.06357893967467731, 25.48501014712358881 ) ) ;
#2631=CARTESIAN_POINT ( 'NONE',  ( -4.162674018437150458, -3.424137510344606117, 48.79210541969628423 ) ) ;
#2632=( BOUNDED_SURFACE ( )  B_SPLINE_SURFACE ( 3, 1, ( 
 ( #18330, #14023 ),
 ( #22835, #24414 ),
 ( #4686, #9722 ),
 ( #21222, #27265 ) ),
 .UNSPECIFIED., .F., .F., .F. ) 
 B_SPLINE_SURFACE_WITH_KNOTS ( ( 4, 4 ),
 ( 2, 2 ),
 ( 0.000000000000000000, 1.000000000000000000 ),
 ( 0.000000000000000000, 1.000000000000000000 ),
 .UNSPECIFIED. ) 
 GEOMETRIC_REPRESENTATION_ITEM ( )  RATIONAL_B_SPLINE_SURFACE ( (
 ( 1.000000000000000000, 1.000000000000000000),
 ( 0.7789835883360578528, 0.9689951854195403280),
 ( 0.7789835883360578528, 0.9689951854195403280),
 ( 1.000000000000000000, 1.000000000000000000) ) ) 
 REPRESENTATION_ITEM ( '' )  SURFACE ( )  );
#2643=CARTESIAN_POINT ( 'NONE',  ( -2.911734481061404534, -17.36785190846011417, -44.38410240830297226 ) ) ;
#2650=EDGE_LOOP ( 'NONE', ( #16941, #6061, #26086, #4322 ) ) ;
#2654=EDGE_CURVE ( 'NONE', #25436, #18316, #7104, .T. ) ;
#2655=CARTESIAN_POINT ( 'NONE',  ( -1.048996300304498419, -14.87787369922200043, -43.31387123529974303 ) ) ;
#2666=CARTESIAN_POINT ( 'NONE',  ( -1.048994561756789734, -27.53485040342867407, 36.59609844253159139 ) ) ;
#2685=VERTEX_POINT ( 'NONE', #27528 ) ;
#2692=CARTESIAN_POINT ( 'NONE',  ( -20.21097721650785672, -17.67178726257375487, -23.76068422213751674 ) ) ;
#2694=B_SPLINE_CURVE_WITH_KNOTS ( 'NONE', 3,
 ( #2139, #7206, #4742, #9065, #4450, #17690 ),
 .UNSPECIFIED., .F., .F.,
 ( 4, 2, 4 ),
 ( 0.000000000000000000, 0.0004335184443140234316, 0.0008670368886280468632 ),
 .UNSPECIFIED. ) ;
#2696=CARTESIAN_POINT ( 'NONE',  ( -55.24728320129491266, 0.01214321324517175435, -0.008013189884952098135 ) ) ;
#2697=ORIENTED_EDGE ( 'NONE', *, *, #18312, .F. ) ;
#2698=EDGE_CURVE ( 'NONE', #20693, #4272, #16495, .T. ) ;
#2699=CARTESIAN_POINT ( 'NONE',  ( -4.473127245936434626, -41.70021447285072469, -26.34600523034523434 ) ) ;
#2703=ORIENTED_EDGE ( 'NONE', *, *, #18737, .F. ) ;
#2707=CARTESIAN_POINT ( 'NONE',  ( -55.25297051322618813, -0.01466904165775489814, 0.002853887643043841529 ) ) ;
#2714=CARTESIAN_POINT ( 'NONE',  ( -1.113427685307007531, -16.03057832159182539, -42.96952363574826705 ) ) ;
#2726=VERTEX_POINT ( 'NONE', #18166 ) ;
#2730=CARTESIAN_POINT ( 'NONE',  ( -22.23226125620929494, -30.68305173820431619, -7.677408153693907167 ) ) ;
#2733=CARTESIAN_POINT ( 'NONE',  ( -20.24399999263414429, 23.20123049637393464, 18.44171895251370330 ) ) ;
#2745=CARTESIAN_POINT ( 'NONE',  ( -4.473127245936431073, -49.22197550883370809, -3.196405119333634470 ) ) ;
#2754=CARTESIAN_POINT ( 'NONE',  ( -55.24340739397742794, -0.0007387096945702591004, -0.01010924026184094153 ) ) ;
#2758=CARTESIAN_POINT ( 'NONE',  ( -1.056502255334265339, 13.66916755949911177, 43.72121397317208391 ) ) ;
#2763=CARTESIAN_POINT ( 'NONE',  ( -55.24198130335446422, 0.008252882783649323831, 0.004276389980779915848 ) ) ;
#2788=VERTEX_POINT ( 'NONE', #17010 ) ;
#2790=CARTESIAN_POINT ( 'NONE',  ( -55.24340739397742794, -0.01010924026184046101, 0.0007387096945705813253 ) ) ;
#2793=ORIENTED_EDGE ( 'NONE', *, *, #1155, .T. ) ;
#2794=CARTESIAN_POINT ( 'NONE',  ( -22.34422965417124729, -37.30738373203622871, -6.759368364654178230 ) ) ;
#2795=VERTEX_POINT ( 'NONE', #14706 ) ;
#2806=( BOUNDED_SURFACE ( )  B_SPLINE_SURFACE ( 3, 1, ( 
 ( #9652, #5186 ),
 ( #11670, #4904 ),
 ( #22774, #3041 ),
 ( #1016, #22477 ) ),
 .UNSPECIFIED., .F., .F., .F. ) 
 B_SPLINE_SURFACE_WITH_KNOTS ( ( 4, 4 ),
 ( 2, 2 ),
 ( 0.000000000000000000, 1.000000000000000000 ),
 ( 0.000000000000000000, 1.000000000000000000 ),
 .UNSPECIFIED. ) 
 GEOMETRIC_REPRESENTATION_ITEM ( )  RATIONAL_B_SPLINE_SURFACE ( (
 ( 1.000000000000000000, 1.000000000000000000),
 ( 0.7789835883360576307, 0.9689951854195403280),
 ( 0.7789835883360576307, 0.9689951854195403280),
 ( 1.000000000000000000, 1.000000000000000000) ) ) 
 REPRESENTATION_ITEM ( '' )  SURFACE ( )  );
#2815=LINE ( 'NONE', #25001, #17972 ) ;
#2820=EDGE_LOOP ( 'NONE', ( #962, #18818, #23589, #27214 ) ) ;
#2834=CARTESIAN_POINT ( 'NONE',  ( -25.21435515916043357, -34.29329011225959079, -4.655591116594231416 ) ) ;
#2838=B_SPLINE_CURVE_WITH_KNOTS ( 'NONE', 3,
 ( #7960, #16724, #23488, #1862, #12801, #14963, #21451, #132, #3898, #4313, #6625, #25924, #4442 ),
 .UNSPECIFIED., .F., .F.,
 ( 4, 3, 3, 3, 4 ),
 ( 1.250926888277100303E-17, 0.0007657099931970583933, 0.001531419946797919589, 0.002296279302920155134, 0.003061450627205745088 ),
 .UNSPECIFIED. ) ;
#2842=CARTESIAN_POINT ( 'NONE',  ( -21.41430102051744200, -1.815007301162189446, -30.75470819672111134 ) ) ;
#2844=EDGE_CURVE ( 'NONE', #1503, #13365, #15260, .T. ) ;
#2852=CARTESIAN_POINT ( 'NONE',  ( -55.24728320129491266, -0.0006547948648744401781, 0.01453410071985650025 ) ) ;
#2857=CARTESIAN_POINT ( 'NONE',  ( -25.21435515916025594, 34.29329011225976842, -4.655591116594504086 ) ) ;
#2859=( BOUNDED_SURFACE ( )  B_SPLINE_SURFACE ( 3, 1, ( 
 ( #16146, #9537 ),
 ( #463, #24949 ),
 ( #2763, #20750 ),
 ( #20319, #26935 ) ),
 .UNSPECIFIED., .F., .F., .F. ) 
 B_SPLINE_SURFACE_WITH_KNOTS ( ( 4, 4 ),
 ( 2, 2 ),
 ( 0.000000000000000000, 1.000000000000000000 ),
 ( 0.000000000000000000, 1.000000000000000000 ),
 .UNSPECIFIED. ) 
 GEOMETRIC_REPRESENTATION_ITEM ( )  RATIONAL_B_SPLINE_SURFACE ( (
 ( 1.000000000000000000, 1.000000000000000000),
 ( 0.9593753223639863714, 0.9995975284513187731),
 ( 0.9593753223639863714, 0.9995975284513187731),
 ( 1.000000000000000000, 1.000000000000000000) ) ) 
 REPRESENTATION_ITEM ( '' )  SURFACE ( )  );
#2860=CARTESIAN_POINT ( 'NONE',  ( -2.904412668506669348, -46.12477647685265936, 11.97478724945559136 ) ) ;
#2867=CARTESIAN_POINT ( 'NONE',  ( -20.20612092514784308, -27.77903665678158873, 10.22177639105890279 ) ) ;
#2872=ORIENTED_EDGE ( 'NONE', *, *, #18785, .T. ) ;
#2878=ADVANCED_FACE ( 'NONE', ( #21765 ), #13725, .F. ) ;
#2883=CARTESIAN_POINT ( 'NONE',  ( -20.20700224038492010, 24.51628800869071867, 16.58740185276683832 ) ) ;
#2886=CARTESIAN_POINT ( 'NONE',  ( -20.24399999263415140, -24.70869149526192032, 16.36687688782885530 ) ) ;
#2888=CARTESIAN_POINT ( 'NONE',  ( -20.24399999263415495, -27.76448601145549233, -10.36954246768234889 ) ) ;
#2891=B_SPLINE_CURVE_WITH_KNOTS ( 'NONE', 3,
 ( #4791, #13410, #22210, #9107 ),
 .UNSPECIFIED., .F., .F.,
 ( 4, 4 ),
 ( 1.904175111373004964E-16, 0.001982023823822943748 ),
 .UNSPECIFIED. ) ;
#2892=FACE_OUTER_BOUND ( 'NONE', #4368, .T. ) ;
#2896=CARTESIAN_POINT ( 'NONE',  ( -7.078251931573406708, -34.59014398252944034, -38.93060825814217196 ) ) ;
#2902=CARTESIAN_POINT ( 'NONE',  ( -1.048996300304498419, -0.7649764263854993418, -45.79145529752469201 ) ) ;
#2904=( BOUNDED_SURFACE ( )  B_SPLINE_SURFACE ( 3, 1, ( 
 ( #9655, #17843 ),
 ( #7358, #16124 ),
 ( #5039, #7225 ),
 ( #586, #24350 ) ),
 .UNSPECIFIED., .F., .F., .F. ) 
 B_SPLINE_SURFACE_WITH_KNOTS ( ( 4, 4 ),
 ( 2, 2 ),
 ( 0.000000000000000000, 1.000000000000000000 ),
 ( 0.000000000000000000, 1.000000000000000000 ),
 .UNSPECIFIED. ) 
 GEOMETRIC_REPRESENTATION_ITEM ( )  RATIONAL_B_SPLINE_SURFACE ( (
 ( 1.000000000000000000, 1.000000000000000000),
 ( 0.9593753223639863714, 0.9995975284513187731),
 ( 0.9593753223639863714, 0.9995975284513187731),
 ( 1.000000000000000000, 1.000000000000000000) ) ) 
 REPRESENTATION_ITEM ( '' )  SURFACE ( )  );
#2906=EDGE_CURVE ( 'NONE', #18869, #16496, #16356, .T. ) ;
#2907=CARTESIAN_POINT ( 'NONE',  ( -55.24300891470648622, -0.002702093572889207890, -0.009439835024157681651 ) ) ;
#2908=CARTESIAN_POINT ( 'NONE',  ( -1.619063947482197729, -38.92136151114888776, 25.20140673341416360 ) ) ;
#2909=CARTESIAN_POINT ( 'NONE',  ( -1.044556982611269280, 37.98985389331847529, 25.56989963842161728 ) ) ;
#2911=ORIENTED_EDGE ( 'NONE', *, *, #4965, .T. ) ;
#2915=ORIENTED_EDGE ( 'NONE', *, *, #2698, .F. ) ;
#2920=CARTESIAN_POINT ( 'NONE',  ( -1.019300379054419725, -35.83762006677378764, 28.53917295602937187 ) ) ;
#2930=VECTOR ( 'NONE', #18557, 999.9999999999998863 ) ;
#2935=CARTESIAN_POINT ( 'NONE',  ( -1.050229599974473516, -37.20249516760156183, 26.71319688967675177 ) ) ;
#2938=ORIENTED_EDGE ( 'NONE', *, *, #23419, .T. ) ;
#2945=EDGE_CURVE ( 'NONE', #17470, #12390, #3318, .T. ) ;
#2947=ORIENTED_EDGE ( 'NONE', *, *, #5235, .F. ) ;
#2952=B_SPLINE_CURVE_WITH_KNOTS ( 'NONE', 3,
 ( #9476, #11476, #27447, #5288, #7616, #16226 ),
 .UNSPECIFIED., .F., .F.,
 ( 4, 2, 4 ),
 ( 3.178475462313071774E-16, 0.003576372551511121031, 0.007152745103021923741 ),
 .UNSPECIFIED. ) ;
#2953=CARTESIAN_POINT ( 'NONE',  ( -9.156249394959706578, 25.18996226954685369, 48.32878616080981260 ) ) ;
#2964=CARTESIAN_POINT ( 'NONE',  ( -1.323439229708141651, -2.317790194800056547, -46.01398008004440499 ) ) ;
#2968=CARTESIAN_POINT ( 'NONE',  ( -21.41430102051744910, 7.777552968935758315, -29.81033373822130628 ) ) ;
#2984=( BOUNDED_SURFACE ( )  B_SPLINE_SURFACE ( 3, 1, ( 
 ( #11143, #19919 ),
 ( #203, #6834 ),
 ( #8991, #15577 ),
 ( #4662, #17191 ) ),
 .UNSPECIFIED., .F., .F., .F. ) 
 B_SPLINE_SURFACE_WITH_KNOTS ( ( 4, 4 ),
 ( 2, 2 ),
 ( 0.000000000000000000, 1.000000000000000000 ),
 ( 0.000000000000000000, 1.000000000000000000 ),
 .UNSPECIFIED. ) 
 GEOMETRIC_REPRESENTATION_ITEM ( )  RATIONAL_B_SPLINE_SURFACE ( (
 ( 1.000000000000000000, 1.000000000000000000),
 ( 0.9934239774497838349, 0.8357310067453913582),
 ( 0.9934239774497838349, 0.8357310067453913582),
 ( 1.000000000000000000, 1.000000000000000000) ) ) 
 REPRESENTATION_ITEM ( '' )  SURFACE ( )  );
#2988=CARTESIAN_POINT ( 'NONE',  ( -20.20700224038492721, -10.08426345511609235, -27.82980252387815767 ) ) ;
#2998=ADVANCED_FACE ( 'NONE', ( #3181 ), #28422, .F. ) ;
#3001=CARTESIAN_POINT ( 'NONE',  ( -1.048171036023513025, 36.44209502233747600, 27.73816396939524509 ) ) ;
#3008=CARTESIAN_POINT ( 'NONE',  ( -16.86833981943427574, 39.83928801320588775, -19.19877306373863490 ) ) ;
#3011=DIRECTION ( 'NONE',  ( 0.000000000000000000, 5.223019709708233256E-21, -1.000000000000000000 ) ) ;
#3023=ORIENTED_EDGE ( 'NONE', *, *, #15796, .F. ) ;
#3025=B_SPLINE_CURVE_WITH_KNOTS ( 'NONE', 3,
 ( #13464, #1961, #10764, #5548 ),
 .UNSPECIFIED., .F., .F.,
 ( 4, 4 ),
 ( 1.892757412642747523E-16, 0.001982023823822945917 ),
 .UNSPECIFIED. ) ;
#3026=CARTESIAN_POINT ( 'NONE',  ( -1.050231094221194983, -45.79908322896422135, 0.2545420581353859402 ) ) ;
#3031=CARTESIAN_POINT ( 'NONE',  ( -1.619063947482201282, 44.80407745103784123, -11.94059994246174838 ) ) ;
#3032=ORIENTED_EDGE ( 'NONE', *, *, #18785, .F. ) ;
#3035=( BOUNDED_SURFACE ( )  B_SPLINE_SURFACE ( 3, 1, ( 
 ( #3580, #28030 ),
 ( #1698, #21561 ),
 ( #18992, #19540 ),
 ( #12361, #1422 ) ),
 .UNSPECIFIED., .F., .F., .F. ) 
 B_SPLINE_SURFACE_WITH_KNOTS ( ( 4, 4 ),
 ( 2, 2 ),
 ( 0.000000000000000000, 1.000000000000000000 ),
 ( 0.000000000000000000, 1.000000000000000000 ),
 .UNSPECIFIED. ) 
 GEOMETRIC_REPRESENTATION_ITEM ( )  RATIONAL_B_SPLINE_SURFACE ( (
 ( 1.000000000000000000, 1.000000000000000000),
 ( 0.7789835883360578528, 0.9689951854195403280),
 ( 0.7789835883360578528, 0.9689951854195403280),
 ( 1.000000000000000000, 1.000000000000000000) ) ) 
 REPRESENTATION_ITEM ( '' )  SURFACE ( )  );
#3036=EDGE_CURVE ( 'NONE', #1086, #7747, #1026, .T. ) ;
#3040=EDGE_LOOP ( 'NONE', ( #11677, #10672, #23494, #20948 ) ) ;
#3041=CARTESIAN_POINT ( 'NONE',  ( -7.078251931573406708, -38.93060825814203696, 34.59014398252958244 ) ) ;
#3043=CARTESIAN_POINT ( 'NONE',  ( -1.619063947482197729, -2.489035965910479486, -46.30105812165547974 ) ) ;
#3046=CARTESIAN_POINT ( 'NONE',  ( -1.323830074806771284, 2.318057800980712457, -46.01435746200690602 ) ) ;
#3047=EDGE_LOOP ( 'NONE', ( #6635, #6862, #25887, #24554 ) ) ;
#3059=B_SPLINE_CURVE_WITH_KNOTS ( 'NONE', 3,
 ( #3942, #28109, #12711, #21637, #21497, #1911, #10713 ),
 .UNSPECIFIED., .F., .F.,
 ( 4, 3, 4 ),
 ( 0.000000000000000000, 0.006568092053401818758, 0.02506242213020845946 ),
 .UNSPECIFIED. ) ;
#3069=B_SPLINE_CURVE_WITH_KNOTS ( 'NONE', 3,
 ( #26332, #19995, #26607, #566, #24475, #11496 ),
 .UNSPECIFIED., .F., .F.,
 ( 4, 2, 4 ),
 ( 0.000000000000000000, 0.0004335184443140181732, 0.0008670368886280363464 ),
 .UNSPECIFIED. ) ;
#3072=CARTESIAN_POINT ( 'NONE',  ( -25.21435515916043713, 25.00736669481056751, 23.92354251275909505 ) ) ;
#3080=ORIENTED_EDGE ( 'NONE', *, *, #15550, .F. ) ;
#3082=ORIENTED_EDGE ( 'NONE', *, *, #14692, .F. ) ;
#3093=CARTESIAN_POINT ( 'NONE',  ( -6.574463467970635300, 47.03022655117400319, -20.55340846381147202 ) ) ;
#3096=CARTESIAN_POINT ( 'NONE',  ( -20.20700224038492365, 8.199606986804329978, -28.44216453106539078 ) ) ;
#3100=CARTESIAN_POINT ( 'NONE',  ( -1.259972190295307604, -2.243354636026084759, -45.95417440459613800 ) ) ;
#3106=CARTESIAN_POINT ( 'NONE',  ( -8.786685647604889127, 9.545808661480615243, -52.67761315067287597 ) ) ;
#3107=B_SPLINE_CURVE_WITH_KNOTS ( 'NONE', 3,
 ( #1701, #26164, #1570, #6456, #16967, #15206, #8341, #13067, #21852, #10913 ),
 .UNSPECIFIED., .F., .F.,
 ( 4, 2, 2, 2, 4 ),
 ( 7.757919228897728493E-18, 0.0003346267210630983675, 0.0006692534421261890371, 0.001003880163189279761, 0.001338506884252370268 ),
 .UNSPECIFIED. ) ;
#3109=EDGE_LOOP ( 'NONE', ( #13631, #9794, #13363, #1337 ) ) ;
#3111=CARTESIAN_POINT ( 'NONE',  ( -55.24340739397742084, 0.006539691034612836289, -0.007744344507854826129 ) ) ;
#3112=CARTESIAN_POINT ( 'NONE',  ( -1.463510566862823437, -38.76366072687759612, 25.15876608740857989 ) ) ;
#3128=CARTESIAN_POINT ( 'NONE',  ( -20.20700224038492010, -18.19058640100240254, -23.35150625415651859 ) ) ;
#3130=CARTESIAN_POINT ( 'NONE',  ( -7.078251931573406708, 20.86696228105292761, 47.71415099571781582 ) ) ;
#3143=CARTESIAN_POINT ( 'NONE',  ( -55.24300891470650754, 0.006048736206179803135, 0.007734635432136488173 ) ) ;
#3146=CARTESIAN_POINT ( 'NONE',  ( -20.90916690077965256, -34.84883504600963988, -18.74041620980156253 ) ) ;
#3148=CARTESIAN_POINT ( 'NONE',  ( -1.239374126674604337, -38.61989855450958231, -25.08410696974230092 ) ) ;
#3151=CARTESIAN_POINT ( 'NONE',  ( -20.20700224038492721, -27.82980252387812570, 10.08426345511618649 ) ) ;
#3152=B_SPLINE_CURVE_WITH_KNOTS ( 'NONE', 3,
 ( #4072, #8268, #17031, #21788, #6121, #3940, #21633 ),
 .UNSPECIFIED., .F., .F.,
 ( 4, 3, 4 ),
 ( 0.000000000000000000, 0.006568092053401763247, 0.02506242213020846987 ),
 .UNSPECIFIED. ) ;
#3163=CARTESIAN_POINT ( 'NONE',  ( -1.045287976400365970, 45.76855895860946077, 1.530335034933974381 ) ) ;
#3173=ORIENTED_EDGE ( 'NONE', *, *, #16759, .F. ) ;
#3174=ORIENTED_EDGE ( 'NONE', *, *, #3377, .T. ) ;
#3180=ORIENTED_EDGE ( 'NONE', *, *, #17166, .T. ) ;
#3181=FACE_OUTER_BOUND ( 'NONE', #1759, .T. ) ;
#3182=CARTESIAN_POINT ( 'NONE',  ( -1.050230347699842692, 5.964912479342754695E-15, -45.79907861674080749 ) ) ;
#3193=EDGE_CURVE ( 'NONE', #8101, #17023, #26946, .T. ) ;
#3201=CARTESIAN_POINT ( 'NONE',  ( -24.53237795827029899, -24.99972053297889119, 22.94498492516371613 ) ) ;
#3203=DIRECTION ( 'NONE',  ( 0.000000000000000000, 5.223019709707975211E-21, -1.000000000000000000 ) ) ;
#3210=DIRECTION ( 'NONE',  ( 0.7563875759206388771, -0.5490129373055229189, 0.3556158456312960015 ) ) ;
#3217=CARTESIAN_POINT ( 'NONE',  ( -20.47566262905010248, 7.708089517695595028, 28.85746289809567600 ) ) ;
#3224=B_SPLINE_CURVE_WITH_KNOTS ( 'NONE', 3,
 ( #7947, #3884, #18161, #21297, #20325, #23339, #5915, #20611, #16004, #13990 ),
 .UNSPECIFIED., .F., .F.,
 ( 4, 2, 2, 2, 4 ),
 ( 2.913600445039318278E-16, 0.0003346187017559116412, 0.0006692374035115318488, 0.001003856105267152219, 0.001338474807022772481 ),
 .UNSPECIFIED. ) ;
#3231=CARTESIAN_POINT ( 'NONE',  ( -1.619063947482201282, 43.26576862488434472, -16.67502769180576649 ) ) ;
#3233=FACE_OUTER_BOUND ( 'NONE', #5180, .T. ) ;
#3236=CARTESIAN_POINT ( 'NONE',  ( -1.259920593601976169, 28.82601305773653877, -35.85909937955931071 ) ) ;
#3241=CARTESIAN_POINT ( 'NONE',  ( -1.155031165708883867, -2.068616213631259804, -45.85732438018710155 ) ) ;
#3248=CARTESIAN_POINT ( 'NONE',  ( -20.21097721650788159, -23.76068422213743503, 17.67178726257384014 ) ) ;
#3255=EDGE_LOOP ( 'NONE', ( #26348, #17389, #1106, #11172 ) ) ;
#3262=CARTESIAN_POINT ( 'NONE',  ( -1.619063947482197729, 2.489035965910801895, 46.30105812165545842 ) ) ;
#3263=AXIS2_PLACEMENT_3D ( 'NONE', #16073, #26579, #24878 ) ;
#3264=VERTEX_POINT ( 'NONE', #5158 ) ;
#3273=CARTESIAN_POINT ( 'NONE',  ( -1.050230346682689664, 14.15203301556493010, 43.55772679531834513 ) ) ;
#3276=FACE_OUTER_BOUND ( 'NONE', #28306, .T. ) ;
#3281=ORIENTED_EDGE ( 'NONE', *, *, #26808, .T. ) ;
#3289=CARTESIAN_POINT ( 'NONE',  ( -25.21435515916025594, 1.749597353048488237E-16, -4.373993382621220594E-17 ) ) ;
#3293=DIRECTION ( 'NONE',  ( 0.000000000000000000, 5.223019709707975211E-21, -1.000000000000000000 ) ) ;
#3294=CARTESIAN_POINT ( 'NONE',  ( -55.24271866751342941, 0.004256484107793635611, 0.008488649505346116536 ) ) ;
#3295=CARTESIAN_POINT ( 'NONE',  ( -1.155031165708884533, 44.25214473648929925, 12.20332162035416879 ) ) ;
#3303=EDGE_CURVE ( 'NONE', #11177, #25953, #26103, .T. ) ;
#3309=CARTESIAN_POINT ( 'NONE',  ( -8.786685647604894456, -23.24040270374358030, 48.22796981442792230 ) ) ;
#3318=B_SPLINE_CURVE_WITH_KNOTS ( 'NONE', 3,
 ( #20450, #22484, #9390, #14105, #18141, #11678, #20301, #4910, #15986, #22924 ),
 .UNSPECIFIED., .F., .F.,
 ( 4, 2, 2, 2, 4 ),
 ( 2.863532086325413454E-16, 0.0003346187017559064912, 0.0006692374035115266446, 0.001003856105267146798, 0.001338474807022767060 ),
 .UNSPECIFIED. ) ;
#3324=CARTESIAN_POINT ( 'NONE',  ( -1.463510566862832318, 2.430838777910187432, -46.14841196428340453 ) ) ;
#3326=VERTEX_POINT ( 'NONE', #11791 ) ;
#3327=CARTESIAN_POINT ( 'NONE',  ( -1.056502255334265339, 14.64009593116102614, -43.40574022158779144 ) ) ;
#3329=CARTESIAN_POINT ( 'NONE',  ( -1.539763995773681726, -25.17088606276573515, -38.84665165401054310 ) ) ;
#3331=CARTESIAN_POINT ( 'NONE',  ( -25.21435515916025594, 1.749597353048488237E-16, -4.373993382621220594E-17 ) ) ;
#3336=EDGE_LOOP ( 'NONE', ( #23435, #26824, #26553, #26062, #28440, #24937 ) ) ;
#3337=ORIENTED_EDGE ( 'NONE', *, *, #10894, .T. ) ;
#3351=CARTESIAN_POINT ( 'NONE',  ( -20.57838717382308147, 16.28767523336157552, 25.16001208503087838 ) ) ;
#3352=DIRECTION ( 'NONE',  ( 1.000000000000000000, -6.938893903907226837E-18, 1.734723475976806709E-18 ) ) ;
#3360=DIRECTION ( 'NONE',  ( -5.541455922705464902E-20, 5.223019709708320524E-21, -1.000000000000000000 ) ) ;
#3361=CARTESIAN_POINT ( 'NONE',  ( -7.733045908741340568, -10.42750254442575120, -51.44704017882771296 ) ) ;
#3364=CARTESIAN_POINT ( 'NONE',  ( -1.113427685306993320, 25.34053733836532274, -38.22586258295203265 ) ) ;
#3366=CARTESIAN_POINT ( 'NONE',  ( -20.57838717382308147, 7.715628353034087894, 28.96176188950209962 ) ) ;
#3370=ORIENTED_EDGE ( 'NONE', *, *, #4451, .T. ) ;
#3377=EDGE_CURVE ( 'NONE', #14092, #5592, #25221, .T. ) ;
#3379=CARTESIAN_POINT ( 'NONE',  ( -1.155001620486255209, 28.62773628245669499, -35.88346938217563320 ) ) ;
#3380=CARTESIAN_POINT ( 'NONE',  ( -28.41354790283022069, 14.62505768302800924, -18.00456980371904692 ) ) ;
#3382=CARTESIAN_POINT ( 'NONE',  ( -20.47566338032525124, 10.72601609985066062, 27.87687989047296711 ) ) ;
#3394=EDGE_CURVE ( 'NONE', #16076, #19079, #6591, .T. ) ;
#3397=CARTESIAN_POINT ( 'NONE',  ( -1.259920593601994376, 35.85909937955963755, 28.82601305773611600 ) ) ;
#3402=AXIS2_PLACEMENT_3D ( 'NONE', #11010, #15159, #28267 ) ;
#3403=ORIENTED_EDGE ( 'NONE', *, *, #13698, .F. ) ;
#3404=( BOUNDED_SURFACE ( )  B_SPLINE_SURFACE ( 3, 1, ( 
 ( #12742, #6286 ),
 ( #23857, #4247 ),
 ( #4108, #21671 ),
 ( #1943, #10749 ) ),
 .UNSPECIFIED., .F., .F., .F. ) 
 B_SPLINE_SURFACE_WITH_KNOTS ( ( 4, 4 ),
 ( 2, 2 ),
 ( 0.000000000000000000, 1.000000000000000000 ),
 ( 0.000000000000000000, 1.000000000000000000 ),
 .UNSPECIFIED. ) 
 GEOMETRIC_REPRESENTATION_ITEM ( )  RATIONAL_B_SPLINE_SURFACE ( (
 ( 1.000000000000000000, 1.000000000000000000),
 ( 0.9593753223639863714, 0.9995975284513187731),
 ( 0.9593753223639863714, 0.9995975284513187731),
 ( 1.000000000000000000, 1.000000000000000000) ) ) 
 REPRESENTATION_ITEM ( '' )  SURFACE ( )  );
#3406=CARTESIAN_POINT ( 'NONE',  ( -1.583189561560252701, -29.24830400313139478, 36.01941156322819637 ) ) ;
#3407=ORIENTED_EDGE ( 'NONE', *, *, #24876, .F. ) ;
#3425=CARTESIAN_POINT ( 'NONE',  ( -1.019300379054419725, 44.15350047934416011, 12.21833869579419130 ) ) ;
#3429=CARTESIAN_POINT ( 'NONE',  ( -1.583189561560256253, -44.83405390829680215, -11.94859433442884900 ) ) ;
#3432=CARTESIAN_POINT ( 'NONE',  ( -22.34422965417124018, -27.39717383755262148, 26.20925041532883881 ) ) ;
#3433=CARTESIAN_POINT ( 'NONE',  ( -25.21435515916043713, -30.48034229288650820, -16.39063784838731053 ) ) ;
#3434=EDGE_CURVE ( 'NONE', #4384, #17500, #18026, .T. ) ;
#3438=CARTESIAN_POINT ( 'NONE',  ( -1.050231094221210082, 13.91061116148191878, -43.63617436699743024 ) ) ;
#3441=CARTESIAN_POINT ( 'NONE',  ( -20.57838717382308147, 25.16001208503129760, 16.28767523336092893 ) ) ;
#3454=EDGE_CURVE ( 'NONE', #22293, #4663, #25615, .T. ) ;
#3458=ORIENTED_EDGE ( 'NONE', *, *, #3806, .F. ) ;
#3463=CARTESIAN_POINT ( 'NONE',  ( -1.044556982611273277, 12.57890920527776224, -44.03203163107531282 ) ) ;
#3466=ORIENTED_EDGE ( 'NONE', *, *, #22943, .F. ) ;
#3478=CARTESIAN_POINT ( 'NONE',  ( -4.473127245936431073, 18.25038884639870673, -45.82513704981550262 ) ) ;
#3489=CARTESIAN_POINT ( 'NONE',  ( -20.20700224038492721, -27.82980252387812570, 10.08426345511618649 ) ) ;
#3493=LINE ( 'NONE', #25245, #21636 ) ;
#3495=CARTESIAN_POINT ( 'NONE',  ( -4.473127245936434626, 12.17046501147516224, -47.80062405537804437 ) ) ;
#3497=VERTEX_POINT ( 'NONE', #21045 ) ;
#3499=ORIENTED_EDGE ( 'NONE', *, *, #14692, .T. ) ;
#3504=ORIENTED_EDGE ( 'NONE', *, *, #24803, .F. ) ;
#3510=EDGE_CURVE ( 'NONE', #10441, #28137, #804, .T. ) ;
#3517=ORIENTED_EDGE ( 'NONE', *, *, #25233, .F. ) ;
#3519=CARTESIAN_POINT ( 'NONE',  ( -7.711401346138175406, -45.70592430511711513, -25.75361633141480766 ) ) ;
#3524=CARTESIAN_POINT ( 'NONE',  ( -20.38016308990357928, -16.25718651464962861, 24.94368798801368925 ) ) ;
#3532=CARTESIAN_POINT ( 'NONE',  ( -1.323439229708128551, -38.58845475799787295, -25.17120723334079457 ) ) ;
#3541=CARTESIAN_POINT ( 'NONE',  ( -1.539760825549682188, -44.72358953107742252, -11.93465943778497262 ) ) ;
#3553=ORIENTED_EDGE ( 'NONE', *, *, #19586, .F. ) ;
#3561=ORIENTED_EDGE ( 'NONE', *, *, #9009, .F. ) ;
#3566=CARTESIAN_POINT ( 'NONE',  ( -20.38016308990357928, 1.509191766064626128, 29.73560196176844173 ) ) ;
#3568=CARTESIAN_POINT ( 'NONE',  ( -1.045287976400365970, 44.00138577190666922, 12.68782741917247670 ) ) ;
#3579=ORIENTED_EDGE ( 'NONE', *, *, #18568, .T. ) ;
#3580=CARTESIAN_POINT ( 'NONE',  ( -55.25719721206881729, 0.007063345920777610795, -0.008651607285660192076 ) ) ;
#3585=CARTESIAN_POINT ( 'NONE',  ( -1.046936909428679563, -12.93351869073243243, 43.93225665392628088 ) ) ;
#3589=CARTESIAN_POINT ( 'NONE',  ( -55.24728320129491266, -0.003868537197316565448, -0.01402509393918558236 ) ) ;
#3604=B_SPLINE_CURVE_WITH_KNOTS ( 'NONE', 3,
 ( #3778, #17007, #19039, #12139, #27816, #1194 ),
 .UNSPECIFIED., .F., .F.,
 ( 4, 2, 4 ),
 ( 1.550807859811640467E-16, 0.003570751334075634390, 0.007141502668151113523 ),
 .UNSPECIFIED. ) ;
#3605=B_SPLINE_CURVE_WITH_KNOTS ( 'NONE', 3,
 ( #18776, #5694, #23263, #18165, #26943, #22509 ),
 .UNSPECIFIED., .F., .F.,
 ( 4, 2, 4 ),
 ( 3.709064347514218400E-16, 0.003576372551511170905, 0.007152745103021971446 ),
 .UNSPECIFIED. ) ;
#3612=ADVANCED_FACE ( 'NONE', ( #4625 ), #4040, .F. ) ;
#3613=( BOUNDED_SURFACE ( )  B_SPLINE_SURFACE ( 3, 1, ( 
 ( #22684, #2953 ),
 ( #16324, #9713 ),
 ( #5385, #27103 ),
 ( #22973, #26966 ) ),
 .UNSPECIFIED., .F., .F., .F. ) 
 B_SPLINE_SURFACE_WITH_KNOTS ( ( 4, 4 ),
 ( 2, 2 ),
 ( 0.000000000000000000, 1.000000000000000000 ),
 ( 0.000000000000000000, 1.000000000000000000 ),
 .UNSPECIFIED. ) 
 GEOMETRIC_REPRESENTATION_ITEM ( )  RATIONAL_B_SPLINE_SURFACE ( (
 ( 1.000000000000000000, 1.000000000000000000),
 ( 0.7789835883360578528, 0.9689951854195403280),
 ( 0.7789835883360578528, 0.9689951854195403280),
 ( 1.000000000000000000, 1.000000000000000000) ) ) 
 REPRESENTATION_ITEM ( '' )  SURFACE ( )  );
#3615=CONICAL_SURFACE ( 'NONE', #19685, 34.60786435723138510, 0.8559913436420825139 ) ;
#3627=CARTESIAN_POINT ( 'NONE',  ( -21.41427618760458174, -11.22988868156165410, 28.68857606049978415 ) ) ;
#3636=ORIENTED_EDGE ( 'NONE', *, *, #6568, .F. ) ;
#3651=CARTESIAN_POINT ( 'NONE',  ( -20.20700224038492365, 8.199606986804329978, -28.44216453106539078 ) ) ;
#3659=B_SPLINE_CURVE_WITH_KNOTS ( 'NONE', 3,
 ( #26781, #11965, #20740, #13543, #1033, #17851, #22343, #2606, #2909, #9237 ),
 .UNSPECIFIED., .F., .F.,
 ( 4, 2, 2, 2, 4 ),
 ( 8.299636676276019848E-18, 0.0003346267210630991806, 0.0006692534421261901213, 0.001003880163189280845, 0.001338506884252371786 ),
 .UNSPECIFIED. ) ;
#3663=DIRECTION ( 'NONE',  ( -1.000000000000000000, 6.938893903907226837E-18, 5.541455922705464902E-20 ) ) ;
#3667=EDGE_CURVE ( 'NONE', #13496, #18216, #1178, .T. ) ;
#3675=B_SPLINE_CURVE_WITH_KNOTS ( 'NONE', 3,
 ( #4404, #13047, #2094, #15605, #10897, #8884, #19658, #4837 ),
 .UNSPECIFIED., .F., .F.,
 ( 4, 2, 2, 4 ),
 ( 2.194186273941487449E-16, 0.002761568181852863766, 0.005523136363705508090, 0.01104627272741078893 ),
 .UNSPECIFIED. ) ;
#3692=CARTESIAN_POINT ( 'NONE',  ( -1.045287976400365970, 15.59869763335068171, -43.05558670614252037 ) ) ;
#3696=CARTESIAN_POINT ( 'NONE',  ( -1.619063947482197729, -46.30105812165550105, -2.489035965909997206 ) ) ;
#3704=DIRECTION ( 'NONE',  ( 0.000000000000000000, 5.223019709707975211E-21, -1.000000000000000000 ) ) ;
#3706=CARTESIAN_POINT ( 'NONE',  ( -1.259920593601969729, 12.06711544331625596, 44.39818421957802741 ) ) ;
#3708=ADVANCED_FACE ( 'NONE', ( #22786 ), #9369, .T. ) ;
#3714=EDGE_CURVE ( 'NONE', #16059, #2788, #4752, .T. ) ;
#3720=EDGE_CURVE ( 'NONE', #15305, #17251, #17268, .T. ) ;
#3721=B_SPLINE_CURVE_WITH_KNOTS ( 'NONE', 3,
 ( #2420, #7198, #13651, #27020, #22305, #11215, #17816 ),
 .UNSPECIFIED., .F., .F.,
 ( 4, 3, 4 ),
 ( 3.469446951953614189E-18, 0.009512539173626420944, 0.02506242213020843865 ),
 .UNSPECIFIED. ) ;
#3726=LINE ( 'NONE', #19262, #23927 ) ;
#3748=CARTESIAN_POINT ( 'NONE',  ( -1.058197053496172213, 42.99116279335175506, 15.81317659443640444 ) ) ;
#3750=CARTESIAN_POINT ( 'NONE',  ( -1.045287976400383290, 28.14015102489806708, -36.12803364096618708 ) ) ;
#3753=FACE_OUTER_BOUND ( 'NONE', #7965, .T. ) ;
#3762=AXIS2_PLACEMENT_3D ( 'NONE', #20538, #9606, #18090 ) ;
#3763=CARTESIAN_POINT ( 'NONE',  ( -1.048994561756802391, 0.7655149579823430361, -45.79144455904140187 ) ) ;
#3764=ORIENTED_EDGE ( 'NONE', *, *, #1155, .F. ) ;
#3768=CARTESIAN_POINT ( 'NONE',  ( -1.619063947482197729, -29.22875152547730337, 35.99532424477411041 ) ) ;
#3775=CARTESIAN_POINT ( 'NONE',  ( -6.574463467970654840, 5.014313797967739461, 51.07975593197901532 ) ) ;
#3778=CARTESIAN_POINT ( 'NONE',  ( -20.57838717382308502, 23.26537097894105699, -18.89542499756508320 ) ) ;
#3783=EDGE_CURVE ( 'NONE', #1503, #22323, #23166, .T. ) ;
#3785=CARTESIAN_POINT ( 'NONE',  ( -1.619063947482201282, -44.80407745103776307, 11.94059994246206635 ) ) ;
#3786=CARTESIAN_POINT ( 'NONE',  ( -55.24271866751342941, 0.008433070970614256479, -0.004365563123935527895 ) ) ;
#3789=( BOUNDED_SURFACE ( )  B_SPLINE_SURFACE ( 3, 1, ( 
 ( #23437, #21401 ),
 ( #18819, #3425 ),
 ( #12752, #6168 ),
 ( #7911, #14498 ) ),
 .UNSPECIFIED., .F., .F., .F. ) 
 B_SPLINE_SURFACE_WITH_KNOTS ( ( 4, 4 ),
 ( 2, 2 ),
 ( 0.000000000000000000, 1.000000000000000000 ),
 ( 0.000000000000000000, 1.000000000000000000 ),
 .UNSPECIFIED. ) 
 GEOMETRIC_REPRESENTATION_ITEM ( )  RATIONAL_B_SPLINE_SURFACE ( (
 ( 1.000000000000000000, 1.000000000000000000),
 ( 0.9934239774497838349, 0.8357310067453913582),
 ( 0.9934239774497838349, 0.8357310067453913582),
 ( 1.000000000000000000, 1.000000000000000000) ) ) 
 REPRESENTATION_ITEM ( '' )  SURFACE ( )  );
#3796=ORIENTED_EDGE ( 'NONE', *, *, #27894, .F. ) ;
#3806=EDGE_CURVE ( 'NONE', #8074, #21771, #16258, .T. ) ;
#3807=ORIENTED_EDGE ( 'NONE', *, *, #16762, .T. ) ;
#3810=CARTESIAN_POINT ( 'NONE',  ( -1.155031165708883423, 28.62780465193363355, 35.88345263711016031 ) ) ;
#3816=VECTOR ( 'NONE', #8691, 1000.000000000000000 ) ;
#3819=CIRCLE ( 'NONE', #24058, 34.60786435723138510 ) ;
#3827=ORIENTED_EDGE ( 'NONE', *, *, #3510, .T. ) ;
#3830=ORIENTED_EDGE ( 'NONE', *, *, #8140, .F. ) ;
#3837=AXIS2_PLACEMENT_3D ( 'NONE', #3856, #12484, #8186 ) ;
#3852=DIRECTION ( 'NONE',  ( 0.000000000000000000, 5.223019709707975211E-21, -1.000000000000000000 ) ) ;
#3855=CARTESIAN_POINT ( 'NONE',  ( -55.24271866751342941, 0.009369360294296125852, 0.001545935011630558513 ) ) ;
#3856=CARTESIAN_POINT ( 'NONE',  ( -8.786685647604885574, 6.096987947571466530E-17, -1.524246986892866633E-17 ) ) ;
#3874=DIRECTION ( 'NONE',  ( -0.7563875759206388771, 0.3556158456312860094, -0.5490129373055293582 ) ) ;
#3878=CARTESIAN_POINT ( 'NONE',  ( -1.049817751779889008, -14.63752841325019105, 43.39729912094394848 ) ) ;
#3884=CARTESIAN_POINT ( 'NONE',  ( -1.044557008772713402, -15.70482370518787718, 43.01636061109000053 ) ) ;
#3886=VERTEX_POINT ( 'NONE', #10525 ) ;
#3892=CARTESIAN_POINT ( 'NONE',  ( -1.259972190295298944, 43.01178231151332909, -16.33417789844387968 ) ) ;
#3897=CARTESIAN_POINT ( 'NONE',  ( -1.031422197589711987, 28.14735071801795740, 36.13727897780095333 ) ) ;
#3898=CARTESIAN_POINT ( 'NONE',  ( -1.049817751779873909, -36.75003908324312363, -27.33161971822185876 ) ) ;
#3911=( BOUNDED_SURFACE ( )  B_SPLINE_SURFACE ( 3, 1, ( 
 ( #14944, #5914 ),
 ( #3589, #14670 ),
 ( #12368, #27483 ),
 ( #7795, #16552 ) ),
 .UNSPECIFIED., .F., .F., .F. ) 
 B_SPLINE_SURFACE_WITH_KNOTS ( ( 4, 4 ),
 ( 2, 2 ),
 ( 0.000000000000000000, 1.000000000000000000 ),
 ( 0.000000000000000000, 1.000000000000000000 ),
 .UNSPECIFIED. ) 
 GEOMETRIC_REPRESENTATION_ITEM ( )  RATIONAL_B_SPLINE_SURFACE ( (
 ( 1.000000000000000000, 1.000000000000000000),
 ( 0.7789835883360576307, 0.9689951854195403280),
 ( 0.7789835883360576307, 0.9689951854195403280),
 ( 1.000000000000000000, 1.000000000000000000) ) ) 
 REPRESENTATION_ITEM ( '' )  SURFACE ( )  );
#3915=B_SPLINE_CURVE_WITH_KNOTS ( 'NONE', 3,
 ( #25240, #25678, #13994, #14270, #23091, #3351 ),
 .UNSPECIFIED., .F., .F.,
 ( 4, 2, 4 ),
 ( 4.341940435234061368E-16, 0.003576372551511239426, 0.007152745103022045171 ),
 .UNSPECIFIED. ) ;
#3917=VERTEX_POINT ( 'NONE', #18873 ) ;
#3922=CARTESIAN_POINT ( 'NONE',  ( -1.019300379054419947, 28.53917295602898463, -35.83762006677410028 ) ) ;
#3928=ORIENTED_EDGE ( 'NONE', *, *, #7453, .F. ) ;
#3935=EDGE_CURVE ( 'NONE', #13364, #10267, #21398, .T. ) ;
#3938=B_SPLINE_CURVE_WITH_KNOTS ( 'NONE', 3,
 ( #27131, #24582, #16202, #25011, #5264, #26704, #14039, #3112, #11888, #20656 ),
 .UNSPECIFIED., .F., .F.,
 ( 4, 2, 2, 2, 4 ),
 ( 2.799429325053882983E-16, 0.0003346187017559012328, 0.0006692374035115225247, 0.001003856105267143762, 0.001338474807022765108 ),
 .UNSPECIFIED. ) ;
#3940=CARTESIAN_POINT ( 'NONE',  ( -12.82751273423884442, 6.573887447703498310, 48.43568301531131937 ) ) ;
#3942=CARTESIAN_POINT ( 'NONE',  ( -25.21435515916042647, 25.00736669481023355, -23.92354251275945742 ) ) ;
#3943=( BOUNDED_SURFACE ( )  B_SPLINE_SURFACE ( 3, 1, ( 
 ( #20316, #9400 ),
 ( #2471, #2758 ),
 ( #23191, #25336 ),
 ( #458, #5611 ) ),
 .UNSPECIFIED., .F., .F., .F. ) 
 B_SPLINE_SURFACE_WITH_KNOTS ( ( 4, 4 ),
 ( 2, 2 ),
 ( 0.000000000000000000, 1.000000000000000000 ),
 ( 0.000000000000000000, 1.000000000000000000 ),
 .UNSPECIFIED. ) 
 GEOMETRIC_REPRESENTATION_ITEM ( )  RATIONAL_B_SPLINE_SURFACE ( (
 ( 1.000000000000000000, 1.000000000000000000),
 ( 0.9593753223639863714, 0.9995975284513187731),
 ( 0.9593753223639863714, 0.9995975284513187731),
 ( 1.000000000000000000, 1.000000000000000000) ) ) 
 REPRESENTATION_ITEM ( '' )  SURFACE ( )  );
#3956=CARTESIAN_POINT ( 'NONE',  ( -1.045287976400379737, -37.92705037016725100, 25.66401692420055269 ) ) ;
#3962=CARTESIAN_POINT ( 'NONE',  ( -1.045287976400351981, -15.59869763335126436, -43.05558670614231431 ) ) ;
#3967=EDGE_CURVE ( 'NONE', #9705, #27648, #10458, .T. ) ;
#3974=CARTESIAN_POINT ( 'NONE',  ( -1.239374126674604337, 11.92219841463829333, -44.48112152129351671 ) ) ;
#3979=CARTESIAN_POINT ( 'NONE',  ( -20.20700224038492365, 10.08426345511628597, 27.82980252387807951 ) ) ;
#3983=CARTESIAN_POINT ( 'NONE',  ( -8.786685647604890903, -48.22796981442753150, 23.24040270374441874 ) ) ;
#3985=CARTESIAN_POINT ( 'NONE',  ( -55.24390624410018802, 0.009209468562452933355, 0.004896917417131438528 ) ) ;
#3991=CARTESIAN_POINT ( 'NONE',  ( -1.583189561560256253, -46.33203782964459805, 2.490696082060350314 ) ) ;
#3992=CARTESIAN_POINT ( 'NONE',  ( -20.37983603106074426, -1.508851015062371292, 29.73529213200292531 ) ) ;
#3999=CARTESIAN_POINT ( 'NONE',  ( -1.044557008772707407, 37.98985164565329598, -25.56990300676994821 ) ) ;
#4002=EDGE_CURVE ( 'NONE', #28150, #654, #11078, .T. ) ;
#4017=ORIENTED_EDGE ( 'NONE', *, *, #5697, .T. ) ;
#4022=CARTESIAN_POINT ( 'NONE',  ( -4.178947244162634966, 37.51424432987651159, -31.41809272265936315 ) ) ;
#4030=CARTESIAN_POINT ( 'NONE',  ( -1.239374126674604337, -45.98822239537608425, -2.406737988130961181 ) ) ;
#4031=CARTESIAN_POINT ( 'NONE',  ( 14.74894986621300141, -12.50000000000000000, 6.523836839588689598E-17 ) ) ;
#4033=CARTESIAN_POINT ( 'NONE',  ( -20.24419206586953734, -28.55732805495821225, -7.929973069813295972 ) ) ;
#4036=CARTESIAN_POINT ( 'NONE',  ( -2.265401668238146815, 29.73100299756566756, -36.42007794497261841 ) ) ;
#4038=ORIENTED_EDGE ( 'NONE', *, *, #2042, .T. ) ;
#4040=( BOUNDED_SURFACE ( )  B_SPLINE_SURFACE ( 3, 1, ( 
 ( #2605, #24082 ),
 ( #26358, #17572 ),
 ( #17994, #10970 ),
 ( #11387, #8663 ) ),
 .UNSPECIFIED., .F., .F., .F. ) 
 B_SPLINE_SURFACE_WITH_KNOTS ( ( 4, 4 ),
 ( 2, 2 ),
 ( 0.000000000000000000, 1.000000000000000000 ),
 ( 0.000000000000000000, 1.000000000000000000 ),
 .UNSPECIFIED. ) 
 GEOMETRIC_REPRESENTATION_ITEM ( )  RATIONAL_B_SPLINE_SURFACE ( (
 ( 1.000000000000000000, 1.000000000000000000),
 ( 0.9593753223639863714, 0.9995975284513187731),
 ( 0.9593753223639863714, 0.9995975284513187731),
 ( 1.000000000000000000, 1.000000000000000000) ) ) 
 REPRESENTATION_ITEM ( '' )  SURFACE ( )  );
#4062=EDGE_LOOP ( 'NONE', ( #24061, #25405, #12345, #15857 ) ) ;
#4064=ORIENTED_EDGE ( 'NONE', *, *, #6443, .T. ) ;
#4072=CARTESIAN_POINT ( 'NONE',  ( -25.21435515916043713, 4.655591116594827383, 34.29329011225949841 ) ) ;
#4073=CARTESIAN_POINT ( 'NONE',  ( -20.47566338032523348, 7.708089572830403746, -28.85746366088566361 ) ) ;
#4075=CARTESIAN_POINT ( 'NONE',  ( -6.588769196390773963, 47.06982923582537381, 20.50531526814514294 ) ) ;
#4077=B_SPLINE_CURVE_WITH_KNOTS ( 'NONE', 3,
 ( #21988, #26170, #26035, #28318, #11196, #10643, #15075, #21858, #2115, #4565 ),
 .UNSPECIFIED., .F., .F.,
 ( 4, 3, 3, 4 ),
 ( 0.001530725384384964971, 0.001531419946797918505, 0.002296279302920153399, 0.003061450627205758099 ),
 .UNSPECIFIED. ) ;
#4090=FACE_OUTER_BOUND ( 'NONE', #17882, .T. ) ;
#4091=ORIENTED_EDGE ( 'NONE', *, *, #992, .F. ) ;
#4093=EDGE_CURVE ( 'NONE', #20968, #25314, #24905, .T. ) ;
#4095=CARTESIAN_POINT ( 'NONE',  ( -28.41354790283022069, -1.249099604786914286, 23.16239616762932130 ) ) ;
#4103=CARTESIAN_POINT ( 'NONE',  ( -2.911734481061400537, 30.23325065583413718, 36.84482841982617884 ) ) ;
#4108=CARTESIAN_POINT ( 'NONE',  ( -55.24198130335446422, 0.006617369590172447053, -0.006527480770973747085 ) ) ;
#4121=CARTESIAN_POINT ( 'NONE',  ( -1.045287976400362417, 25.66401692420069125, 37.92705037016716574 ) ) ;
#4126=CARTESIAN_POINT ( 'NONE',  ( -4.780792508754321268, 3.764354093953580449, -49.38761389561002346 ) ) ;
#4136=CARTESIAN_POINT ( 'NONE',  ( -2.911734481061388102, 46.11606034418780098, 12.03743348210733011 ) ) ;
#4143=DIRECTION ( 'NONE',  ( 0.000000000000000000, -5.223019709708190374E-21, 1.000000000000000000 ) ) ;
#4152=CARTESIAN_POINT ( 'NONE',  ( -1.259920593601975058, -45.95412615877143026, -2.243284667987618608 ) ) ;
#4154=CONICAL_SURFACE ( 'NONE', #473, 34.60786435723138510, 0.8559913436420825139 ) ;
#4155=ORIENTED_EDGE ( 'NONE', *, *, #26437, .F. ) ;
#4161=CARTESIAN_POINT ( 'NONE',  ( -55.24390624410018802, 0.01032895241566708991, 0.001451500391952845713 ) ) ;
#4174=CARTESIAN_POINT ( 'NONE',  ( -1.046935749539996907, 1.275486069320473481, -45.77872888003166452 ) ) ;
#4176=B_SPLINE_CURVE_WITH_KNOTS ( 'NONE', 3,
 ( #7575, #9870, #25125, #5393 ),
 .UNSPECIFIED., .F., .F.,
 ( 4, 4 ),
 ( 1.895855152355442610E-16, 0.001982023823822946784 ),
 .UNSPECIFIED. ) ;
#4179=ORIENTED_EDGE ( 'NONE', *, *, #25398, .F. ) ;
#4181=VECTOR ( 'NONE', #13356, 1000.000000000000000 ) ;
#4183=CARTESIAN_POINT ( 'NONE',  ( -25.21435515916043713, 30.48034229288662544, 16.39063784838709736 ) ) ;
#4194=DIRECTION ( 'NONE',  ( 0.7563875759206388771, -0.3556158456312938365, -0.5490129373055243622 ) ) ;
#4197=CARTESIAN_POINT ( 'NONE',  ( -1.045287976400383290, -44.00138577190632816, 12.68782741917368106 ) ) ;
#4198=CARTESIAN_POINT ( 'NONE',  ( -24.53237795827005741, 30.86653739599987745, -14.09663893005569513 ) ) ;
#4201=ORIENTED_EDGE ( 'NONE', *, *, #16418, .F. ) ;
#4204=B_SPLINE_CURVE_WITH_KNOTS ( 'NONE', 3,
 ( #8079, #20999, #1154, #18999, #21143, #18850 ),
 .UNSPECIFIED., .F., .F.,
 ( 4, 2, 4 ),
 ( 1.396102177145585797E-16, 0.003570751334075633089, 0.007141502668151126533 ),
 .UNSPECIFIED. ) ;
#4214=CARTESIAN_POINT ( 'NONE',  ( -20.57838717382308147, -25.16001208503093522, 16.28767523336148315 ) ) ;
#4218=CARTESIAN_POINT ( 'NONE',  ( -12.82751273423881777, 23.15139349681311387, -43.04932478553539710 ) ) ;
#4221=CARTESIAN_POINT ( 'NONE',  ( -1.050229599974477290, 26.71319688967688322, 37.20249516760145525 ) ) ;
#4222=VERTEX_POINT ( 'NONE', #20089 ) ;
#4229=VERTEX_POINT ( 'NONE', #2104 ) ;
#4231=CARTESIAN_POINT ( 'NONE',  ( -8.259864102781673267, 25.58601832199082793, -46.42816643551579148 ) ) ;
#4234=ORIENTED_EDGE ( 'NONE', *, *, #15831, .T. ) ;
#4240=VERTEX_POINT ( 'NONE', #28301 ) ;
#4242=ADVANCED_FACE ( 'NONE', ( #4273 ), #7938, .F. ) ;
#4247=CARTESIAN_POINT ( 'NONE',  ( -1.056502255334265339, -27.33667001641142846, 36.75727364034761990 ) ) ;
#4256=CARTESIAN_POINT ( 'NONE',  ( -1.619063947482197729, 46.30105812165548684, -2.489035965910316506 ) ) ;
#4264=CARTESIAN_POINT ( 'NONE',  ( -1.619063947482197729, 2.489035965910159298, -46.30105812165548684 ) ) ;
#4268=DIRECTION ( 'NONE',  ( 0.000000000000000000, 5.223019709707975211E-21, -1.000000000000000000 ) ) ;
#4272=VERTEX_POINT ( 'NONE', #17365 ) ;
#4273=FACE_OUTER_BOUND ( 'NONE', #12342, .T. ) ;
#4275=CARTESIAN_POINT ( 'NONE',  ( -1.619063947482197729, -35.99532424477357750, 29.22875152547795707 ) ) ;
#4276=AXIS2_PLACEMENT_3D ( 'NONE', #14490, #23010, #25593 ) ;
#4277=( BOUNDED_SURFACE ( )  B_SPLINE_SURFACE ( 3, 1, ( 
 ( #6656, #15403 ),
 ( #24213, #12551 ),
 ( #23668, #3922 ),
 ( #12690, #21476 ) ),
 .UNSPECIFIED., .F., .F., .F. ) 
 B_SPLINE_SURFACE_WITH_KNOTS ( ( 4, 4 ),
 ( 2, 2 ),
 ( 0.000000000000000000, 1.000000000000000000 ),
 ( 0.000000000000000000, 1.000000000000000000 ),
 .UNSPECIFIED. ) 
 GEOMETRIC_REPRESENTATION_ITEM ( )  RATIONAL_B_SPLINE_SURFACE ( (
 ( 1.000000000000000000, 1.000000000000000000),
 ( 0.9934239774497837239, 0.8357310067453919133),
 ( 0.9934239774497837239, 0.8357310067453919133),
 ( 1.000000000000000000, 1.000000000000000000) ) ) 
 REPRESENTATION_ITEM ( '' )  SURFACE ( )  );
#4288=CARTESIAN_POINT ( 'NONE',  ( -1.259972190295306715, 35.85909728507050431, -28.82609802125271514 ) ) ;
#4305=CARTESIAN_POINT ( 'NONE',  ( -1.045287976400365970, -36.12803364096568259, 28.14015102489869591 ) ) ;
#4309=CARTESIAN_POINT ( 'NONE',  ( -24.53239521893647890, -24.99972072650158950, -22.94500969220225883 ) ) ;
#4310=ORIENTED_EDGE ( 'NONE', *, *, #28261, .F. ) ;
#4313=CARTESIAN_POINT ( 'NONE',  ( -1.048994561756786625, -36.59609844253148481, -27.53485040342882328 ) ) ;
#4314=LINE ( 'NONE', #27820, #22526 ) ;
#4315=CARTESIAN_POINT ( 'NONE',  ( -1.259972190295305827, -43.01178231151318698, 16.33417789844418522 ) ) ;
#4322=ORIENTED_EDGE ( 'NONE', *, *, #1372, .F. ) ;
#4339=CARTESIAN_POINT ( 'NONE',  ( -7.078251931573406708, 26.33626633876224332, -44.92740138729174504 ) ) ;
#4359=CARTESIAN_POINT ( 'NONE',  ( -1.031422197589711987, 37.93675465142509040, 25.67058493451400381 ) ) ;
#4363=CARTESIAN_POINT ( 'NONE',  ( -2.904412668506661355, 36.79926976721492338, 30.27712468694946679 ) ) ;
#4365=CARTESIAN_POINT ( 'NONE',  ( -4.473127245936431073, 49.22197550883368677, 3.196405119333978639 ) ) ;
#4368=EDGE_LOOP ( 'NONE', ( #129, #17004, #23082, #1339 ) ) ;
#4370=CARTESIAN_POINT ( 'NONE',  ( -55.24300891470648622, 0.005486913146696770563, 0.008142823778062024953 ) ) ;
#4371=CARTESIAN_POINT ( 'NONE',  ( -1.050230347699842692, 1.897926697972695375E-16, 45.79907861674080749 ) ) ;
#4375=ORIENTED_EDGE ( 'NONE', *, *, #8741, .F. ) ;
#4384=VERTEX_POINT ( 'NONE', #16643 ) ;
#4388=CARTESIAN_POINT ( 'NONE',  ( -55.24271866751342941, -0.009369360294295348696, -0.001545935011630817420 ) ) ;
#4389=AXIS2_PLACEMENT_3D ( 'NONE', #25541, #12279, #3360 ) ;
#4400=CARTESIAN_POINT ( 'NONE',  ( -20.57838717382308147, 29.92853265176831812, -1.611677988432464126 ) ) ;
#4404=CARTESIAN_POINT ( 'NONE',  ( -1.619063947482201282, 16.67502769180561728, -43.26576862488438735 ) ) ;
#4408=DIRECTION ( 'NONE',  ( -1.000000000000000000, 6.938893903907226837E-18, -1.734723475976806709E-18 ) ) ;
#4413=EDGE_CURVE ( 'NONE', #9705, #2306, #14614, .T. ) ;
#4414=EDGE_CURVE ( 'NONE', #5134, #1484, #21335, .T. ) ;
#4416=CARTESIAN_POINT ( 'NONE',  ( 14.74894986621300319, -1.025372615548127706E-16, 37.50000000000001421 ) ) ;
#4420=ORIENTED_EDGE ( 'NONE', *, *, #16578, .F. ) ;
#4423=CARTESIAN_POINT ( 'NONE',  ( -1.539760825549685519, -46.22267384399379608, 2.469813586483570855 ) ) ;
#4428=CARTESIAN_POINT ( 'NONE',  ( -20.90916690077962414, -7.054312691028722604, 38.93431874629081335 ) ) ;
#4431=EDGE_LOOP ( 'NONE', ( #6276, #12961, #6313, #22162, #18688, #8431, #27158, #10091, #2470, #5610, #8737, #14048, #1153, #27707, #4887, #24334, #24264, #5022, #23742, #6988, #15471, #14898, #20508, #26497, #18801, #20527, #26502, #20113, #11498, #15763, #22030, #12006, #13227, #7405, #26020, #22858, #2911, #4017, #22291, #20008, #12905, #12007, #17086, #1366, #13395, #15127, #15827, #25654, #9398, #4980, #26215, #14720, #15165, #7769, #6031, #19298, #19635, #26676, #12025, #27991, #8603, #10889, #27269, #18075 ) ) ;
#4432=VERTEX_POINT ( 'NONE', #3962 ) ;
#4433=CARTESIAN_POINT ( 'NONE',  ( -1.050230346682680782, -26.91946103437133431, -37.05264119692680680 ) ) ;
#4436=CARTESIAN_POINT ( 'NONE',  ( -15.02187109954788191, -45.60876405941872491, 8.264310930412850809 ) ) ;
#4439=ORIENTED_EDGE ( 'NONE', *, *, #26328, .F. ) ;
#4440=CARTESIAN_POINT ( 'NONE',  ( -8.786685647604887350, 53.04920435127183254, -7.199674155859138835 ) ) ;
#4441=CARTESIAN_POINT ( 'NONE',  ( -8.786685647604885574, 6.096987947571466530E-17, -1.524246986892866633E-17 ) ) ;
#4442=CARTESIAN_POINT ( 'NONE',  ( -1.045287976400383290, -36.12803364096628655, -28.14015102489793918 ) ) ;
#4443=EDGE_CURVE ( 'NONE', #744, #5523, #24097, .T. ) ;
#4445=EDGE_CURVE ( 'NONE', #12449, #6247, #6631, .T. ) ;
#4450=CARTESIAN_POINT ( 'NONE',  ( -20.47566338032516597, 18.81547714195514232, 23.19796701701855213 ) ) ;
#4451=EDGE_CURVE ( 'NONE', #14777, #5273, #21240, .T. ) ;
#4459=ORIENTED_EDGE ( 'NONE', *, *, #3935, .F. ) ;
#4467=CARTESIAN_POINT ( 'NONE',  ( -1.056502255334265339, -13.66916755949880802, -43.72121397317219049 ) ) ;
#4469=B_SPLINE_CURVE_WITH_KNOTS ( 'NONE', 3,
 ( #19661, #234, #13049, #4547, #367, #2374, #8733, #6863, #15608, #4696 ),
 .UNSPECIFIED., .F., .F.,
 ( 4, 2, 2, 2, 4 ),
 ( 2.879654849182128713E-16, 0.0003346187017559071959, 0.0006692374035115264278, 0.001003856105267145714, 0.001338474807022764891 ),
 .UNSPECIFIED. ) ;
#4478=( BOUNDED_SURFACE ( )  B_SPLINE_SURFACE ( 3, 1, ( 
 ( #13783, #22886 ),
 ( #9620, #27166 ),
 ( #18103, #11923 ),
 ( #406, #18383 ) ),
 .UNSPECIFIED., .F., .F., .F. ) 
 B_SPLINE_SURFACE_WITH_KNOTS ( ( 4, 4 ),
 ( 2, 2 ),
 ( 0.000000000000000000, 1.000000000000000000 ),
 ( 0.000000000000000000, 1.000000000000000000 ),
 .UNSPECIFIED. ) 
 GEOMETRIC_REPRESENTATION_ITEM ( )  RATIONAL_B_SPLINE_SURFACE ( (
 ( 1.000000000000000000, 1.000000000000000000),
 ( 0.9934239774497838349, 0.8357310067453913582),
 ( 0.9934239774497838349, 0.8357310067453913582),
 ( 1.000000000000000000, 1.000000000000000000) ) ) 
 REPRESENTATION_ITEM ( '' )  SURFACE ( )  );
#4483=ORIENTED_EDGE ( 'NONE', *, *, #17565, .F. ) ;
#4494=CARTESIAN_POINT ( 'NONE',  ( -4.780792508754322157, 37.74278713234441796, 32.07473752860738614 ) ) ;
#4496=CARTESIAN_POINT ( 'NONE',  ( -1.046935749540015115, 37.78548154587994645, -25.87617179820928826 ) ) ;
#4497=CARTESIAN_POINT ( 'NONE',  ( -6.588769196390775740, -4.956336548259307584, 51.10255870850478033 ) ) ;
#4512=CARTESIAN_POINT ( 'NONE',  ( -55.24340739397742084, -0.0007387096945734077319, 0.01010924026184317238 ) ) ;
#4517=ORIENTED_EDGE ( 'NONE', *, *, #3394, .T. ) ;
#4522=CARTESIAN_POINT ( 'NONE',  ( -55.24300891470650754, -0.009439835024158502175, -0.002702093572893477045 ) ) ;
#4527=LINE ( 'NONE', #11298, #23527 ) ;
#4530=CARTESIAN_POINT ( 'NONE',  ( -19.53423201713129842, 1.355459634611817431E-16, -3.388649086529543578E-17 ) ) ;
#4532=EDGE_CURVE ( 'NONE', #28478, #24539, #20398, .T. ) ;
#4539=DIRECTION ( 'NONE',  ( 1.000000000000000000, -6.938893903907226837E-18, 1.734723475976806709E-18 ) ) ;
#4540=CARTESIAN_POINT ( 'NONE',  ( -1.050229599974477512, -27.12684363859229109, 36.90196321294325799 ) ) ;
#4544=CARTESIAN_POINT ( 'NONE',  ( -1.619063947482197729, 11.94059994246222622, 44.80407745103770623 ) ) ;
#4547=CARTESIAN_POINT ( 'NONE',  ( -1.113548883309557924, 16.03115934825529010, -42.96943836789110094 ) ) ;
#4548=CARTESIAN_POINT ( 'NONE',  ( -1.239374126674604337, -45.98822239537607715, 2.406737988131604666 ) ) ;
#4551=B_SPLINE_CURVE_WITH_KNOTS ( 'NONE', 3,
 ( #25342, #16844, #5767, #27620, #1573, #7941 ),
 .UNSPECIFIED., .F., .F.,
 ( 4, 2, 4 ),
 ( 3.565531997320606436E-16, 0.003576372551511159629, 0.007152745103021962772 ),
 .UNSPECIFIED. ) ;
#4552=CARTESIAN_POINT ( 'NONE',  ( -28.13707043255157103, -22.88591869784691823, -0.7675454997506192534 ) ) ;
#4561=VECTOR ( 'NONE', #21442, 1000.000000000000114 ) ;
#4565=CARTESIAN_POINT ( 'NONE',  ( -1.045287976400362417, -1.530335034933495653, 45.76855895860946788 ) ) ;
#4566=ORIENTED_EDGE ( 'NONE', *, *, #11450, .T. ) ;
#4579=EDGE_CURVE ( 'NONE', #12327, #22671, #15898, .T. ) ;
#4581=CARTESIAN_POINT ( 'NONE',  ( -1.619063947482197729, 43.26576862488456499, 16.67502769180516964 ) ) ;
#4585=CARTESIAN_POINT ( 'NONE',  ( -7.711401346138398338, -10.36923727626085423, 51.42722225669433556 ) ) ;
#4590=ORIENTED_EDGE ( 'NONE', *, *, #12843, .F. ) ;
#4592=B_SPLINE_CURVE_WITH_KNOTS ( 'NONE', 3,
 ( #8842, #24960, #23355, #26813, #763, #5223, #16161 ),
 .UNSPECIFIED., .F., .F.,
 ( 4, 3, 4 ),
 ( 8.845388854693243284E-18, 0.009512539173626400127, 0.02506242213020845599 ),
 .UNSPECIFIED. ) ;
#4598=FACE_OUTER_BOUND ( 'NONE', #817, .T. ) ;
#4602=( BOUNDED_SURFACE ( )  B_SPLINE_SURFACE ( 3, 1, ( 
 ( #26235, #6533 ),
 ( #1500, #15286 ),
 ( #24102, #4365 ),
 ( #10311, #17870 ) ),
 .UNSPECIFIED., .F., .F., .F. ) 
 B_SPLINE_SURFACE_WITH_KNOTS ( ( 4, 4 ),
 ( 2, 2 ),
 ( 0.000000000000000000, 1.000000000000000000 ),
 ( 0.000000000000000000, 1.000000000000000000 ),
 .UNSPECIFIED. ) 
 GEOMETRIC_REPRESENTATION_ITEM ( )  RATIONAL_B_SPLINE_SURFACE ( (
 ( 1.000000000000000000, 1.000000000000000000),
 ( 0.7789835883360578528, 0.9689951854195403280),
 ( 0.7789835883360578528, 0.9689951854195403280),
 ( 1.000000000000000000, 1.000000000000000000) ) ) 
 REPRESENTATION_ITEM ( '' )  SURFACE ( )  );
#4604=LINE ( 'NONE', #26343, #15667 ) ;
#4606=CARTESIAN_POINT ( 'NONE',  ( -1.619063947482201282, -44.80407745103776307, 11.94059994246206635 ) ) ;
#4608=EDGE_CURVE ( 'NONE', #744, #27143, #85, .T. ) ;
#4615=CARTESIAN_POINT ( 'NONE',  ( -12.94347594948481728, -21.16159467081325474, 43.91326021875537577 ) ) ;
#4621=DIRECTION ( 'NONE',  ( 1.000000000000000000, -6.938893903907226837E-18, 1.734723475976806709E-18 ) ) ;
#4622=B_SPLINE_CURVE_WITH_KNOTS ( 'NONE', 3,
 ( #9873, #12166, #12297, #1219, #19071, #10018, #18778, #27551 ),
 .UNSPECIFIED., .F., .F.,
 ( 4, 2, 2, 4 ),
 ( 2.194186273941487942E-16, 0.002761568181852859863, 0.005523136363705500283, 0.01104627272741079066 ),
 .UNSPECIFIED. ) ;
#4625=FACE_OUTER_BOUND ( 'NONE', #16870, .T. ) ;
#4628=CARTESIAN_POINT ( 'NONE',  ( -1.619063947482197729, -29.22875152547781852, -35.99532424477369830 ) ) ;
#4633=ORIENTED_EDGE ( 'NONE', *, *, #8578, .T. ) ;
#4637=EDGE_CURVE ( 'NONE', #24758, #14951, #11428, .T. ) ;
#4641=EDGE_CURVE ( 'NONE', #9315, #5518, #10765, .T. ) ;
#4646=CARTESIAN_POINT ( 'NONE',  ( -2.904412668506656026, 44.35433137608966092, 17.42365698954652586 ) ) ;
#4651=CARTESIAN_POINT ( 'NONE',  ( -8.786685647604896232, -7.199674155858612146, 53.04920435127190359 ) ) ;
#4654=ORIENTED_EDGE ( 'NONE', *, *, #18793, .T. ) ;
#4658=DIRECTION ( 'NONE',  ( -1.000000000000000000, 6.938893903907226837E-18, -1.734723475976806709E-18 ) ) ;
#4659=CARTESIAN_POINT ( 'NONE',  ( -55.24271866751342941, 0.009388511352200529583, -0.001425019990779194824 ) ) ;
#4662=CARTESIAN_POINT ( 'NONE',  ( -55.24390624410018802, -0.004896917417131185259, 0.009209468562452437224 ) ) ;
#4663=VERTEX_POINT ( 'NONE', #5489 ) ;
#4664=CARTESIAN_POINT ( 'NONE',  ( -1.049819825607605672, 43.39756533277881800, -14.63675055554395321 ) ) ;
#4667=ORIENTED_EDGE ( 'NONE', *, *, #19230, .T. ) ;
#4670=ORIENTED_EDGE ( 'NONE', *, *, #11184, .F. ) ;
#4679=CARTESIAN_POINT ( 'NONE',  ( -20.20700224038492010, 27.82980252387833886, 10.08426345511560207 ) ) ;
#4686=CARTESIAN_POINT ( 'NONE',  ( -55.24728320129491266, 0.008013189884950885564, -0.01214321324516771938 ) ) ;
#4691=LINE ( 'NONE', #6718, #10705 ) ;
#4692=CARTESIAN_POINT ( 'NONE',  ( -23.79248802219729697, -22.01156985585185311, -24.83956736572401525 ) ) ;
#4694=CARTESIAN_POINT ( 'NONE',  ( -1.583189561560252701, 43.29471907393764951, 16.68617981233657943 ) ) ;
#4696=CARTESIAN_POINT ( 'NONE',  ( -1.619063947482201282, 16.67502769180561728, -43.26576862488438735 ) ) ;
#4704=LINE ( 'NONE', #4416, #7394 ) ;
#4709=EDGE_LOOP ( 'NONE', ( #12241, #28457, #10627, #17138 ) ) ;
#4712=CONICAL_SURFACE ( 'NONE', #14348, 34.60786435723138510, 0.8559913436420825139 ) ;
#4715=CARTESIAN_POINT ( 'NONE',  ( -1.045287976400365970, -37.92705037016778391, -25.66401692419976399 ) ) ;
#4719=CARTESIAN_POINT ( 'NONE',  ( -9.156249394959713683, -48.32878616081028866, -25.18996226954597972 ) ) ;
#4724=B_SPLINE_CURVE_WITH_KNOTS ( 'NONE', 3,
 ( #16654, #25857, #12187, #20956, #14623, #23425, #27998 ),
 .UNSPECIFIED., .F., .F.,
 ( 4, 3, 4 ),
 ( 0.000000000000000000, 0.006568092053401801411, 0.02506242213020845253 ),
 .UNSPECIFIED. ) ;
#4726=CARTESIAN_POINT ( 'NONE',  ( -1.048171036023499925, -43.86077206077059998, 13.17819047681649103 ) ) ;
#4728=CARTESIAN_POINT ( 'NONE',  ( -4.473127245936434626, -18.25038884639903003, -45.82513704981538183 ) ) ;
#4732=ORIENTED_EDGE ( 'NONE', *, *, #26697, .T. ) ;
#4738=ORIENTED_EDGE ( 'NONE', *, *, #22167, .T. ) ;
#4742=CARTESIAN_POINT ( 'NONE',  ( -20.24419206586952669, 18.44224248888906814, 23.20105925399704461 ) ) ;
#4749=CARTESIAN_POINT ( 'NONE',  ( -20.21097721650786383, 28.05863614620939472, -9.464413208035171721 ) ) ;
#4751=EDGE_CURVE ( 'NONE', #15303, #12261, #27735, .T. ) ;
#4752=CIRCLE ( 'NONE', #13951, 34.60786435723138510 ) ;
#4754=CARTESIAN_POINT ( 'NONE',  ( -20.57838717382308147, 25.16001208503129760, 16.28767523336092893 ) ) ;
#4756=CARTESIAN_POINT ( 'NONE',  ( -20.37983603106074426, -24.94323704205426040, 16.25728007463434110 ) ) ;
#4771=CARTESIAN_POINT ( 'NONE',  ( -25.21435515916025594, 1.749597353048488237E-16, -4.373993382621220594E-17 ) ) ;
#4774=CARTESIAN_POINT ( 'NONE',  ( -25.21435515916043002, -4.655591116594591128, -34.29329011225954105 ) ) ;
#4790=VERTEX_POINT ( 'NONE', #10265 ) ;
#4791=CARTESIAN_POINT ( 'NONE',  ( -20.20700224038492721, 29.58392382092673500, 0.9908225410479544193 ) ) ;
#4793=CARTESIAN_POINT ( 'NONE',  ( -1.019300379054419725, 38.21680004809200426, 25.26451264419602438 ) ) ;
#4797=B_SPLINE_CURVE_WITH_KNOTS ( 'NONE', 3,
 ( #3366, #3217, #9999, #12284, #25400, #16764 ),
 .UNSPECIFIED., .F., .F.,
 ( 4, 2, 4 ),
 ( 4.906538933386797396E-18, 0.0004335151646191504906, 0.0008670303292382959938 ),
 .UNSPECIFIED. ) ;
#4801=CARTESIAN_POINT ( 'NONE',  ( -1.019300379054419947, 25.26451264419699783, 38.21680004809136477 ) ) ;
#4806=CARTESIAN_POINT ( 'NONE',  ( -1.045287976400365970, -36.12803364096568259, 28.14015102489869591 ) ) ;
#4809=ORIENTED_EDGE ( 'NONE', *, *, #1046, .T. ) ;
#4814=CARTESIAN_POINT ( 'NONE',  ( -20.47566338032530098, -23.19796701701852015, 18.81547714195498244 ) ) ;
#4826=( BOUNDED_SURFACE ( )  B_SPLINE_SURFACE ( 3, 1, ( 
 ( #6940, #26492 ),
 ( #2455, #11246 ),
 ( #6509, #444 ),
 ( #22036, #300 ) ),
 .UNSPECIFIED., .F., .F., .F. ) 
 B_SPLINE_SURFACE_WITH_KNOTS ( ( 4, 4 ),
 ( 2, 2 ),
 ( 0.000000000000000000, 1.000000000000000000 ),
 ( 0.000000000000000000, 1.000000000000000000 ),
 .UNSPECIFIED. ) 
 GEOMETRIC_REPRESENTATION_ITEM ( )  RATIONAL_B_SPLINE_SURFACE ( (
 ( 1.000000000000000000, 1.000000000000000000),
 ( 0.7789835883360576307, 0.9689951854195403280),
 ( 0.7789835883360576307, 0.9689951854195403280),
 ( 1.000000000000000000, 1.000000000000000000) ) ) 
 REPRESENTATION_ITEM ( '' )  SURFACE ( )  );
#4827=CARTESIAN_POINT ( 'NONE',  ( -8.786685647604885574, 6.069026232697080105E-17, 53.53553390275978785 ) ) ;
#4833=CARTESIAN_POINT ( 'NONE',  ( -4.162674018437136247, 11.82104147411627970, 47.46216648493545165 ) ) ;
#4834=CARTESIAN_POINT ( 'NONE',  ( -55.24390624410018802, 0.001451500391953283731, -0.01032895241566680888 ) ) ;
#4837=CARTESIAN_POINT ( 'NONE',  ( -8.786685647604890903, 23.24040270374391426, -48.22796981442777309 ) ) ;
#4850=ORIENTED_EDGE ( 'NONE', *, *, #4751, .F. ) ;
#4854=B_SPLINE_CURVE_WITH_KNOTS ( 'NONE', 3,
 ( #24903, #5162, #13938, #27468, #12083, #7637 ),
 .UNSPECIFIED., .F., .F.,
 ( 4, 2, 4 ),
 ( 1.072867218403649326E-17, 0.003576372551510812684, 0.007152745103021620164 ),
 .UNSPECIFIED. ) ;
#4855=DIRECTION ( 'NONE',  ( 0.000000000000000000, 5.223019709708233256E-21, -1.000000000000000000 ) ) ;
#4858=CARTESIAN_POINT ( 'NONE',  ( -55.24271866751342941, 0.008488649505346581442, -0.004256484107793381474 ) ) ;
#4859=FACE_OUTER_BOUND ( 'NONE', #22923, .T. ) ;
#4863=CARTESIAN_POINT ( 'NONE',  ( -20.47566338032527611, 23.19796701701867647, -18.81547714195482612 ) ) ;
#4866=ORIENTED_EDGE ( 'NONE', *, *, #3434, .F. ) ;
#4875=CARTESIAN_POINT ( 'NONE',  ( -8.786685647604885574, 6.096987947571466530E-17, -1.524246986892866633E-17 ) ) ;
#4876=CARTESIAN_POINT ( 'NONE',  ( -4.473127245936431073, -47.80062405537792358, 12.17046501147566318 ) ) ;
#4879=EDGE_CURVE ( 'NONE', #7066, #2795, #13960, .T. ) ;
#4887=ORIENTED_EDGE ( 'NONE', *, *, #8850, .T. ) ;
#4895=DIRECTION ( 'NONE',  ( -5.541455922705464902E-20, 5.223019709708320524E-21, -1.000000000000000000 ) ) ;
#4896=ORIENTED_EDGE ( 'NONE', *, *, #19775, .F. ) ;
#4904=CARTESIAN_POINT ( 'NONE',  ( -4.473127245936434626, -37.94261489385694830, 31.51789735524234004 ) ) ;
#4910=CARTESIAN_POINT ( 'NONE',  ( -1.463510566862827655, 44.64091840826493041, -11.94877850058517765 ) ) ;
#4924=VERTEX_POINT ( 'NONE', #23040 ) ;
#4926=CARTESIAN_POINT ( 'NONE',  ( -55.24390624410018802, 0.01027195578988056128, 0.001811362924362418811 ) ) ;
#4936=ADVANCED_FACE ( 'NONE', ( #850 ), #10526, .F. ) ;
#4943=ORIENTED_EDGE ( 'NONE', *, *, #8331, .F. ) ;
#4945=ORIENTED_EDGE ( 'NONE', *, *, #17473, .F. ) ;
#4946=CARTESIAN_POINT ( 'NONE',  ( -55.24390624410018802, -0.01027195578987734684, 0.001811362924359352471 ) ) ;
#4949=ORIENTED_EDGE ( 'NONE', *, *, #19572, .T. ) ;
#4951=VERTEX_POINT ( 'NONE', #22605 ) ;
#4957=CARTESIAN_POINT ( 'NONE',  ( -1.045287976400383290, -12.68782741917353185, -44.00138577190637079 ) ) ;
#4965=EDGE_CURVE ( 'NONE', #6633, #7508, #28373, .T. ) ;
#4967=CARTESIAN_POINT ( 'NONE',  ( -1.056502255334265339, 43.72121397317224734, -13.66916755949864637 ) ) ;
#4980=ORIENTED_EDGE ( 'NONE', *, *, #26121, .T. ) ;
#4983=ORIENTED_EDGE ( 'NONE', *, *, #18568, .F. ) ;
#4984=CARTESIAN_POINT ( 'NONE',  ( -7.078251931573400491, -34.59014398252887190, 38.93060825814266934 ) ) ;
#4985=( BOUNDED_SURFACE ( )  B_SPLINE_SURFACE ( 3, 1, ( 
 ( #24052, #26324 ),
 ( #8633, #6765 ),
 ( #15376, #26741 ),
 ( #28467, #6906 ) ),
 .UNSPECIFIED., .F., .F., .F. ) 
 B_SPLINE_SURFACE_WITH_KNOTS ( ( 4, 4 ),
 ( 2, 2 ),
 ( 0.000000000000000000, 1.000000000000000000 ),
 ( 0.000000000000000000, 1.000000000000000000 ),
 .UNSPECIFIED. ) 
 GEOMETRIC_REPRESENTATION_ITEM ( )  RATIONAL_B_SPLINE_SURFACE ( (
 ( 1.000000000000000000, 1.000000000000000000),
 ( 0.7789835883360576307, 0.9689951854195403280),
 ( 0.7789835883360576307, 0.9689951854195403280),
 ( 1.000000000000000000, 1.000000000000000000) ) ) 
 REPRESENTATION_ITEM ( '' )  SURFACE ( )  );
#4987=CARTESIAN_POINT ( 'NONE',  ( -20.57838717382308147, -27.96569011373078339, 10.78122205917029675 ) ) ;
#4996=DIRECTION ( 'NONE',  ( 0.000000000000000000, 5.223019709707975211E-21, -1.000000000000000000 ) ) ;
#4999=EDGE_CURVE ( 'NONE', #15484, #10441, #21559, .T. ) ;
#5002=CARTESIAN_POINT ( 'NONE',  ( -4.473127245936434626, -47.80062405537809411, -12.17046501147497750 ) ) ;
#5007=CARTESIAN_POINT ( 'NONE',  ( -25.21435515916043713, -25.00736669481004526, 23.92354251275963861 ) ) ;
#5009=ORIENTED_EDGE ( 'NONE', *, *, #8118, .F. ) ;
#5011=CARTESIAN_POINT ( 'NONE',  ( -20.20700224038492721, 0.9908225410482660589, 29.58392382092671724 ) ) ;
#5022=ORIENTED_EDGE ( 'NONE', *, *, #11967, .T. ) ;
#5032=CARTESIAN_POINT ( 'NONE',  ( -20.20700224038492721, -27.82980252387826781, -10.08426345511578504 ) ) ;
#5039=CARTESIAN_POINT ( 'NONE',  ( -55.24198130335446422, -0.008252882783648586573, -0.004276389980780055493 ) ) ;
#5042=CARTESIAN_POINT ( 'NONE',  ( -1.583189561560252701, -46.33203782964464068, -2.490696082059713046 ) ) ;
#5044=AXIS2_PLACEMENT_3D ( 'NONE', #5843, #3663, #25973 ) ;
#5045=CARTESIAN_POINT ( 'NONE',  ( -55.24271866751342941, -0.006757859501009782881, 0.006671293903667897471 ) ) ;
#5053=CARTESIAN_POINT ( 'NONE',  ( -20.21097721650787093, -8.835581399094968091, 28.26295598655181607 ) ) ;
#5054=ORIENTED_EDGE ( 'NONE', *, *, #5500, .F. ) ;
#5063=EDGE_CURVE ( 'NONE', #23740, #15365, #24055, .T. ) ;
#5065=CARTESIAN_POINT ( 'NONE',  ( -20.24399999263414784, -28.55700515887714275, 7.930419334766489747 ) ) ;
#5075=B_SPLINE_CURVE_WITH_KNOTS ( 'NONE', 3,
 ( #27069, #10079, #1280, #18845, #27614, #13839, #7935, #15864, #11540, #25491 ),
 .UNSPECIFIED., .F., .F.,
 ( 4, 2, 2, 2, 4 ),
 ( 2.888718286224068903E-16, 0.0003346187017559086596, 0.0006692374035115283793, 0.001003856105267148099, 0.001338474807022767927 ),
 .UNSPECIFIED. ) ;
#5087=CARTESIAN_POINT ( 'NONE',  ( -1.031422197589711764, 36.13727897780167808, 28.14735071801703725 ) ) ;
#5092=EDGE_CURVE ( 'NONE', #27064, #14776, #27373, .T. ) ;
#5097=B_SPLINE_CURVE_WITH_KNOTS ( 'NONE', 3,
 ( #5007, #7326, #3432, #26884, #13784, #22592, #14357 ),
 .UNSPECIFIED., .F., .F.,
 ( 4, 3, 4 ),
 ( 0.000000000000000000, 0.006568092053401826565, 0.02506242213020857396 ),
 .UNSPECIFIED. ) ;
#5099=FACE_OUTER_BOUND ( 'NONE', #23142, .T. ) ;
#5100=VECTOR ( 'NONE', #12463, 1000.000000000000114 ) ;
#5106=DIRECTION ( 'NONE',  ( 0.7563875759206388771, 0.03500244528122559151, -0.6531865459554678788 ) ) ;
#5110=EDGE_LOOP ( 'NONE', ( #15024, #24395, #18397, #8044 ) ) ;
#5111=CARTESIAN_POINT ( 'NONE',  ( -1.056502255334264895, 43.40574022158773460, -14.64009593116116292 ) ) ;
#5113=CARTESIAN_POINT ( 'NONE',  ( -8.786685647604898008, 48.22796981442765940, -23.24040270374399952 ) ) ;
#5129=CARTESIAN_POINT ( 'NONE',  ( -1.155031165708882757, 2.068616213631583545, 45.85732438018710866 ) ) ;
#5131=ORIENTED_EDGE ( 'NONE', *, *, #12730, .T. ) ;
#5132=CARTESIAN_POINT ( 'NONE',  ( -1.019300379054419725, 35.83762006677400791, -28.53917295602911253 ) ) ;
#5134=VERTEX_POINT ( 'NONE', #8811 ) ;
#5135=CARTESIAN_POINT ( 'NONE',  ( -21.41430102051752016, -16.60879216503617073, 25.94791611261633690 ) ) ;
#5139=CARTESIAN_POINT ( 'NONE',  ( -1.045287976400386842, 37.92705037016744285, -25.66401692420027203 ) ) ;
#5141=CARTESIAN_POINT ( 'NONE',  ( -25.21435515916043002, -4.655591116594591128, -34.29329011225954105 ) ) ;
#5143=CARTESIAN_POINT ( 'NONE',  ( -55.24390624410018802, 0.001451500391951047672, 0.01032895241566990016 ) ) ;
#5150=CARTESIAN_POINT ( 'NONE',  ( -20.20700224038492010, 8.199606986804733211, 28.44216453106527709 ) ) ;
#5158=CARTESIAN_POINT ( 'NONE',  ( -25.21435515916043713, 23.92354251275973809, 25.00736669480994934 ) ) ;
#5162=CARTESIAN_POINT ( 'NONE',  ( -24.53239521893627995, 33.25736993155740606, -6.738460611583019677 ) ) ;
#5164=B_SPLINE_CURVE_WITH_KNOTS ( 'NONE', 3,
 ( #14915, #23735, #10348, #25308, #6023, #21109, #1397, #27451 ),
 .UNSPECIFIED., .F., .F.,
 ( 4, 2, 2, 4 ),
 ( 0.000000000000000000, 0.002761524886576651079, 0.005523049773153302158, 0.01104609954630660432 ),
 .UNSPECIFIED. ) ;
#5166=CARTESIAN_POINT ( 'NONE',  ( -20.24399999263414784, 16.36687688782894412, 24.70869149526185282 ) ) ;
#5172=ORIENTED_EDGE ( 'NONE', *, *, #3303, .F. ) ;
#5180=EDGE_LOOP ( 'NONE', ( #802, #3561, #25283, #12153 ) ) ;
#5186=CARTESIAN_POINT ( 'NONE',  ( -1.583189561560253589, -36.01941156322766346, 29.24830400313204848 ) ) ;
#5191=CARTESIAN_POINT ( 'NONE',  ( -1.155001620486251213, 2.068551059060327546, -45.85729774065935516 ) ) ;
#5200=B_SPLINE_CURVE_WITH_KNOTS ( 'NONE', 3,
 ( #20264, #11642, #16240, #22446, #699, #9781, #2714, #11792, #9354, #7196 ),
 .UNSPECIFIED., .F., .F.,
 ( 4, 2, 2, 2, 4 ),
 ( 4.210279659405072890E-18, 0.0003346267210630970664, 0.0006692534421261899045, 0.001003880163189282580, 0.001338506884252375472 ),
 .UNSPECIFIED. ) ;
#5204=EDGE_CURVE ( 'NONE', #17827, #2087, #15319, .T. ) ;
#5205=VERTEX_POINT ( 'NONE', #13683 ) ;
#5206=ORIENTED_EDGE ( 'NONE', *, *, #21632, .F. ) ;
#5213=CARTESIAN_POINT ( 'NONE',  ( -21.41430102051751305, -23.81424706376350287, 19.54553566814611898 ) ) ;
#5215=CARTESIAN_POINT ( 'NONE',  ( -12.94347594948494340, 6.555928820869281637, -48.30328466416744249 ) ) ;
#5220=CARTESIAN_POINT ( 'NONE',  ( -20.21097721650786738, -9.464413208035280078, -28.05863614620935209 ) ) ;
#5221=CARTESIAN_POINT ( 'NONE',  ( -10.86508079875782329, 24.22249093393363850, 45.04061326950845512 ) ) ;
#5222=CARTESIAN_POINT ( 'NONE',  ( -8.786685647604885574, 6.096987947571466530E-17, -1.524246986892866633E-17 ) ) ;
#5223=CARTESIAN_POINT ( 'NONE',  ( -21.81686047589426991, 6.867757412721210208, 37.90526371014249918 ) ) ;
#5235=EDGE_CURVE ( 'NONE', #28150, #7707, #3659, .T. ) ;
#5239=ADVANCED_FACE ( 'NONE', ( #7234 ), #25890, .T. ) ;
#5254=DIRECTION ( 'NONE',  ( 0.7563875759206388771, -0.2351350468682826267, 0.6104009704506950795 ) ) ;
#5255=CARTESIAN_POINT ( 'NONE',  ( -21.41427618760458884, 11.22988868156184772, -28.68857606049970244 ) ) ;
#5257=CARTESIAN_POINT ( 'NONE',  ( -15.02187109954786060, -8.264310930412701595, -45.60876405941874623 ) ) ;
#5262=CARTESIAN_POINT ( 'NONE',  ( -22.23342874802667879, -30.68433055777675733, 7.677086057585283285 ) ) ;
#5263=CARTESIAN_POINT ( 'NONE',  ( -1.155001620486253877, 45.85729774065937647, 2.068551059060488750 ) ) ;
#5264=CARTESIAN_POINT ( 'NONE',  ( -1.155001620486248548, -38.31519699443482097, 25.28075036143263077 ) ) ;
#5266=CARTESIAN_POINT ( 'NONE',  ( -25.21435515916025594, 1.749597353048488237E-16, -4.373993382621220594E-17 ) ) ;
#5268=ORIENTED_EDGE ( 'NONE', *, *, #6000, .T. ) ;
#5270=EDGE_CURVE ( 'NONE', #4384, #21682, #8227, .T. ) ;
#5271=CARTESIAN_POINT ( 'NONE',  ( -24.53239521893647179, -33.71193723315173685, -3.868435622621356096 ) ) ;
#5272=CARTESIAN_POINT ( 'NONE',  ( -20.20700224038492721, 0.9908225410478516126, -29.58392382092673145 ) ) ;
#5273=VERTEX_POINT ( 'NONE', #9823 ) ;
#5276=CARTESIAN_POINT ( 'NONE',  ( -24.53237795827032031, -16.68575684089471878, 29.54731592868582979 ) ) ;
#5278=ORIENTED_EDGE ( 'NONE', *, *, #15826, .T. ) ;
#5283=CARTESIAN_POINT ( 'NONE',  ( -55.24340739397742084, 0.009842732675352565408, -0.002421372372454350108 ) ) ;
#5284=B_SPLINE_CURVE_WITH_KNOTS ( 'NONE', 3,
 ( #7723, #16478, #17037, #23123 ),
 .UNSPECIFIED., .F., .F.,
 ( 4, 4 ),
 ( 2.005388357681274105E-16, 0.001982023823822939412 ),
 .UNSPECIFIED. ) ;
#5286=CARTESIAN_POINT ( 'NONE',  ( -20.57838717382308147, 29.92853265176831812, -1.611677988432464126 ) ) ;
#5288=CARTESIAN_POINT ( 'NONE',  ( -22.23342874802668589, 26.81018246605539446, -16.78332232459650797 ) ) ;
#5293=CARTESIAN_POINT ( 'NONE',  ( -1.050229599974481065, 36.90196321294333615, 27.12684363859215608 ) ) ;
#5297=CARTESIAN_POINT ( 'NONE',  ( -7.711401346138264223, -38.61705198405337569, 35.51061203065550131 ) ) ;
#5298=CARTESIAN_POINT ( 'NONE',  ( -20.38016308990357928, -18.69911008768351479, -23.16952666206578826 ) ) ;
#5301=VERTEX_POINT ( 'NONE', #16431 ) ;
#5303=CARTESIAN_POINT ( 'NONE',  ( -1.113427685307007975, 44.18561238466754304, 12.28784199929889098 ) ) ;
#5314=CARTESIAN_POINT ( 'NONE',  ( -6.588769196390754423, -20.50531526814530636, 47.06982923582530276 ) ) ;
#5318=CARTESIAN_POINT ( 'NONE',  ( -20.47566338032530808, 25.06314818626709240, 16.24827550219793437 ) ) ;
#5329=CARTESIAN_POINT ( 'NONE',  ( -55.25719721206881729, 0.004044147484875269816, -0.01041086141212288138 ) ) ;
#5338=EDGE_CURVE ( 'NONE', #24458, #13365, #8825, .T. ) ;
#5340=B_SPLINE_CURVE_WITH_KNOTS ( 'NONE', 3,
 ( #24711, #13735, #2508, #7420, #7146, #16037, #2360, #24841 ),
 .UNSPECIFIED., .F., .F.,
 ( 4, 2, 2, 4 ),
 ( 0.000000000000000000, 0.002761524886576648477, 0.005523049773153296954, 0.01104609954630659391 ),
 .UNSPECIFIED. ) ;
#5343=CARTESIAN_POINT ( 'NONE',  ( -21.41430102051744555, 1.815007301162403497, 30.75470819672109002 ) ) ;
#5346=CARTESIAN_POINT ( 'NONE',  ( -55.24728320129491266, 0.01453410071985698077, 0.0006547948648746833647 ) ) ;
#5347=ORIENTED_EDGE ( 'NONE', *, *, #17831, .T. ) ;
#5353=EDGE_CURVE ( 'NONE', #22045, #12390, #20737, .T. ) ;
#5355=DIRECTION ( 'NONE',  ( 1.000000000000000000, -6.938893903907226837E-18, 1.734723475976806709E-18 ) ) ;
#5359=ORIENTED_EDGE ( 'NONE', *, *, #19131, .F. ) ;
#5363=CARTESIAN_POINT ( 'NONE',  ( -20.47566262905010248, 25.06314747784837138, -16.24827521404660047 ) ) ;
#5378=( BOUNDED_SURFACE ( )  B_SPLINE_SURFACE ( 3, 1, ( 
 ( #4161, #12518 ),
 ( #1855, #8364 ),
 ( #25644, #28331 ),
 ( #15088, #23907 ) ),
 .UNSPECIFIED., .F., .F., .F. ) 
 B_SPLINE_SURFACE_WITH_KNOTS ( ( 4, 4 ),
 ( 2, 2 ),
 ( 0.000000000000000000, 1.000000000000000000 ),
 ( 0.000000000000000000, 1.000000000000000000 ),
 .UNSPECIFIED. ) 
 GEOMETRIC_REPRESENTATION_ITEM ( )  RATIONAL_B_SPLINE_SURFACE ( (
 ( 1.000000000000000000, 1.000000000000000000),
 ( 0.9934239774497837239, 0.8357310067453919133),
 ( 0.9934239774497837239, 0.8357310067453919133),
 ( 1.000000000000000000, 1.000000000000000000) ) ) 
 REPRESENTATION_ITEM ( '' )  SURFACE ( )  );
#5379=VERTEX_POINT ( 'NONE', #16428 ) ;
#5385=CARTESIAN_POINT ( 'NONE',  ( -55.24728320129491266, -0.01362040845703012606, 0.005114031043466422087 ) ) ;
#5393=CARTESIAN_POINT ( 'NONE',  ( -20.20700224038492721, 18.19058640100257662, 23.35150625415638714 ) ) ;
#5399=ORIENTED_EDGE ( 'NONE', *, *, #2654, .F. ) ;
#5403=EDGE_CURVE ( 'NONE', #19868, #20968, #1802, .T. ) ;
#5420=ORIENTED_EDGE ( 'NONE', *, *, #14588, .F. ) ;
#5422=EDGE_CURVE ( 'NONE', #6247, #25314, #2838, .T. ) ;
#5423=CARTESIAN_POINT ( 'NONE',  ( -28.13707043255157103, -18.96624908365836859, 12.83104814250474668 ) ) ;
#5424=CARTESIAN_POINT ( 'NONE',  ( -1.049819825607590351, 14.63675055554442395, 43.39756533277866879 ) ) ;
#5429=FACE_OUTER_BOUND ( 'NONE', #17472, .T. ) ;
#5434=ORIENTED_EDGE ( 'NONE', *, *, #23124, .T. ) ;
#5437=CARTESIAN_POINT ( 'NONE',  ( -1.619063947482201282, 11.94059994246159384, -44.80407745103787676 ) ) ;
#5442=CARTESIAN_POINT ( 'NONE',  ( -28.41354790283022069, -18.00456980371910376, -14.62505768302794529 ) ) ;
#5444=ORIENTED_EDGE ( 'NONE', *, *, #9030, .F. ) ;
#5449=CARTESIAN_POINT ( 'NONE',  ( -55.24728320129491266, -0.01137345571546789259, 0.009072670231975133240 ) ) ;
#5456=CARTESIAN_POINT ( 'NONE',  ( -18.41936578851711204, 41.75701384111740566, -7.566034416290932541 ) ) ;
#5460=CARTESIAN_POINT ( 'NONE',  ( -55.24198130335446422, -0.006617369590171728877, 0.006527480770973505091 ) ) ;
#5461=CONICAL_SURFACE ( 'NONE', #12812, 34.60786435723138510, 0.8559913436420825139 ) ;
#5462=EDGE_CURVE ( 'NONE', #24670, #15546, #11991, .T. ) ;
#5463=CARTESIAN_POINT ( 'NONE',  ( -1.048171036023512803, -15.11933492062798656, 43.23005599774316465 ) ) ;
#5470=B_SPLINE_CURVE_WITH_KNOTS ( 'NONE', 3,
 ( #5150, #12475, #5740, #3979 ),
 .UNSPECIFIED., .F., .F.,
 ( 4, 4 ),
 ( 1.877672896018868361E-16, 0.001982023823822947652 ),
 .UNSPECIFIED. ) ;
#5475=ORIENTED_EDGE ( 'NONE', *, *, #12024, .F. ) ;
#5479=CARTESIAN_POINT ( 'NONE',  ( -1.539760825549692180, 11.93465943778514315, -44.72358953107736568 ) ) ;
#5482=EDGE_LOOP ( 'NONE', ( #2793, #22821 ) ) ;
#5489=CARTESIAN_POINT ( 'NONE',  ( -8.786685647604890903, 47.14957014837354876, -25.35688121747519119 ) ) ;
#5490=VERTEX_POINT ( 'NONE', #4031 ) ;
#5496=EDGE_CURVE ( 'NONE', #17315, #8356, #15668, .T. ) ;
#5498=FACE_OUTER_BOUND ( 'NONE', #1629, .T. ) ;
#5500=EDGE_CURVE ( 'NONE', #22518, #21826, #2270, .T. ) ;
#5501=B_SPLINE_CURVE_WITH_KNOTS ( 'NONE', 3,
 ( #18069, #20220, #27129, #5262, #24724, #7014 ),
 .UNSPECIFIED., .F., .F.,
 ( 4, 2, 4 ),
 ( 3.689388176052398149E-16, 0.003576372551511164399, 0.007152745103021965374 ),
 .UNSPECIFIED. ) ;
#5502=CARTESIAN_POINT ( 'NONE',  ( -20.37983603106074426, -28.74620395171555742, 7.753708011498863684 ) ) ;
#5504=CARTESIAN_POINT ( 'NONE',  ( -20.21097721650785672, 17.13687097598137399, -24.14932365326959030 ) ) ;
#5505=CARTESIAN_POINT ( 'NONE',  ( 60.46576798286869803, -12.50000000000000000, 1.048913872128491071E-16 ) ) ;
#5508=CARTESIAN_POINT ( 'NONE',  ( -20.20997486282892552, 0.3303599360442536770, 29.60348406988233450 ) ) ;
#5509=CARTESIAN_POINT ( 'NONE',  ( -1.464342487929864323, -25.15873223207664466, 38.76467504336611114 ) ) ;
#5513=CARTESIAN_POINT ( 'NONE',  ( -28.41354790283022069, -19.47297445639540214, 12.60397206714853624 ) ) ;
#5514=CARTESIAN_POINT ( 'NONE',  ( -1.031422197589716205, -45.78027046666443312, 1.530725436377931237 ) ) ;
#5515=CARTESIAN_POINT ( 'NONE',  ( -6.588769196390764193, -11.07780292579730208, -50.13301368233293687 ) ) ;
#5516=ORIENTED_EDGE ( 'NONE', *, *, #6111, .F. ) ;
#5517=CARTESIAN_POINT ( 'NONE',  ( -1.155031165708886087, 25.28071330859886245, -38.31525684316149949 ) ) ;
#5518=VERTEX_POINT ( 'NONE', #8634 ) ;
#5523=VERTEX_POINT ( 'NONE', #17264 ) ;
#5533=AXIS2_PLACEMENT_3D ( 'NONE', #13930, #13642, #20259 ) ;
#5538=CONICAL_SURFACE ( 'NONE', #1415, 34.60786435723138510, 0.8559913436420825139 ) ;
#5545=CARTESIAN_POINT ( 'NONE',  ( -55.24390624410018802, 0.01027195578987812573, -0.001811362924359468263 ) ) ;
#5548=CARTESIAN_POINT ( 'NONE',  ( -20.20700224038492365, 8.199606986804329978, -28.44216453106539078 ) ) ;
#5549=CARTESIAN_POINT ( 'NONE',  ( -1.045287976400383290, -36.12803364096628655, -28.14015102489793918 ) ) ;
#5558=ORIENTED_EDGE ( 'NONE', *, *, #3935, .T. ) ;
#5560=AXIS2_PLACEMENT_3D ( 'NONE', #13218, #6341, #19567 ) ;
#5565=CARTESIAN_POINT ( 'NONE',  ( -55.24300891470650754, -0.009812809446892518245, 0.0003472257464213444889 ) ) ;
#5566=AXIS2_PLACEMENT_3D ( 'NONE', #21566, #24299, #4143 ) ;
#5585=CARTESIAN_POINT ( 'NONE',  ( -55.24390624410018802, -0.007503127514281482044, 0.007245494385991411469 ) ) ;
#5587=CARTESIAN_POINT ( 'NONE',  ( -20.20700224038492721, -24.51628800869035274, 16.58740185276737122 ) ) ;
#5590=CARTESIAN_POINT ( 'NONE',  ( -55.24340739397742084, 0.005344433640973447058, 0.008612749836246493332 ) ) ;
#5592=VERTEX_POINT ( 'NONE', #559 ) ;
#5601=LINE ( 'NONE', #16242, #7299 ) ;
#5608=CARTESIAN_POINT ( 'NONE',  ( -4.473127245936434626, 47.80062405537817938, 12.17046501147466842 ) ) ;
#5609=EDGE_CURVE ( 'NONE', #25165, #23320, #11644, .T. ) ;
#5610=ORIENTED_EDGE ( 'NONE', *, *, #19384, .T. ) ;
#5611=CARTESIAN_POINT ( 'NONE',  ( -1.031422197589716205, 15.60268798220698017, 43.06660437151292342 ) ) ;
#5616=CARTESIAN_POINT ( 'NONE',  ( -55.24271866751342941, -0.008488649505345844185, 0.004256484107793130807 ) ) ;
#5618=CARTESIAN_POINT ( 'NONE',  ( -1.031422197589716205, -1.530725436377144755, 45.78027046666445443 ) ) ;
#5625=ORIENTED_EDGE ( 'NONE', *, *, #24669, .F. ) ;
#5628=CARTESIAN_POINT ( 'NONE',  ( -20.57838717382308147, 18.89542499756500149, -23.26537097894111383 ) ) ;
#5630=CARTESIAN_POINT ( 'NONE',  ( -1.323439229708141429, 12.01475235539445485, -44.47813215539048315 ) ) ;
#5636=CARTESIAN_POINT ( 'NONE',  ( -20.37983603106073716, -23.16947629293375854, -18.69865230096518616 ) ) ;
#5639=CARTESIAN_POINT ( 'NONE',  ( -20.20700224038492010, -16.58740185276728241, -24.51628800869040958 ) ) ;
#5640=CONICAL_SURFACE ( 'NONE', #16663, 34.60786435723138510, 0.8559913436420825139 ) ;
#5642=EDGE_CURVE ( 'NONE', #27723, #13723, #18267, .T. ) ;
#5656=B_SPLINE_CURVE_WITH_KNOTS ( 'NONE', 3,
 ( #11591, #14165, #1089, #15911, #5255, #20369 ),
 .UNSPECIFIED., .F., .F.,
 ( 4, 2, 4 ),
 ( 3.409603294638168262E-16, 0.003576372551511143149, 0.007152745103021945425 ),
 .UNSPECIFIED. ) ;
#5659=CIRCLE ( 'NONE', #23614, 53.53553390275978785 ) ;
#5691=CARTESIAN_POINT ( 'NONE',  ( -1.463510566862830986, 29.09194585123833932, -35.90603835816513367 ) ) ;
#5692=APPLICATION_CONTEXT ( 'automotive_design' ) ;
#5694=CARTESIAN_POINT ( 'NONE',  ( -24.53239521893647179, -16.68574937150994231, -29.54733954334103174 ) ) ;
#5697=EDGE_CURVE ( 'NONE', #7508, #27740, #9731, .T. ) ;
#5699=VERTEX_POINT ( 'NONE', #12348 ) ;
#5702=CARTESIAN_POINT ( 'NONE',  ( -1.113427685306995318, 28.52429901637220411, 35.91272432484627330 ) ) ;
#5708=CARTESIAN_POINT ( 'NONE',  ( -55.25719721206881729, -0.009391134844732829459, -0.006045473558784549006 ) ) ;
#5709=ADVANCED_FACE ( 'NONE', ( #21934 ), #28312, .F. ) ;
#5721=CARTESIAN_POINT ( 'NONE',  ( -1.619063947482194177, 29.22875152547808852, 35.99532424477347092 ) ) ;
#5731=ORIENTED_EDGE ( 'NONE', *, *, #3967, .T. ) ;
#5732=( BOUNDED_SURFACE ( )  B_SPLINE_SURFACE ( 3, 1, ( 
 ( #7112, #4359 ),
 ( #13414, #4793 ),
 ( #26373, #21920 ),
 ( #19900, #10987 ) ),
 .UNSPECIFIED., .F., .F., .F. ) 
 B_SPLINE_SURFACE_WITH_KNOTS ( ( 4, 4 ),
 ( 2, 2 ),
 ( 0.000000000000000000, 1.000000000000000000 ),
 ( 0.000000000000000000, 1.000000000000000000 ),
 .UNSPECIFIED. ) 
 GEOMETRIC_REPRESENTATION_ITEM ( )  RATIONAL_B_SPLINE_SURFACE ( (
 ( 1.000000000000000000, 1.000000000000000000),
 ( 0.9934239774497838349, 0.8357310067453913582),
 ( 0.9934239774497838349, 0.8357310067453913582),
 ( 1.000000000000000000, 1.000000000000000000) ) ) 
 REPRESENTATION_ITEM ( '' )  SURFACE ( )  );
#5737=ORIENTED_EDGE ( 'NONE', *, *, #7671, .T. ) ;
#5739=ORIENTED_EDGE ( 'NONE', *, *, #24669, .T. ) ;
#5740=CARTESIAN_POINT ( 'NONE',  ( -20.21097721650786738, 9.464413208035470149, 28.05863614620928459 ) ) ;
#5743=CARTESIAN_POINT ( 'NONE',  ( -24.53239521893647890, -6.738460611583005466, -33.25736993155761922 ) ) ;
#5745=DIRECTION ( 'NONE',  ( 1.000000000000000000, -6.938893903907226837E-18, 1.734723475976806709E-18 ) ) ;
#5746=EDGE_LOOP ( 'NONE', ( #10300, #11762, #18359, #8310 ) ) ;
#5752=CARTESIAN_POINT ( 'NONE',  ( -1.539760825549689294, 44.72358953107748647, 11.93465943778467597 ) ) ;
#5755=CARTESIAN_POINT ( 'NONE',  ( -20.57838717382308147, 18.89542499756533545, 23.26537097894084383 ) ) ;
#5758=ORIENTED_EDGE ( 'NONE', *, *, #18604, .T. ) ;
#5765=CARTESIAN_POINT ( 'NONE',  ( -1.046935749539997573, 45.77872888003167162, 1.275486069320633353 ) ) ;
#5767=CARTESIAN_POINT ( 'NONE',  ( -23.79223135445720061, 3.207301057648340503, -33.03345552685145492 ) ) ;
#5774=DIRECTION ( 'NONE',  ( -1.000000000000000000, 6.938893903907226837E-18, -1.734723475976806709E-18 ) ) ;
#5785=CARTESIAN_POINT ( 'NONE',  ( -1.583189561560253589, 38.94740041318330981, 25.21827308671188561 ) ) ;
#5789=CARTESIAN_POINT ( 'NONE',  ( -20.24399999263415850, -18.44171895251379567, 23.20123049637386003 ) ) ;
#5805=DIRECTION ( 'NONE',  ( 1.000000000000000000, -6.938893903907226837E-18, 1.734723475976806709E-18 ) ) ;
#5813=CARTESIAN_POINT ( 'NONE',  ( -22.23342874802668234, -11.82490389046295043, 29.33662284748872651 ) ) ;
#5814=CARTESIAN_POINT ( 'NONE',  ( -20.20898968516257810, 0.6607166829023055632, 29.59696826051171925 ) ) ;
#5817=CARTESIAN_POINT ( 'NONE',  ( -55.24390624410018802, 0.01032895241567037548, -0.001451500391950801341 ) ) ;
#5819=CARTESIAN_POINT ( 'NONE',  ( -7.078251931573406708, 11.16394717458676311, -50.86685171665416050 ) ) ;
#5843=CARTESIAN_POINT ( 'NONE',  ( 0.000000000000000000, 0.000000000000000000, 0.000000000000000000 ) ) ;
#5847=CARTESIAN_POINT ( 'NONE',  ( -9.156249394959713683, -8.027840202794317648, -53.90509764945126392 ) ) ;
#5849=CARTESIAN_POINT ( 'NONE',  ( -1.019300379054419725, 2.023851374323315078, 45.76814864815086992 ) ) ;
#5860=ORIENTED_EDGE ( 'NONE', *, *, #28321, .F. ) ;
#5861=CARTESIAN_POINT ( 'NONE',  ( -1.463510566862828766, -43.13857742234517190, -16.57250862017402682 ) ) ;
#5867=DIRECTION ( 'NONE',  ( 0.7637818620346800147, 0.3617919495470829916, 0.5345501402766235088 ) ) ;
#5871=EDGE_CURVE ( 'NONE', #21801, #3497, #28265, .T. ) ;
#5878=CARTESIAN_POINT ( 'NONE',  ( -55.24340739397742084, -0.006539691034612123317, 0.007744344507854589339 ) ) ;
#5883=CARTESIAN_POINT ( 'NONE',  ( -1.044557008772714513, -12.57891310333380552, -44.03203053429566438 ) ) ;
#5885=LINE ( 'NONE', #12896, #8807 ) ;
#5900=CARTESIAN_POINT ( 'NONE',  ( -1.463510566862834539, 38.76366072687779507, -25.15876608740827436 ) ) ;
#5902=EDGE_LOOP ( 'NONE', ( #14282, #18232, #26452, #12564 ) ) ;
#5903=ADVANCED_FACE ( 'NONE', ( #22375 ), #7755, .F. ) ;
#5906=FACE_OUTER_BOUND ( 'NONE', #11611, .T. ) ;
#5907=( BOUNDED_SURFACE ( )  B_SPLINE_SURFACE ( 3, 1, ( 
 ( #10239, #14384 ),
 ( #19001, #6194 ),
 ( #16972, #1705 ),
 ( #10086, #25763 ) ),
 .UNSPECIFIED., .F., .F., .F. ) 
 B_SPLINE_SURFACE_WITH_KNOTS ( ( 4, 4 ),
 ( 2, 2 ),
 ( 0.000000000000000000, 1.000000000000000000 ),
 ( 0.000000000000000000, 1.000000000000000000 ),
 .UNSPECIFIED. ) 
 GEOMETRIC_REPRESENTATION_ITEM ( )  RATIONAL_B_SPLINE_SURFACE ( (
 ( 1.000000000000000000, 1.000000000000000000),
 ( 0.7789835883360578528, 0.9689951854195403280),
 ( 0.7789835883360578528, 0.9689951854195403280),
 ( 1.000000000000000000, 1.000000000000000000) ) ) 
 REPRESENTATION_ITEM ( '' )  SURFACE ( )  );
#5908=CARTESIAN_POINT ( 'NONE',  ( -28.13707043255157103, 6.342158660427315020, 22.00298671236732773 ) ) ;
#5914=CARTESIAN_POINT ( 'NONE',  ( -1.583189561560253589, 46.33203782964461936, -2.490696082060032790 ) ) ;
#5915=CARTESIAN_POINT ( 'NONE',  ( -1.323830074806774615, -16.42382241777507090, 43.04593525292983003 ) ) ;
#5916=CARTESIAN_POINT ( 'NONE',  ( -1.463510566862831208, -46.14841196428341874, -2.430838777910016901 ) ) ;
#5933=CARTESIAN_POINT ( 'NONE',  ( -4.162674018437135359, 31.44946543094296487, -37.46098494546600932 ) ) ;
#5935=VERTEX_POINT ( 'NONE', #18906 ) ;
#5942=CARTESIAN_POINT ( 'NONE',  ( -7.078251931573400491, -20.86696228105191864, 47.71415099571825635 ) ) ;
#5943=( BOUNDED_SURFACE ( )  B_SPLINE_SURFACE ( 3, 1, ( 
 ( #3294, #841 ),
 ( #7479, #12077 ),
 ( #27462, #3148 ),
 ( #20695, #558 ) ),
 .UNSPECIFIED., .F., .F., .F. ) 
 B_SPLINE_SURFACE_WITH_KNOTS ( ( 4, 4 ),
 ( 2, 2 ),
 ( 0.000000000000000000, 1.000000000000000000 ),
 ( 0.000000000000000000, 1.000000000000000000 ),
 .UNSPECIFIED. ) 
 GEOMETRIC_REPRESENTATION_ITEM ( )  RATIONAL_B_SPLINE_SURFACE ( (
 ( 1.000000000000000000, 1.000000000000000000),
 ( 0.9934239774497838349, 0.8357310067453913582),
 ( 0.9934239774497838349, 0.8357310067453913582),
 ( 1.000000000000000000, 1.000000000000000000) ) ) 
 REPRESENTATION_ITEM ( '' )  SURFACE ( )  );
#5944=ADVANCED_FACE ( 'NONE', ( #1619 ), #1480, .F. ) ;
#5947=B_SPLINE_CURVE_WITH_KNOTS ( 'NONE', 3,
 ( #8625, #24177, #26046, #23631, #21441, #26316 ),
 .UNSPECIFIED., .F., .F.,
 ( 4, 2, 4 ),
 ( 5.135960789613967459E-18, 0.0004335151646191499485, 0.0008670303292382946928 ),
 .UNSPECIFIED. ) ;
#5948=CARTESIAN_POINT ( 'NONE',  ( -18.41936578851711559, 29.33493038358074045, -30.66520733838660462 ) ) ;
#5951=CARTESIAN_POINT ( 'NONE',  ( -20.20700224038492010, 18.19058640100223556, -23.35150625415664649 ) ) ;
#5957=CARTESIAN_POINT ( 'NONE',  ( -55.25719721206881729, -0.007063345920780820901, -0.008651607285661404648 ) ) ;
#5961=VERTEX_POINT ( 'NONE', #18616 ) ;
#5968=ADVANCED_FACE ( 'NONE', ( #14438 ), #23394, .F. ) ;
#5969=DIRECTION ( 'NONE',  ( 0.000000000000000000, -1.000000000000000000, 0.000000000000000000 ) ) ;
#5971=CARTESIAN_POINT ( 'NONE',  ( -23.77929240705205771, -25.06639637888440220, -26.20227034809546041 ) ) ;
#5973=CARTESIAN_POINT ( 'NONE',  ( -20.20612092514785019, 27.77903665678167400, -10.22177639105870384 ) ) ;
#5986=CARTESIAN_POINT ( 'NONE',  ( 14.74894986621300319, -1.023413983156987147E-16, 2.558534957892467869E-17 ) ) ;
#5988=ORIENTED_EDGE ( 'NONE', *, *, #491, .F. ) ;
#5989=CARTESIAN_POINT ( 'NONE',  ( -55.24390624410018802, -0.007503127514281482044, 0.007245494385991411469 ) ) ;
#5990=CARTESIAN_POINT ( 'NONE',  ( -55.24300891470650754, 0.005486913146700745682, -0.008142823778062297305 ) ) ;
#6000=EDGE_CURVE ( 'NONE', #5518, #9315, #2547, .T. ) ;
#6015=B_SPLINE_CURVE_WITH_KNOTS ( 'NONE', 3,
 ( #22805, #20616, #16450, #3489 ),
 .UNSPECIFIED., .F., .F.,
 ( 4, 4 ),
 ( 1.904170172768910460E-16, 0.001982023823822945917 ),
 .UNSPECIFIED. ) ;
#6018=CARTESIAN_POINT ( 'NONE',  ( -19.53423201713129842, 4.045852573675910766E-15, -28.92774122539760384 ) ) ;
#6023=CARTESIAN_POINT ( 'NONE',  ( -5.986830583229487246, -50.53158596890438758, 4.559539818181663762 ) ) ;
#6027=FACE_OUTER_BOUND ( 'NONE', #8960, .T. ) ;
#6031=ORIENTED_EDGE ( 'NONE', *, *, #7257, .T. ) ;
#6034=EDGE_CURVE ( 'NONE', #17270, #8158, #82, .T. ) ;
#6039=CARTESIAN_POINT ( 'NONE',  ( -25.21435515916043357, -16.39063784838764093, -30.48034229288631991 ) ) ;
#6040=CARTESIAN_POINT ( 'NONE',  ( -7.078251931573400491, 11.16394717458747898, 50.86685171665398997 ) ) ;
#6051=LINE ( 'NONE', #5908, #2312 ) ;
#6052=CARTESIAN_POINT ( 'NONE',  ( -1.050231094221201644, -13.91061116148162391, 43.63617436699752261 ) ) ;
#6053=CIRCLE ( 'NONE', #19799, 53.53553390275978785 ) ;
#6054=CARTESIAN_POINT ( 'NONE',  ( -20.24399999263414429, 18.44171895251396265, -23.20123049637371793 ) ) ;
#6058=CARTESIAN_POINT ( 'NONE',  ( -1.155001620486257208, -28.62773628245643209, 35.88346938217584636 ) ) ;
#6059=CARTESIAN_POINT ( 'NONE',  ( 60.46576798286869803, -4.195655488513964285E-16, 1.048913872128491071E-16 ) ) ;
#6061=ORIENTED_EDGE ( 'NONE', *, *, #350, .F. ) ;
#6062=AXIS2_PLACEMENT_3D ( 'NONE', #11020, #6284, #19781 ) ;
#6068=CARTESIAN_POINT ( 'NONE',  ( -1.323830074806773727, 43.04593525292991529, 16.42382241777492524 ) ) ;
#6073=CARTESIAN_POINT ( 'NONE',  ( -1.031422197589716205, -15.60268798220608844, 43.06660437151324317 ) ) ;
#6078=CARTESIAN_POINT ( 'NONE',  ( -28.41354790283022069, -23.16239616762932130, -1.249099604786995332 ) ) ;
#6080=CARTESIAN_POINT ( 'NONE',  ( -8.786685647604887350, -38.68584556812326980, -37.00619870957918778 ) ) ;
#6087=EDGE_CURVE ( 'NONE', #12327, #4924, #13954, .T. ) ;
#6094=CARTESIAN_POINT ( 'NONE',  ( -1.583189561560252701, 16.68617981233703063, -43.29471907393747898 ) ) ;
#6095=CARTESIAN_POINT ( 'NONE',  ( -55.24390624410018802, -0.009374879212966679906, -0.004572280736703028189 ) ) ;
#6099=CARTESIAN_POINT ( 'NONE',  ( -8.786685647604894456, 7.199674155859698388, 53.04920435127174017 ) ) ;
#6107=CARTESIAN_POINT ( 'NONE',  ( -5.986830583229487246, -26.01297580803291964, 43.56094206392985058 ) ) ;
#6111=EDGE_CURVE ( 'NONE', #12390, #3917, #11398, .T. ) ;
#6121=CARTESIAN_POINT ( 'NONE',  ( -16.86833981943427929, 5.948101187262172296, 43.82216161736197790 ) ) ;
#6133=ADVANCED_FACE ( 'NONE', ( #1837 ), #5907, .F. ) ;
#6136=CARTESIAN_POINT ( 'NONE',  ( -9.156249394959713683, 38.17928057392048657, 38.89149400288364689 ) ) ;
#6137=( GEOMETRIC_REPRESENTATION_CONTEXT ( 3 ) GLOBAL_UNCERTAINTY_ASSIGNED_CONTEXT ( ( #22652 ) ) GLOBAL_UNIT_ASSIGNED_CONTEXT ( ( #24161, #965, #24874 ) ) REPRESENTATION_CONTEXT ( 'NONE', 'WORKASPACE' ) );
#6140=CARTESIAN_POINT ( 'NONE',  ( -2.911734481061415636, 25.69892591260268588, -40.13920818157085080 ) ) ;
#6152=PRODUCT_DEFINITION_FORMATION_WITH_SPECIFIED_SOURCE ( 'ANY', '', #15175, .NOT_KNOWN. ) ;
#6153=( BOUNDED_SURFACE ( )  B_SPLINE_SURFACE ( 3, 1, ( 
 ( #6925, #28351 ),
 ( #151, #13374 ),
 ( #17701, #26201 ),
 ( #286, #15394 ) ),
 .UNSPECIFIED., .F., .F., .F. ) 
 B_SPLINE_SURFACE_WITH_KNOTS ( ( 4, 4 ),
 ( 2, 2 ),
 ( 0.000000000000000000, 1.000000000000000000 ),
 ( 0.000000000000000000, 1.000000000000000000 ),
 .UNSPECIFIED. ) 
 GEOMETRIC_REPRESENTATION_ITEM ( )  RATIONAL_B_SPLINE_SURFACE ( (
 ( 1.000000000000000000, 1.000000000000000000),
 ( 0.7789835883360578528, 0.9689951854195403280),
 ( 0.7789835883360578528, 0.9689951854195403280),
 ( 1.000000000000000000, 1.000000000000000000) ) ) 
 REPRESENTATION_ITEM ( '' )  SURFACE ( )  );
#6154=EDGE_CURVE ( 'NONE', #21801, #14085, #25346, .T. ) ;
#6155=CARTESIAN_POINT ( 'NONE',  ( -1.045287976400365970, 28.14015102489882736, 36.12803364096558312 ) ) ;
#6168=CARTESIAN_POINT ( 'NONE',  ( -1.239374126674604337, 44.48112152129363750, 11.92219841463783503 ) ) ;
#6173=CARTESIAN_POINT ( 'NONE',  ( -2.904412668506655582, 2.864640348250632851, -47.56768199507435213 ) ) ;
#6175=CARTESIAN_POINT ( 'NONE',  ( -22.23342874802669300, 20.31166691703127114, -24.24669006619380696 ) ) ;
#6182=CARTESIAN_POINT ( 'NONE',  ( -20.20700224038492010, -0.9908225410476447781, 29.58392382092673500 ) ) ;
#6187=FACE_OUTER_BOUND ( 'NONE', #2650, .T. ) ;
#6193=CARTESIAN_POINT ( 'NONE',  ( -1.323439229708141207, -46.01398008004442630, 2.317790194800218195 ) ) ;
#6194=CARTESIAN_POINT ( 'NONE',  ( -7.078251931573400491, 44.92740138729166688, -26.33626633876239609 ) ) ;
#6197=CARTESIAN_POINT ( 'NONE',  ( -1.539763995773687499, -29.16712963492436828, 35.94321074656927095 ) ) ;
#6210=CARTESIAN_POINT ( 'NONE',  ( -1.113427685307007087, 42.96952363574832390, -16.03057832159165486 ) ) ;
#6213=ORIENTED_EDGE ( 'NONE', *, *, #1533, .T. ) ;
#6215=CARTESIAN_POINT ( 'NONE',  ( -1.583189561560255143, -46.33203782964464068, -2.490696082059702832 ) ) ;
#6217=CARTESIAN_POINT ( 'NONE',  ( -20.20612092514784663, -28.48192215759672408, -8.058517256680987728 ) ) ;
#6220=CARTESIAN_POINT ( 'NONE',  ( -1.050229599974473293, 0.2556477501659514262, -45.79907399707867199 ) ) ;
#6227=EDGE_CURVE ( 'NONE', #6545, #976, #15146, .T. ) ;
#6230=ORIENTED_EDGE ( 'NONE', *, *, #5353, .F. ) ;
#6234=CARTESIAN_POINT ( 'NONE',  ( -10.86508079875781263, -22.20099862734791074, 46.07061504567109012 ) ) ;
#6237=CARTESIAN_POINT ( 'NONE',  ( -7.711401346138435642, 45.70592430511758408, 25.75361633141439199 ) ) ;
#6242=VERTEX_POINT ( 'NONE', #19547 ) ;
#6247=VERTEX_POINT ( 'NONE', #4715 ) ;
#6255=CARTESIAN_POINT ( 'NONE',  ( -10.86508079875781618, 50.67624451685635734, 6.877801422380954044 ) ) ;
#6257=CARTESIAN_POINT ( 'NONE',  ( -1.019300379054419947, 44.15350047934399669, -12.21833869579480236 ) ) ;
#6258=CARTESIAN_POINT ( 'NONE',  ( -1.046936909428682450, 27.93981068760674802, 36.28616897897423144 ) ) ;
#6268=EDGE_LOOP ( 'NONE', ( #23361, #12832, #24833, #19188 ) ) ;
#6276=ORIENTED_EDGE ( 'NONE', *, *, #6000, .F. ) ;
#6278=VERTEX_POINT ( 'NONE', #17797 ) ;
#6279=CARTESIAN_POINT ( 'NONE',  ( -4.178947244162626973, 31.41809272265978947, 37.51424432987617053 ) ) ;
#6280=CARTESIAN_POINT ( 'NONE',  ( -1.583189561560255143, -43.29471907393753582, -16.68617981233685299 ) ) ;
#6284=DIRECTION ( 'NONE',  ( 1.000000000000000000, -6.938893903907226837E-18, 1.734723475976806709E-18 ) ) ;
#6286=CARTESIAN_POINT ( 'NONE',  ( -1.031422197589716205, -28.14735071801717936, 36.13727897780158571 ) ) ;
#6301=CARTESIAN_POINT ( 'NONE',  ( -25.21435515916043002, 23.92354251275938992, -25.00736669481030106 ) ) ;
#6302=ORIENTED_EDGE ( 'NONE', *, *, #5642, .F. ) ;
#6305=DIRECTION ( 'NONE',  ( 0.000000000000000000, -5.223019709708233256E-21, 1.000000000000000000 ) ) ;
#6309=CARTESIAN_POINT ( 'NONE',  ( -1.583189561560255143, -11.94859433442934282, -44.83405390829668136 ) ) ;
#6313=ORIENTED_EDGE ( 'NONE', *, *, #4751, .T. ) ;
#6327=CARTESIAN_POINT ( 'NONE',  ( -8.786685647604885574, 6.096987947571466530E-17, -1.524246986892866633E-17 ) ) ;
#6328=DIRECTION ( 'NONE',  ( 1.000000000000000000, -6.938893903907226837E-18, 1.734723475976806709E-18 ) ) ;
#6334=CARTESIAN_POINT ( 'NONE',  ( -1.049819825607597235, -43.39756533277870432, 14.63675055554426407 ) ) ;
#6341=DIRECTION ( 'NONE',  ( 1.000000000000000000, -6.938893903907226837E-18, 1.734723475976806709E-18 ) ) ;
#6345=CARTESIAN_POINT ( 'NONE',  ( -1.050230347699842692, 0.0002315326058698765721, -45.79907861674080749 ) ) ;
#6350=( BOUNDED_SURFACE ( )  B_SPLINE_SURFACE ( 3, 1, ( 
 ( #5545, #16193 ),
 ( #14312, #797 ),
 ( #27416, #16335 ),
 ( #14029, #27121 ) ),
 .UNSPECIFIED., .F., .F., .F. ) 
 B_SPLINE_SURFACE_WITH_KNOTS ( ( 4, 4 ),
 ( 2, 2 ),
 ( 0.000000000000000000, 1.000000000000000000 ),
 ( 0.000000000000000000, 1.000000000000000000 ),
 .UNSPECIFIED. ) 
 GEOMETRIC_REPRESENTATION_ITEM ( )  RATIONAL_B_SPLINE_SURFACE ( (
 ( 1.000000000000000000, 1.000000000000000000),
 ( 0.9934239774497837239, 0.8357310067453919133),
 ( 0.9934239774497837239, 0.8357310067453919133),
 ( 1.000000000000000000, 1.000000000000000000) ) ) 
 REPRESENTATION_ITEM ( '' )  SURFACE ( )  );
#6355=CARTESIAN_POINT ( 'NONE',  ( -12.94347594948497537, -42.93165645342824632, 23.08810053288727104 ) ) ;
#6358=B_SPLINE_CURVE_WITH_KNOTS ( 'NONE', 3,
 ( #3983, #24142, #10763, #2092, #14918, #10895, #28291, #28155 ),
 .UNSPECIFIED., .F., .F.,
 ( 4, 2, 2, 4 ),
 ( 0.000000000000000000, 0.002761524886576654115, 0.005523049773153308230, 0.01104609954630660952 ),
 .UNSPECIFIED. ) ;
#6360=CARTESIAN_POINT ( 'NONE',  ( -21.81686047589426991, -16.72402253294291796, 34.70276904128906637 ) ) ;
#6363=CARTESIAN_POINT ( 'NONE',  ( -1.045287976400365970, 45.76855895860943235, -1.530335034934267258 ) ) ;
#6364=CARTESIAN_POINT ( 'NONE',  ( -22.34422965417122953, 6.759368364654329220, -37.30738373203623581 ) ) ;
#6372=EDGE_CURVE ( 'NONE', #7039, #22163, #24602, .T. ) ;
#6376=ORIENTED_EDGE ( 'NONE', *, *, #18126, .F. ) ;
#6377=EDGE_LOOP ( 'NONE', ( #11424, #18656 ) ) ;
#6386=CARTESIAN_POINT ( 'NONE',  ( -20.57838717382308147, 7.715628353033680220, -28.96176188950220975 ) ) ;
#6387=CARTESIAN_POINT ( 'NONE',  ( -21.81686047589415622, 38.17230180719270294, 5.181745222995608025 ) ) ;
#6397=CARTESIAN_POINT ( 'NONE',  ( -4.162674018437148682, 41.48630000627055381, -25.90909455705125453 ) ) ;
#6405=ORIENTED_EDGE ( 'NONE', *, *, #22642, .T. ) ;
#6411=B_SPLINE_CURVE_WITH_KNOTS ( 'NONE', 3,
 ( #2883, #859, #9644, #13953, #5318, #4754 ),
 .UNSPECIFIED., .F., .F.,
 ( 4, 2, 4 ),
 ( 4.906538933386797396E-18, 0.0004335184443140297200, 0.0008670368886280544526 ),
 .UNSPECIFIED. ) ;
#6412=B_SPLINE_CURVE_WITH_KNOTS ( 'NONE', 3,
 ( #21868, #28192, #1997, #17257, #24045, #19838, #18236, #550 ),
 .UNSPECIFIED., .F., .F.,
 ( 4, 2, 2, 4 ),
 ( 2.196627850418165012E-16, 0.002761568181852864633, 0.005523136363705508957, 0.01104627272741078546 ),
 .UNSPECIFIED. ) ;
#6427=VECTOR ( 'NONE', #11559, 1000.000000000000114 ) ;
#6432=CARTESIAN_POINT ( 'NONE',  ( -1.058197053496154671, 25.48582931365525184, 38.06270006878825995 ) ) ;
#6434=B_SPLINE_CURVE_WITH_KNOTS ( 'NONE', 3,
 ( #28464, #4309, #13086, #21872, #2128, #25646 ),
 .UNSPECIFIED., .F., .F.,
 ( 4, 2, 4 ),
 ( 3.729292374017667178E-16, 0.003576372551511173073, 0.007152745103021973180 ),
 .UNSPECIFIED. ) ;
#6443=EDGE_CURVE ( 'NONE', #18869, #243, #23147, .T. ) ;
#6445=CARTESIAN_POINT ( 'NONE',  ( -55.24271866751342941, 0.006757859501006707216, 0.006671293903669109175 ) ) ;
#6448=CARTESIAN_POINT ( 'NONE',  ( -1.058473599757826067, -35.99997772736190882, 28.32531354681322711 ) ) ;
#6456=CARTESIAN_POINT ( 'NONE',  ( -1.323439229708126774, -12.01475235539415642, 44.47813215539056131 ) ) ;
#6468=VECTOR ( 'NONE', #9900, 1000.000000000000114 ) ;
#6469=ORIENTED_EDGE ( 'NONE', *, *, #5609, .T. ) ;
#6471=CARTESIAN_POINT ( 'NONE',  ( -55.24390624410018802, -0.007245494385991085341, 0.007503127514277716827 ) ) ;
#6482=DIRECTION ( 'NONE',  ( 1.000000000000000000, -6.938893903907226837E-18, 1.734723475976806709E-18 ) ) ;
#6485=CARTESIAN_POINT ( 'NONE',  ( -1.464342487929857661, -43.13914623307948659, 16.57334911911557285 ) ) ;
#6487=ORIENTED_EDGE ( 'NONE', *, *, #24795, .T. ) ;
#6496=VECTOR ( 'NONE', #22555, 1000.000000000000114 ) ;
#6497=FACE_OUTER_BOUND ( 'NONE', #9285, .T. ) ;
#6503=DIRECTION ( 'NONE',  ( 0.000000000000000000, 5.223019709707975211E-21, -1.000000000000000000 ) ) ;
#6504=CARTESIAN_POINT ( 'NONE',  ( -55.24271866751342941, -0.001545935011630300039, 0.009369360294295641864 ) ) ;
#6506=EDGE_CURVE ( 'NONE', #5301, #10441, #27869, .T. ) ;
#6509=CARTESIAN_POINT ( 'NONE',  ( -55.25297051322618813, 0.002853887643044372355, 0.01466904165775517396 ) ) ;
#6518=CIRCLE ( 'NONE', #8355, 34.60786435723138510 ) ;
#6524=EDGE_LOOP ( 'NONE', ( #20313, #22871, #1858, #5359 ) ) ;
#6532=EDGE_CURVE ( 'NONE', #23680, #6666, #10711, .T. ) ;
#6533=CARTESIAN_POINT ( 'NONE',  ( -9.156249394959706578, 53.90509764945129945, 8.027840202794124025 ) ) ;
#6535=DIRECTION ( 'NONE',  ( 1.000000000000000000, -6.938893903907226837E-18, 1.734723475976806709E-18 ) ) ;
#6536=EDGE_CURVE ( 'NONE', #4951, #19079, #15280, .T. ) ;
#6537=ORIENTED_EDGE ( 'NONE', *, *, #7073, .F. ) ;
#6543=CARTESIAN_POINT ( 'NONE',  ( -6.588769196390762417, 44.25609997968906839, -26.02756986588556742 ) ) ;
#6545=VERTEX_POINT ( 'NONE', #23954 ) ;
#6547=CARTESIAN_POINT ( 'NONE',  ( -1.619063947482194177, 25.20140673341374438, -38.92136151114915066 ) ) ;
#6550=VERTEX_POINT ( 'NONE', #4214 ) ;
#6558=CARTESIAN_POINT ( 'NONE',  ( -1.019300379054419725, 42.90269154183429379, -16.06793277092006988 ) ) ;
#6559=FACE_OUTER_BOUND ( 'NONE', #16555, .T. ) ;
#6561=CARTESIAN_POINT ( 'NONE',  ( -55.24390624410018802, -0.009209468562450790971, 0.004896917417127758312 ) ) ;
#6565=EDGE_CURVE ( 'NONE', #2087, #26529, #3152, .T. ) ;
#6568=EDGE_CURVE ( 'NONE', #27740, #5273, #23772, .T. ) ;
#6570=FACE_OUTER_BOUND ( 'NONE', #22624, .T. ) ;
#6573=ADVANCED_FACE ( 'NONE', ( #24531 ), #5732, .F. ) ;
#6583=B_SPLINE_CURVE_WITH_KNOTS ( 'NONE', 3,
 ( #24324, #17683, #4585, #24622, #19566, #15233, #17399, #2418 ),
 .UNSPECIFIED., .F., .F.,
 ( 4, 2, 2, 4 ),
 ( 0.000000000000000000, 0.002761524886576653681, 0.005523049773153307362, 0.01104609954630661472 ),
 .UNSPECIFIED. ) ;
#6586=CARTESIAN_POINT ( 'NONE',  ( -6.588769196390763305, 26.02756986588603993, 44.25609997968876996 ) ) ;
#6591=CIRCLE ( 'NONE', #26788, 37.50000000000001421 ) ;
#6593=DIRECTION ( 'NONE',  ( 0.7637818620346800147, -0.6451161201712182214, -0.02150485345384170119 ) ) ;
#6597=CARTESIAN_POINT ( 'NONE',  ( -25.21435515916043357, -25.00736669481038987, -23.92354251275926558 ) ) ;
#6598=CARTESIAN_POINT ( 'NONE',  ( -28.13707043255157103, 6.342158660427001493, -22.00298671236742010 ) ) ;
#6601=FACE_OUTER_BOUND ( 'NONE', #16229, .T. ) ;
#6614=ORIENTED_EDGE ( 'NONE', *, *, #21785, .F. ) ;
#6618=CARTESIAN_POINT ( 'NONE',  ( -8.786685647604885574, 6.617461520090397715E-15, -53.53553390275978785 ) ) ;
#6621=DIRECTION ( 'NONE',  ( -0.7637818620346800147, -0.3617919495470753866, 0.5345501402766286159 ) ) ;
#6624=CARTESIAN_POINT ( 'NONE',  ( -55.24728320129491266, -0.0006547948648734058493, -0.01453410071985278100 ) ) ;
#6625=CARTESIAN_POINT ( 'NONE',  ( -1.048171036023496594, -36.44209502233728415, -27.73816396939552931 ) ) ;
#6631=B_SPLINE_CURVE_WITH_KNOTS ( 'NONE', 3,
 ( #27568, #21379, #7884, #3532, #1234, #18944, #1373, #1654, #19087, #25439 ),
 .UNSPECIFIED., .F., .F.,
 ( 4, 2, 2, 2, 4 ),
 ( 8.420559318810145779E-18, 0.0003346267210630978796, 0.0006692534421261874108, 0.001003880163189276942, 0.001338506884252366365 ),
 .UNSPECIFIED. ) ;
#6633=VERTEX_POINT ( 'NONE', #11548 ) ;
#6634=VERTEX_POINT ( 'NONE', #37 ) ;
#6635=ORIENTED_EDGE ( 'NONE', *, *, #4637, .T. ) ;
#6652=B_SPLINE_CURVE_WITH_KNOTS ( 'NONE', 3,
 ( #23961, #6681, #4363, #15284, #4494, #21923, #1912, #15137 ),
 .UNSPECIFIED., .F., .F.,
 ( 4, 2, 2, 4 ),
 ( 2.223105199230524488E-16, 0.002761568181852866802, 0.005523136363705516763, 0.01104627272741080628 ),
 .UNSPECIFIED. ) ;
#6656=CARTESIAN_POINT ( 'NONE',  ( -55.24390624410018802, 0.001811362924359719581, 0.01027195578987765215 ) ) ;
#6666=VERTEX_POINT ( 'NONE', #17867 ) ;
#6668=ORIENTED_EDGE ( 'NONE', *, *, #10400, .T. ) ;
#6669=CARTESIAN_POINT ( 'NONE',  ( -20.24419206586951603, -1.282847120831435594, -29.61012937815439372 ) ) ;
#6671=EDGE_CURVE ( 'NONE', #25959, #14622, #21021, .T. ) ;
#6681=CARTESIAN_POINT ( 'NONE',  ( -2.265401668238144151, 36.42007794497294526, 29.73100299756526965 ) ) ;
#6683=CARTESIAN_POINT ( 'NONE',  ( -1.048172774974298616, 27.73787987941060607, 36.44231470008685392 ) ) ;
#6687=ORIENTED_EDGE ( 'NONE', *, *, #21067, .T. ) ;
#6689=CARTESIAN_POINT ( 'NONE',  ( -4.178947244162641184, -47.46809051147732106, -11.88256963646720266 ) ) ;
#6696=ORIENTED_EDGE ( 'NONE', *, *, #16505, .T. ) ;
#6710=CARTESIAN_POINT ( 'NONE',  ( -20.37983603106073716, 27.81368274044725553, 10.62371319148611981 ) ) ;
#6715=CARTESIAN_POINT ( 'NONE',  ( -1.239374126674604337, 38.61989855450939046, -25.08410696974256027 ) ) ;
#6718=CARTESIAN_POINT ( 'NONE',  ( -28.41354790283022069, 18.00456980371921034, 14.62505768302780851 ) ) ;
#6723=CARTESIAN_POINT ( 'NONE',  ( -7.078251931573400491, 47.71415099571833451, 20.86696228105175166 ) ) ;
#6740=ORIENTED_EDGE ( 'NONE', *, *, #26003, .F. ) ;
#6756=CARTESIAN_POINT ( 'NONE',  ( -20.24419206586952313, -29.61012937815440083, 1.282847120831551280 ) ) ;
#6758=CARTESIAN_POINT ( 'NONE',  ( -55.24728320129491266, -0.005114031043466088153, -0.01362040845703062046 ) ) ;
#6761=CARTESIAN_POINT ( 'NONE',  ( -1.619063947482197729, -46.30105812165550105, -2.489035965909997206 ) ) ;
#6762=CARTESIAN_POINT ( 'NONE',  ( -12.82751273423880711, 33.78816682541337002, 35.32125660155409008 ) ) ;
#6763=ORIENTED_EDGE ( 'NONE', *, *, #25225, .T. ) ;
#6765=CARTESIAN_POINT ( 'NONE',  ( -4.473127245936434626, -49.22197550883367256, 3.196405119334318812 ) ) ;
#6769=DIRECTION ( 'NONE',  ( -0.7563875759206388771, -0.5490129373055306905, -0.3556158456312839555 ) ) ;
#6771=EDGE_CURVE ( 'NONE', #14914, #15111, #1452, .T. ) ;
#6780=B_SPLINE_CURVE_WITH_KNOTS ( 'NONE', 3,
 ( #22843, #2968, #16049, #27122, #25275, #9579 ),
 .UNSPECIFIED., .F., .F.,
 ( 4, 2, 4 ),
 ( 7.757919228897728493E-18, 0.003570751334075633956, 0.007141502668151267913 ),
 .UNSPECIFIED. ) ;
#6781=CARTESIAN_POINT ( 'NONE',  ( -1.031422197589711764, -43.06660437151319343, -15.60268798220621100 ) ) ;
#6785=CARTESIAN_POINT ( 'NONE',  ( -21.81686047589431965, -33.92779429964186733, 18.24499610240074432 ) ) ;
#6800=CARTESIAN_POINT ( 'NONE',  ( -1.619063947482197729, -43.26576862488445130, -16.67502769180545386 ) ) ;
#6801=CARTESIAN_POINT ( 'NONE',  ( -16.86833981943427929, -5.948101187261880085, -43.82216161736206317 ) ) ;
#6805=CARTESIAN_POINT ( 'NONE',  ( -1.045287976400365970, 1.530335034933814731, -45.76855895860946788 ) ) ;
#6814=EDGE_LOOP ( 'NONE', ( #10293, #5444, #4234, #3928 ) ) ;
#6824=AXIS2_PLACEMENT_3D ( 'NONE', #4875, #27016, #3011 ) ;
#6826=ORIENTED_EDGE ( 'NONE', *, *, #26191, .T. ) ;
#6829=CARTESIAN_POINT ( 'NONE',  ( -1.056502255334264895, -0.5104472526223093887, -45.80535052436396626 ) ) ;
#6834=CARTESIAN_POINT ( 'NONE',  ( -1.019300379054419725, -16.06793277092022976, -42.90269154183422984 ) ) ;
#6835=ORIENTED_EDGE ( 'NONE', *, *, #14180, .F. ) ;
#6836=CARTESIAN_POINT ( 'NONE',  ( -25.21435515916025594, 1.749597353048488237E-16, -4.373993382621220594E-17 ) ) ;
#6838=ORIENTED_EDGE ( 'NONE', *, *, #4532, .F. ) ;
#6839=ORIENTED_EDGE ( 'NONE', *, *, #24229, .F. ) ;
#6846=CARTESIAN_POINT ( 'NONE',  ( -20.20700224038492721, -28.44216453106531617, 8.199606986804630182 ) ) ;
#6849=CARTESIAN_POINT ( 'NONE',  ( -1.031422197589711987, 25.67058493451442658, -37.93675465142480618 ) ) ;
#6858=CARTESIAN_POINT ( 'NONE',  ( -20.21097721650785672, -29.61001326827676294, 0.3305964462500739498 ) ) ;
#6861=ADVANCED_FACE ( 'NONE', ( #27942 ), #8658, .F. ) ;
#6862=ORIENTED_EDGE ( 'NONE', *, *, #19991, .F. ) ;
#6863=CARTESIAN_POINT ( 'NONE',  ( -1.463510566862830986, 16.57250862017420090, -43.13857742234511505 ) ) ;
#6871=CARTESIAN_POINT ( 'NONE',  ( -1.323439229708142983, -35.86372896917450959, 28.92147054731879408 ) ) ;
#6878=CARTESIAN_POINT ( 'NONE',  ( 0.000000000000000000, 0.000000000000000000, 0.000000000000000000 ) ) ;
#6879=CARTESIAN_POINT ( 'NONE',  ( -20.57838717382308502, 28.96176188950218844, -7.715628353033780584 ) ) ;
#6887=FACE_OUTER_BOUND ( 'NONE', #27848, .T. ) ;
#6888=CARTESIAN_POINT ( 'NONE',  ( -25.21435515916025594, 1.749597353048488237E-16, -4.373993382621220594E-17 ) ) ;
#6891=EDGE_CURVE ( 'NONE', #5205, #5134, #21374, .T. ) ;
#6906=CARTESIAN_POINT ( 'NONE',  ( -9.156249394959713683, -53.90509764945124971, 8.027840202794504165 ) ) ;
#6914=B_SPLINE_CURVE_WITH_KNOTS ( 'NONE', 3,
 ( #5549, #9881, #14035, #25278, #11748, #11884, #22847, #18343, #18647, #13745 ),
 .UNSPECIFIED., .F., .F.,
 ( 4, 2, 2, 2, 4 ),
 ( 2.947001115474787729E-16, 0.0003346187017559134843, 0.0006692374035115322825, 0.001003856105267151135, 0.001338474807022769879 ),
 .UNSPECIFIED. ) ;
#6925=CARTESIAN_POINT ( 'NONE',  ( -55.25719721206881729, 0.0006290797159209853082, -0.01115102788683027674 ) ) ;
#6934=CARTESIAN_POINT ( 'NONE',  ( -4.780792508754322157, 49.38761389561003767, 3.764354093953751423 ) ) ;
#6935=CARTESIAN_POINT ( 'NONE',  ( -55.25719721206881729, -0.01115102788683311301, 0.0006290797159230496292 ) ) ;
#6940=CARTESIAN_POINT ( 'NONE',  ( -55.24390624410018802, 0.009209468562452933355, 0.004896917417131438528 ) ) ;
#6942=ADVANCED_FACE ( 'NONE', ( #17558 ), #19501, .F. ) ;
#6943=CARTESIAN_POINT ( 'NONE',  ( -8.786685647604890903, -48.22796981442753150, 23.24040270374441874 ) ) ;
#6949=VERTEX_POINT ( 'NONE', #4606 ) ;
#6952=VECTOR ( 'NONE', #21345, 1000.000000000000000 ) ;
#6956=ORIENTED_EDGE ( 'NONE', *, *, #1604, .F. ) ;
#6964=CARTESIAN_POINT ( 'NONE',  ( -20.47566262905009893, -28.85746289809572218, 7.708089517695493775 ) ) ;
#6976=CARTESIAN_POINT ( 'NONE',  ( -1.031422197589711764, 1.530725436377463389, -45.78027046666443312 ) ) ;
#6977=CARTESIAN_POINT ( 'NONE',  ( -8.259864102781671491, -52.06232470801718648, -9.986657004933428894 ) ) ;
#6983=CARTESIAN_POINT ( 'NONE',  ( -28.13707043255157103, -18.96624908365855688, -12.83104814250447134 ) ) ;
#6988=ORIENTED_EDGE ( 'NONE', *, *, #17276, .T. ) ;
#6990=CARTESIAN_POINT ( 'NONE',  ( 0.000000000000000000, 0.000000000000000000, 0.000000000000000000 ) ) ;
#6993=VERTEX_POINT ( 'NONE', #13375 ) ;
#6998=CARTESIAN_POINT ( 'NONE',  ( -55.24390624410018802, -0.01032895241566962087, 0.001451500391950532459 ) ) ;
#7005=CARTESIAN_POINT ( 'NONE',  ( -1.464342487929859660, -2.431462367721655138, -46.14921266389555399 ) ) ;
#7006=EDGE_CURVE ( 'NONE', #12820, #20942, #7220, .T. ) ;
#7014=CARTESIAN_POINT ( 'NONE',  ( -20.57838717382308147, -28.96176188950213870, 7.715628353033985753 ) ) ;
#7016=CARTESIAN_POINT ( 'NONE',  ( -1.259920593601974392, 45.95412615877143026, 2.243284667987943681 ) ) ;
#7018=ORIENTED_EDGE ( 'NONE', *, *, #17194, .F. ) ;
#7019=CARTESIAN_POINT ( 'NONE',  ( -24.53237795827023859, -33.71192251888856362, 3.868415699416008380 ) ) ;
#7028=B_SPLINE_CURVE_WITH_KNOTS ( 'NONE', 3,
 ( #22548, #8420, #12579, #10022, #28117, #3810, #5702, #27851, #8017, #14742 ),
 .UNSPECIFIED., .F., .F.,
 ( 4, 2, 2, 2, 4 ),
 ( 0.000000000000000000, 0.0003346267210630921333, 0.0006692534421261842666, 0.001003880163189276292, 0.001338506884252368533 ),
 .UNSPECIFIED. ) ;
#7036=CARTESIAN_POINT ( 'NONE',  ( -1.239374126674604337, -25.08410696974215170, 38.61989855450968179 ) ) ;
#7037=CARTESIAN_POINT ( 'NONE',  ( -20.57838717382308147, -1.611677988432568709, -29.92853265176830746 ) ) ;
#7038=EDGE_CURVE ( 'NONE', #7707, #22719, #13958, .T. ) ;
#7039=VERTEX_POINT ( 'NONE', #14390 ) ;
#7040=CARTESIAN_POINT ( 'NONE',  ( -20.57838717382308147, 1.611677988432361097, -29.92853265176831812 ) ) ;
#7047=CARTESIAN_POINT ( 'NONE',  ( -1.583189561560252701, -38.94740041318275559, 25.21827308671274182 ) ) ;
#7051=CARTESIAN_POINT ( 'NONE',  ( -4.162674018437154899, -48.79210541969629844, -3.424137510344775759 ) ) ;
#7052=CARTESIAN_POINT ( 'NONE',  ( -22.34422965417124374, 26.20925041532892763, 27.39717383755251490 ) ) ;
#7066=VERTEX_POINT ( 'NONE', #15975 ) ;
#7068=VERTEX_POINT ( 'NONE', #23054 ) ;
#7069=CARTESIAN_POINT ( 'NONE',  ( -1.031422197589716205, 45.78027046666444733, -1.530725436377611715 ) ) ;
#7070=DIRECTION ( 'NONE',  ( 0.000000000000000000, -5.223019709708233256E-21, 1.000000000000000000 ) ) ;
#7073=EDGE_CURVE ( 'NONE', #27143, #17730, #28319, .T. ) ;
#7075=ORIENTED_EDGE ( 'NONE', *, *, #5496, .F. ) ;
#7080=ORIENTED_EDGE ( 'NONE', *, *, #6671, .F. ) ;
#7081=CARTESIAN_POINT ( 'NONE',  ( -8.786685647604885574, 6.096987947571466530E-17, -1.524246986892866633E-17 ) ) ;
#7082=ORIENTED_EDGE ( 'NONE', *, *, #26677, .F. ) ;
#7085=CARTESIAN_POINT ( 'NONE',  ( -20.57838717382308147, 28.96176188950229502, 7.715628353033378239 ) ) ;
#7088=CARTESIAN_POINT ( 'NONE',  ( -18.41936578851712625, -30.66520733838672186, -29.33493038358061966 ) ) ;
#7095=DIRECTION ( 'NONE',  ( 1.000000000000000000, -6.938893903907226837E-18, 1.734723475976806709E-18 ) ) ;
#7096=EDGE_LOOP ( 'NONE', ( #1395, #6405, #18046, #26539 ) ) ;
#7101=EDGE_LOOP ( 'NONE', ( #8786, #20057, #11537, #14137 ) ) ;
#7104=B_SPLINE_CURVE_WITH_KNOTS ( 'NONE', 3,
 ( #27382, #9546, #5509, #18752, #16304, #13995, #27233, #7547, #22663, #14131 ),
 .UNSPECIFIED., .F., .F.,
 ( 4, 2, 2, 2, 4 ),
 ( 8.673617379884035472E-19, 0.0003346267210630925128, 0.0006692534421261841582, 0.001003880163189275858, 0.001338506884252367449 ),
 .UNSPECIFIED. ) ;
#7105=EDGE_CURVE ( 'NONE', #3326, #17470, #11666, .T. ) ;
#7108=EDGE_CURVE ( 'NONE', #2726, #21682, #24943, .T. ) ;
#7112=CARTESIAN_POINT ( 'NONE',  ( -55.24271866751342941, -0.004256484107792932181, -0.008488649505346277865 ) ) ;
#7120=CARTESIAN_POINT ( 'NONE',  ( -1.031422197589711764, 25.67058493451497725, 37.93675465142443670 ) ) ;
#7122=CARTESIAN_POINT ( 'NONE',  ( -1.619063947482197729, -44.80407745103793360, -11.94059994246142331 ) ) ;
#7126=CARTESIAN_POINT ( 'NONE',  ( -4.162674018437137136, -11.82104147411594752, -47.46216648493552981 ) ) ;
#7139=ORIENTED_EDGE ( 'NONE', *, *, #18379, .F. ) ;
#7145=CARTESIAN_POINT ( 'NONE',  ( -2.911734481061406754, 44.38410240830302911, -17.36785190845994720 ) ) ;
#7146=CARTESIAN_POINT ( 'NONE',  ( -5.986830583229477476, 11.27873876172141365, -49.46736940480261779 ) ) ;
#7150=CARTESIAN_POINT ( 'NONE',  ( -25.21435515916043357, 31.17620025257608418, 15.02493970636113474 ) ) ;
#7154=CARTESIAN_POINT ( 'NONE',  ( -22.34422965417125795, -37.57019010019543970, 5.100074259622997097 ) ) ;
#7157=CARTESIAN_POINT ( 'NONE',  ( -28.13707043255157103, 22.00298671236748760, 6.342158660426773231 ) ) ;
#7173=CARTESIAN_POINT ( 'NONE',  ( 60.46576798286869803, 12.50000000000000000, 1.596046867330078713E-15 ) ) ;
#7179=CARTESIAN_POINT ( 'NONE',  ( -4.473127245936434626, 18.25038884639934977, 45.82513704981523972 ) ) ;
#7187=CARTESIAN_POINT ( 'NONE',  ( -9.156249394959713683, -53.74753343182709386, -9.022661520477562647 ) ) ;
#7189=CARTESIAN_POINT ( 'NONE',  ( -55.24728320129491266, -0.01214321324517104832, 0.008013189884951824049 ) ) ;
#7190=CARTESIAN_POINT ( 'NONE',  ( -5.986830583229376224, -38.20088153919473939, 33.39046620690945844 ) ) ;
#7191=CARTESIAN_POINT ( 'NONE',  ( -8.786685647604887350, 53.04920435127183254, -7.199674155859138835 ) ) ;
#7196=CARTESIAN_POINT ( 'NONE',  ( -1.045287976400351981, -15.59869763335126436, -43.05558670614231431 ) ) ;
#7198=CARTESIAN_POINT ( 'NONE',  ( -10.86508079875781974, 22.20099862734820562, -46.07061504567093380 ) ) ;
#7201=ORIENTED_EDGE ( 'NONE', *, *, #7415, .T. ) ;
#7206=CARTESIAN_POINT ( 'NONE',  ( -20.20612092514784663, 18.30568145913877132, 23.26073121129616439 ) ) ;
#7215=CARTESIAN_POINT ( 'NONE',  ( -20.90916690077959927, 17.17795951644708907, 35.64494649500667833 ) ) ;
#7217=VERTEX_POINT ( 'NONE', #15079 ) ;
#7220=LINE ( 'NONE', #13814, #25002 ) ;
#7222=ORIENTED_EDGE ( 'NONE', *, *, #24229, .T. ) ;
#7225=CARTESIAN_POINT ( 'NONE',  ( -1.056502255334264895, 43.72121397317241787, 13.66916755949804951 ) ) ;
#7229=VERTEX_POINT ( 'NONE', #23899 ) ;
#7230=CARTESIAN_POINT ( 'NONE',  ( -55.24271866751342941, 0.001545935011627245191, 0.009369360294294363373 ) ) ;
#7231=CARTESIAN_POINT ( 'NONE',  ( -8.786685647604887350, -38.68584556812326980, -37.00619870957918778 ) ) ;
#7234=FACE_OUTER_BOUND ( 'NONE', #22087, .T. ) ;
#7243=FACE_OUTER_BOUND ( 'NONE', #895, .T. ) ;
#7255=CARTESIAN_POINT ( 'NONE',  ( -25.21435515916043713, 16.39063784838786475, 30.48034229288620622 ) ) ;
#7257=EDGE_CURVE ( 'NONE', #17694, #1086, #21147, .T. ) ;
#7266=CARTESIAN_POINT ( 'NONE',  ( -4.178947244162639407, -18.28784278438482858, -45.38689110596713050 ) ) ;
#7270=B_SPLINE_CURVE_WITH_KNOTS ( 'NONE', 3,
 ( #20013, #22333, #24788, #27047, #6934, #11819, #9384, #22777 ),
 .UNSPECIFIED., .F., .F.,
 ( 4, 2, 2, 4 ),
 ( 2.324173423859648542E-16, 0.002761568181852869838, 0.005523136363705506355, 0.01104627272741078026 ),
 .UNSPECIFIED. ) ;
#7279=CARTESIAN_POINT ( 'NONE',  ( -1.049819078601898381, 0.5100232645225435402, 45.79653735114490587 ) ) ;
#7286=CARTESIAN_POINT ( 'NONE',  ( -28.13707043255157103, -12.83104814250440029, 18.96624908365860662 ) ) ;
#7290=ORIENTED_EDGE ( 'NONE', *, *, #19177, .F. ) ;
#7299=VECTOR ( 'NONE', #23315, 1000.000000000000000 ) ;
#7301=CARTESIAN_POINT ( 'NONE',  ( -1.113427685307000203, 1.967672929087815881, 45.82016658690749722 ) ) ;
#7305=ORIENTED_EDGE ( 'NONE', *, *, #1604, .T. ) ;
#7311=CARTESIAN_POINT ( 'NONE',  ( -20.24419206586954090, -10.37009329716784656, -27.76448493191440292 ) ) ;
#7319=ORIENTED_EDGE ( 'NONE', *, *, #12036, .F. ) ;
#7320=ORIENTED_EDGE ( 'NONE', *, *, #2514, .F. ) ;
#7326=CARTESIAN_POINT ( 'NONE',  ( -23.77929240705205771, -26.20227034809537514, 25.06639637888449457 ) ) ;
#7332=FACE_BOUND ( 'NONE', #8262, .T. ) ;
#7335=B_SPLINE_CURVE_WITH_KNOTS ( 'NONE', 3,
 ( #6879, #9036, #9602, #532, #15931, #22282 ),
 .UNSPECIFIED., .F., .F.,
 ( 4, 2, 4 ),
 ( 4.982613841084487634E-18, 0.0004335151646191476174, 0.0008670303292382917654 ),
 .UNSPECIFIED. ) ;
#7340=ORIENTED_EDGE ( 'NONE', *, *, #28413, .F. ) ;
#7347=CARTESIAN_POINT ( 'NONE',  ( -16.86833981943423311, 19.19877306373907189, 39.83928801320569590 ) ) ;
#7350=CARTESIAN_POINT ( 'NONE',  ( -20.20700224038492721, -24.51628800869035274, 16.58740185276737122 ) ) ;
#7352=CARTESIAN_POINT ( 'NONE',  ( -1.113548883309553927, -45.82026503946952545, -1.968251867498708174 ) ) ;
#7356=CARTESIAN_POINT ( 'NONE',  ( -22.23226125620929139, 30.68305173820436593, 7.677408153693709991 ) ) ;
#7358=CARTESIAN_POINT ( 'NONE',  ( -55.24198130335446422, -0.009190321388308575826, -0.001391250620105316613 ) ) ;
#7361=CARTESIAN_POINT ( 'NONE',  ( -1.113548883309547710, 1.968251867498868934, -45.82026503946952545 ) ) ;
#7366=EDGE_CURVE ( 'NONE', #8780, #26877, #2952, .T. ) ;
#7374=ORIENTED_EDGE ( 'NONE', *, *, #7006, .F. ) ;
#7379=CARTESIAN_POINT ( 'NONE',  ( -12.94347594948475333, -48.30328466416771960, -6.555928820869143969 ) ) ;
#7380=CARTESIAN_POINT ( 'NONE',  ( -22.23226125620943705, -24.24619897613461461, 20.31044300692198945 ) ) ;
#7394=VECTOR ( 'NONE', #22123, 1000.000000000000000 ) ;
#7396=CARTESIAN_POINT ( 'NONE',  ( -1.045287976400379737, -37.92705037016725100, 25.66401692420055269 ) ) ;
#7397=CARTESIAN_POINT ( 'NONE',  ( -1.583189561560253589, 11.94859433442901597, -44.83405390829675952 ) ) ;
#7400=DIRECTION ( 'NONE',  ( -0.7637818620346800147, 0.5345501402766299481, 0.3617919495470734992 ) ) ;
#7405=ORIENTED_EDGE ( 'NONE', *, *, #11738, .T. ) ;
#7412=AXIS2_PLACEMENT_3D ( 'NONE', #19663, #4408, #6305 ) ;
#7415=EDGE_CURVE ( 'NONE', #24730, #15769, #12533, .T. ) ;
#7420=CARTESIAN_POINT ( 'NONE',  ( -6.574463467970643293, 11.01561683920051848, -50.12924290857540655 ) ) ;
#7431=CARTESIAN_POINT ( 'NONE',  ( -10.86508079875782684, -9.118642906269649018, -50.32133009257454859 ) ) ;
#7433=CARTESIAN_POINT ( 'NONE',  ( -12.82751273423877869, -48.43568301531143305, 6.573887447703340214 ) ) ;
#7439=B_SPLINE_CURVE_WITH_KNOTS ( 'NONE', 3,
 ( #18720, #5479, #12376, #5630, #14396, #8090, #1586, #27920, #3463, #21159 ),
 .UNSPECIFIED., .F., .F.,
 ( 4, 2, 2, 2, 4 ),
 ( 4.336808689942017255E-19, 0.0003346267210630946812, 0.0006692534421261889287, 0.001003880163189283230, 0.001338506884252377424 ),
 .UNSPECIFIED. ) ;
#7446=( BOUNDED_SURFACE ( )  B_SPLINE_SURFACE ( 3, 1, ( 
 ( #5329, #22918 ),
 ( #27347, #18579 ),
 ( #7660, #14394 ),
 ( #23204, #2262 ) ),
 .UNSPECIFIED., .F., .F., .F. ) 
 B_SPLINE_SURFACE_WITH_KNOTS ( ( 4, 4 ),
 ( 2, 2 ),
 ( 0.000000000000000000, 1.000000000000000000 ),
 ( 0.000000000000000000, 1.000000000000000000 ),
 .UNSPECIFIED. ) 
 GEOMETRIC_REPRESENTATION_ITEM ( )  RATIONAL_B_SPLINE_SURFACE ( (
 ( 1.000000000000000000, 1.000000000000000000),
 ( 0.7789835883360578528, 0.9689951854195403280),
 ( 0.7789835883360578528, 0.9689951854195403280),
 ( 1.000000000000000000, 1.000000000000000000) ) ) 
 REPRESENTATION_ITEM ( '' )  SURFACE ( )  );
#7447=CARTESIAN_POINT ( 'NONE',  ( -1.044556982611280160, 1.643392503293353180, 45.76404732357876526 ) ) ;
#7449=CARTESIAN_POINT ( 'NONE',  ( -55.24728320129491266, -0.009072670231974808847, -0.01137345571546840607 ) ) ;
#7453=EDGE_CURVE ( 'NONE', #18004, #24730, #10503, .T. ) ;
#7454=EDGE_LOOP ( 'NONE', ( #19689, #5268 ) ) ;
#7468=EDGE_LOOP ( 'NONE', ( #22644, #11388, #17350, #9395 ) ) ;
#7469=CARTESIAN_POINT ( 'NONE',  ( -1.045287976400383290, 36.12803364096649972, 28.14015102489766917 ) ) ;
#7475=CARTESIAN_POINT ( 'NONE',  ( -22.34422965417126861, 34.15536449444089584, -16.46028608106120572 ) ) ;
#7479=CARTESIAN_POINT ( 'NONE',  ( -55.24300891470650754, 0.003362556190412917256, 0.009225237711101274066 ) ) ;
#7484=ORIENTED_EDGE ( 'NONE', *, *, #8972, .F. ) ;
#7487=CARTESIAN_POINT ( 'NONE',  ( -20.47566262905010248, 16.24827521404687403, 25.06314747784817243 ) ) ;
#7490=ORIENTED_EDGE ( 'NONE', *, *, #28235, .F. ) ;
#7492=VERTEX_POINT ( 'NONE', #12472 ) ;
#7493=AXIS2_PLACEMENT_3D ( 'NONE', #6888, #19974, #4996 ) ;
#7502=CARTESIAN_POINT ( 'NONE',  ( -7.733045908741333463, 51.44704017882777691, -10.42750254442556290 ) ) ;
#7503=ORIENTED_EDGE ( 'NONE', *, *, #20827, .F. ) ;
#7504=CARTESIAN_POINT ( 'NONE',  ( -20.20700224038492721, -28.44216453106542986, -8.199606986804219844 ) ) ;
#7508=VERTEX_POINT ( 'NONE', #1670 ) ;
#7509=VERTEX_POINT ( 'NONE', #20965 ) ;
#7527=B_SPLINE_CURVE_WITH_KNOTS ( 'NONE', 3,
 ( #985, #14072, #25174, #5298, #9776, #27312 ),
 .UNSPECIFIED., .F., .F.,
 ( 4, 2, 4 ),
 ( 0.000000000000000000, 0.0004335184443140231063, 0.0008670368886280462126 ),
 .UNSPECIFIED. ) ;
#7528=VERTEX_POINT ( 'NONE', #16815 ) ;
#7530=EDGE_CURVE ( 'NONE', #8780, #28137, #9245, .T. ) ;
#7546=CARTESIAN_POINT ( 'NONE',  ( -20.57838717382308147, -10.78122205916981358, 27.96569011373096814 ) ) ;
#7547=CARTESIAN_POINT ( 'NONE',  ( -1.058473599757816963, -25.48501014712370960, 38.06357893967457784 ) ) ;
#7556=ORIENTED_EDGE ( 'NONE', *, *, #1050, .F. ) ;
#7568=DIRECTION ( 'NONE',  ( 1.000000000000000000, -6.938893903907226837E-18, 1.734723475976806709E-18 ) ) ;
#7575=CARTESIAN_POINT ( 'NONE',  ( -20.20700224038492721, 16.58740185276746359, 24.51628800869029234 ) ) ;
#7578=CARTESIAN_POINT ( 'NONE',  ( -20.57838717382308147, 10.78122205917039977, 27.96569011373074076 ) ) ;
#7581=CARTESIAN_POINT ( 'NONE',  ( -55.24300891470648622, -0.005486913146696059326, -0.008142823778062177609 ) ) ;
#7599=CARTESIAN_POINT ( 'NONE',  ( -55.24390624410018802, -0.01027195578987978239, -0.001811362924362686826 ) ) ;
#7602=CARTESIAN_POINT ( 'NONE',  ( -1.155001620486252101, -42.97366440495923001, -16.13799328198405902 ) ) ;
#7607=CARTESIAN_POINT ( 'NONE',  ( -1.046936909428682894, 15.35929614323726256, 43.14407378092978718 ) ) ;
#7613=LINE ( 'NONE', #16812, #13456 ) ;
#7614=CARTESIAN_POINT ( 'NONE',  ( -20.20700224038492721, 10.08426345511588984, -27.82980252387822517 ) ) ;
#7616=CARTESIAN_POINT ( 'NONE',  ( -21.41427618760458529, 25.94789270595506991, -16.60878262545428541 ) ) ;
#7627=CARTESIAN_POINT ( 'NONE',  ( -22.34422965417126505, -33.39267070835835227, -17.95715691811035342 ) ) ;
#7631=( BOUNDED_SURFACE ( )  B_SPLINE_SURFACE ( 3, 1, ( 
 ( #16276, #5785 ),
 ( #14543, #23348 ),
 ( #28332, #8219 ),
 ( #21871, #19425 ) ),
 .UNSPECIFIED., .F., .F., .F. ) 
 B_SPLINE_SURFACE_WITH_KNOTS ( ( 4, 4 ),
 ( 2, 2 ),
 ( 0.000000000000000000, 1.000000000000000000 ),
 ( 0.000000000000000000, 1.000000000000000000 ),
 .UNSPECIFIED. ) 
 GEOMETRIC_REPRESENTATION_ITEM ( )  RATIONAL_B_SPLINE_SURFACE ( (
 ( 1.000000000000000000, 1.000000000000000000),
 ( 0.7789835883360576307, 0.9689951854195403280),
 ( 0.7789835883360576307, 0.9689951854195403280),
 ( 1.000000000000000000, 1.000000000000000000) ) ) 
 REPRESENTATION_ITEM ( '' )  SURFACE ( )  );
#7637=CARTESIAN_POINT ( 'NONE',  ( -20.57838717382308502, 28.96176188950218844, -7.715628353033780584 ) ) ;
#7643=ADVANCED_FACE ( 'NONE', ( #26417 ), #2424, .F. ) ;
#7645=B_SPLINE_CURVE_WITH_KNOTS ( 'NONE', 3,
 ( #12493, #19390, #3992, #28026, #21695, #6182 ),
 .UNSPECIFIED., .F., .F.,
 ( 4, 2, 4 ),
 ( 6.505213034913026604E-19, 0.0004335151646191473464, 0.0008670303292382940423 ),
 .UNSPECIFIED. ) ;
#7658=VERTEX_POINT ( 'NONE', #13459 ) ;
#7659=CARTESIAN_POINT ( 'NONE',  ( -8.786685647604890903, -48.22796981442785835, -23.24040270374372952 ) ) ;
#7660=CARTESIAN_POINT ( 'NONE',  ( -55.24728320129491266, 0.01362040845703093098, -0.005114031043466513160 ) ) ;
#7664=CARTESIAN_POINT ( 'NONE',  ( -1.044557008772713402, 1.643388457097889166, -45.76404748504490527 ) ) ;
#7671=EDGE_CURVE ( 'NONE', #9135, #5379, #24880, .T. ) ;
#7675=EDGE_CURVE ( 'NONE', #9661, #1788, #143, .T. ) ;
#7676=CARTESIAN_POINT ( 'NONE',  ( -1.044556982611268170, -28.22896456560694034, -36.05793013899088351 ) ) ;
#7683=DIRECTION ( 'NONE',  ( 1.000000000000000000, -6.938893903907226837E-18, 1.734723475976806709E-18 ) ) ;
#7702=CARTESIAN_POINT ( 'NONE',  ( -1.044556982611269502, 25.56989963842203650, -37.98985389331818396 ) ) ;
#7707=VERTEX_POINT ( 'NONE', #16332 ) ;
#7710=VERTEX_POINT ( 'NONE', #7150 ) ;
#7712=ORIENTED_EDGE ( 'NONE', *, *, #22642, .F. ) ;
#7719=CARTESIAN_POINT ( 'NONE',  ( -1.058197053496163109, 28.32422455455077781, -36.00048521498961662 ) ) ;
#7723=CARTESIAN_POINT ( 'NONE',  ( -20.20700224038492721, -18.19058640100206503, 23.35150625415678860 ) ) ;
#7726=CARTESIAN_POINT ( 'NONE',  ( -4.780792508754331038, 11.68149851467529210, 48.13366140756546230 ) ) ;
#7732=CARTESIAN_POINT ( 'NONE',  ( -28.13707043255157103, 18.96624908365847162, -12.83104814250460990 ) ) ;
#7733=ORIENTED_EDGE ( 'NONE', *, *, #17158, .F. ) ;
#7747=VERTEX_POINT ( 'NONE', #7578 ) ;
#7750=MANIFOLD_SOLID_BREP ( 'Boss-Extrude1', #13255 ) ;
#7755=( BOUNDED_SURFACE ( )  B_SPLINE_SURFACE ( 3, 1, ( 
 ( #13860, #7397 ),
 ( #16165, #3495 ),
 ( #21200, #5819 ),
 ( #5957, #16602 ) ),
 .UNSPECIFIED., .F., .F., .F. ) 
 B_SPLINE_SURFACE_WITH_KNOTS ( ( 4, 4 ),
 ( 2, 2 ),
 ( 0.000000000000000000, 1.000000000000000000 ),
 ( 0.000000000000000000, 1.000000000000000000 ),
 .UNSPECIFIED. ) 
 GEOMETRIC_REPRESENTATION_ITEM ( )  RATIONAL_B_SPLINE_SURFACE ( (
 ( 1.000000000000000000, 1.000000000000000000),
 ( 0.7789835883360576307, 0.9689951854195403280),
 ( 0.7789835883360576307, 0.9689951854195403280),
 ( 1.000000000000000000, 1.000000000000000000) ) ) 
 REPRESENTATION_ITEM ( '' )  SURFACE ( )  );
#7758=CARTESIAN_POINT ( 'NONE',  ( -20.20612092514784663, 23.26073121129637045, -18.30568145913851907 ) ) ;
#7762=FACE_OUTER_BOUND ( 'NONE', #13726, .T. ) ;
#7763=CARTESIAN_POINT ( 'NONE',  ( -25.21435515916043002, 34.05351380035335040, -6.169479169075572145 ) ) ;
#7769=ORIENTED_EDGE ( 'NONE', *, *, #12024, .T. ) ;
#7775=CARTESIAN_POINT ( 'NONE',  ( 0.000000000000000000, 0.000000000000000000, 0.000000000000000000 ) ) ;
#7779=CARTESIAN_POINT ( 'NONE',  ( -9.156249394959706578, 38.89149400288462033, 38.17928057391947760 ) ) ;
#7782=EDGE_LOOP ( 'NONE', ( #2915, #11203, #28083, #3579 ) ) ;
#7787=VERTEX_POINT ( 'NONE', #27845 ) ;
#7788=CARTESIAN_POINT ( 'NONE',  ( -4.780792508754312387, -18.84172549606840619, 45.80716263181253822 ) ) ;
#7795=CARTESIAN_POINT ( 'NONE',  ( -55.25719721206881729, 0.006045473558784871665, -0.009391134844733287426 ) ) ;
#7796=EDGE_CURVE ( 'NONE', #7039, #12676, #5284, .T. ) ;
#7797=CARTESIAN_POINT ( 'NONE',  ( -20.47566262905009538, -27.87687924095555658, -10.72601569609885708 ) ) ;
#7812=CARTESIAN_POINT ( 'NONE',  ( -20.37983603106074071, -16.25728007463423808, -24.94323704205431369 ) ) ;
#7814=ORIENTED_EDGE ( 'NONE', *, *, #26289, .F. ) ;
#7817=CARTESIAN_POINT ( 'NONE',  ( -1.155031165708871654, -28.62780465193337420, -35.88345263711039479 ) ) ;
#7820=ORIENTED_EDGE ( 'NONE', *, *, #23817, .T. ) ;
#7822=FACE_OUTER_BOUND ( 'NONE', #8539, .T. ) ;
#7826=CARTESIAN_POINT ( 'NONE',  ( -28.13707043255157103, 18.06394523322453693, -14.07296284901339334 ) ) ;
#7829=EDGE_CURVE ( 'NONE', #8890, #28211, #4622, .T. ) ;
#7830=CARTESIAN_POINT ( 'NONE',  ( -25.21435515916025594, 1.749597353048488237E-16, -4.373993382621220594E-17 ) ) ;
#7842=CARTESIAN_POINT ( 'NONE',  ( -8.259864102781673267, -25.58601832199047266, 46.42816643551597622 ) ) ;
#7852=ORIENTED_EDGE ( 'NONE', *, *, #11184, .T. ) ;
#7859=CIRCLE ( 'NONE', #5533, 37.50000000000001421 ) ;
#7862=CONICAL_SURFACE ( 'NONE', #10157, 34.60786435723138510, 0.8559913436420825139 ) ;
#7879=( BOUNDED_SURFACE ( )  B_SPLINE_SURFACE ( 3, 1, ( 
 ( #26755, #13104 ),
 ( #19713, #11090 ),
 ( #19860, #147 ),
 ( #8941, #7069 ) ),
 .UNSPECIFIED., .F., .F., .F. ) 
 B_SPLINE_SURFACE_WITH_KNOTS ( ( 4, 4 ),
 ( 2, 2 ),
 ( 0.000000000000000000, 1.000000000000000000 ),
 ( 0.000000000000000000, 1.000000000000000000 ),
 .UNSPECIFIED. ) 
 GEOMETRIC_REPRESENTATION_ITEM ( )  RATIONAL_B_SPLINE_SURFACE ( (
 ( 1.000000000000000000, 1.000000000000000000),
 ( 0.9593753223639863714, 0.9995975284513187731),
 ( 0.9593753223639863714, 0.9995975284513187731),
 ( 1.000000000000000000, 1.000000000000000000) ) ) 
 REPRESENTATION_ITEM ( '' )  SURFACE ( )  );
#7884=CARTESIAN_POINT ( 'NONE',  ( -1.464342487929844783, -38.76467504336602588, -25.15873223207679743 ) ) ;
#7888=( GEOMETRIC_REPRESENTATION_CONTEXT ( 3 ) GLOBAL_UNCERTAINTY_ASSIGNED_CONTEXT ( ( #22940 ) ) GLOBAL_UNIT_ASSIGNED_CONTEXT ( ( #12714, #8142, #12433 ) ) REPRESENTATION_CONTEXT ( 'NONE', 'WORKASPACE' ) );
#7892=CARTESIAN_POINT ( 'NONE',  ( -1.058197053496171769, -42.99116279335166269, -15.81317659443667445 ) ) ;
#7893=CARTESIAN_POINT ( 'NONE',  ( -1.019300379054419725, 16.06793277092052818, 42.90269154183410194 ) ) ;
#7897=FACE_OUTER_BOUND ( 'NONE', #17314, .T. ) ;
#7901=ADVANCED_FACE ( 'NONE', ( #19873 ), #21936, .F. ) ;
#7911=CARTESIAN_POINT ( 'NONE',  ( -55.24390624410018802, -0.004572280736701530256, -0.009374879212970928244 ) ) ;
#7915=CIRCLE ( 'NONE', #22064, 53.53553390275978785 ) ;
#7917=CARTESIAN_POINT ( 'NONE',  ( -1.113548883309547044, -12.28732181966548609, -44.18588492042589166 ) ) ;
#7919=CARTESIAN_POINT ( 'NONE',  ( -12.82751273423883553, -43.04932478553545394, -23.15139349681293623 ) ) ;
#7927=CARTESIAN_POINT ( 'NONE',  ( -18.41936578851709783, -20.09935324538221479, -37.37524689996187277 ) ) ;
#7935=CARTESIAN_POINT ( 'NONE',  ( -1.323830074806760848, -2.318057800980394045, 46.01435746200695576 ) ) ;
#7938=( BOUNDED_SURFACE ( )  B_SPLINE_SURFACE ( 3, 1, ( 
 ( #98, #6309 ),
 ( #8891, #15343 ),
 ( #15057, #11320 ),
 ( #6445, #13185 ) ),
 .UNSPECIFIED., .F., .F., .F. ) 
 B_SPLINE_SURFACE_WITH_KNOTS ( ( 4, 4 ),
 ( 2, 2 ),
 ( 0.000000000000000000, 1.000000000000000000 ),
 ( 0.000000000000000000, 1.000000000000000000 ),
 .UNSPECIFIED. ) 
 GEOMETRIC_REPRESENTATION_ITEM ( )  RATIONAL_B_SPLINE_SURFACE ( (
 ( 1.000000000000000000, 1.000000000000000000),
 ( 0.9934239774497837239, 0.8357310067453919133),
 ( 0.9934239774497837239, 0.8357310067453919133),
 ( 1.000000000000000000, 1.000000000000000000) ) ) 
 REPRESENTATION_ITEM ( '' )  SURFACE ( )  );
#7939=DIRECTION ( 'NONE',  ( 0.7637818620346801257, 0.1788995134688915190, 0.6201872550346635427 ) ) ;
#7941=CARTESIAN_POINT ( 'NONE',  ( -20.57838717382308147, 1.611677988432361097, -29.92853265176831812 ) ) ;
#7947=CARTESIAN_POINT ( 'NONE',  ( -1.045287976400362417, -15.59869763335038506, 43.05558670614261985 ) ) ;
#7956=FACE_OUTER_BOUND ( 'NONE', #6524, .T. ) ;
#7960=CARTESIAN_POINT ( 'NONE',  ( -1.045287976400365970, -37.92705037016778391, -25.66401692419976399 ) ) ;
#7964=AXIS2_PLACEMENT_3D ( 'NONE', #16314, #16461, #25253 ) ;
#7965=EDGE_LOOP ( 'NONE', ( #14229, #28188, #18318, #4866 ) ) ;
#7979=AXIS2_PLACEMENT_3D ( 'NONE', #25617, #14364, #27467 ) ;
#7995=CARTESIAN_POINT ( 'NONE',  ( -1.323439229708136100, 25.17120723334093313, -38.58845475799776636 ) ) ;
#7999=DIRECTION ( 'NONE',  ( 0.000000000000000000, 5.223019709707975211E-21, -1.000000000000000000 ) ) ;
#8014=ORIENTED_EDGE ( 'NONE', *, *, #17510, .F. ) ;
#8017=CARTESIAN_POINT ( 'NONE',  ( -1.044556982611270612, 28.22896456560720679, 36.05793013899066324 ) ) ;
#8018=LINE ( 'NONE', #2056, #11892 ) ;
#8021=CARTESIAN_POINT ( 'NONE',  ( -20.47566338032521216, -16.24827550219808003, 25.06314818626711372 ) ) ;
#8027=ORIENTED_EDGE ( 'NONE', *, *, #12843, .T. ) ;
#8044=ORIENTED_EDGE ( 'NONE', *, *, #1982, .F. ) ;
#8053=CARTESIAN_POINT ( 'NONE',  ( -20.21097721712958517, 28.05863618200121934, 9.464413111084452268 ) ) ;
#8056=CARTESIAN_POINT ( 'NONE',  ( -1.113548883309542603, 12.28732181966579695, 44.18588492042577798 ) ) ;
#8058=ORIENTED_EDGE ( 'NONE', *, *, #11450, .F. ) ;
#8061=CARTESIAN_POINT ( 'NONE',  ( -1.046936909428696882, 12.93351869073272908, -43.93225665392618851 ) ) ;
#8074=VERTEX_POINT ( 'NONE', #14542 ) ;
#8077=CARTESIAN_POINT ( 'NONE',  ( -2.265401668238139266, -17.02144111536849636, 43.82493763960401623 ) ) ;
#8078=CARTESIAN_POINT ( 'NONE',  ( -1.048171036023512803, -43.23005599774311492, -15.11933492062811801 ) ) ;
#8079=CARTESIAN_POINT ( 'NONE',  ( -20.57838717382308147, -10.78122205917020437, -27.96569011373082603 ) ) ;
#8086=VERTEX_POINT ( 'NONE', #8497 ) ;
#8090=CARTESIAN_POINT ( 'NONE',  ( -1.155031165708890306, 12.20332162035463419, -44.25214473648917135 ) ) ;
#8094=ORIENTED_EDGE ( 'NONE', *, *, #11768, .F. ) ;
#8097=CARTESIAN_POINT ( 'NONE',  ( -20.20700224038492721, -23.35150625415671755, -18.19058640100215385 ) ) ;
#8099=CARTESIAN_POINT ( 'NONE',  ( -20.24419206586953379, -24.70913649113841970, -16.36655224501358319 ) ) ;
#8101=VERTEX_POINT ( 'NONE', #25917 ) ;
#8108=CARTESIAN_POINT ( 'NONE',  ( -7.078251931573400491, 20.86696228105224549, -47.71415099571811425 ) ) ;
#8109=CARTESIAN_POINT ( 'NONE',  ( -55.24271866751342941, -0.006757859501005985571, -0.006671293903669251422 ) ) ;
#8116=CARTESIAN_POINT ( 'NONE',  ( -20.20700224038492721, 0.9908225410482660589, 29.58392382092671724 ) ) ;
#8118=EDGE_CURVE ( 'NONE', #15484, #12242, #18513, .T. ) ;
#8120=ADVANCED_FACE ( 'NONE', ( #16860 ), #5378, .F. ) ;
#8123=CARTESIAN_POINT ( 'NONE',  ( -55.24198130335446422, 0.009170435128245552417, -0.001516807524704325135 ) ) ;
#8126=VERTEX_POINT ( 'NONE', #10799 ) ;
#8128=DIRECTION ( 'NONE',  ( 0.000000000000000000, 5.223019709707975211E-21, -1.000000000000000000 ) ) ;
#8133=EDGE_LOOP ( 'NONE', ( #27809, #23414, #4983, #399 ) ) ;
#8134=B_SPLINE_CURVE_WITH_KNOTS ( 'NONE', 3,
 ( #5755, #23316, #14649, #16389, #20856, #12626 ),
 .UNSPECIFIED., .F., .F.,
 ( 4, 2, 4 ),
 ( 1.536381426628689196E-16, 0.003570751334075638293, 0.007141502668151123064 ),
 .UNSPECIFIED. ) ;
#8136=CARTESIAN_POINT ( 'NONE',  ( -20.20700224038492010, 16.58740185276710832, -24.51628800869052682 ) ) ;
#8139=CARTESIAN_POINT ( 'NONE',  ( -20.21097721712959228, 23.76068428613707439, 17.67178718142832494 ) ) ;
#8140=EDGE_CURVE ( 'NONE', #5273, #13567, #14016, .T. ) ;
#8141=CARTESIAN_POINT ( 'NONE',  ( -20.57838717382308147, 27.96569011373101077, 10.78122205916971055 ) ) ;
#8142=( NAMED_UNIT ( * ) PLANE_ANGLE_UNIT ( ) SI_UNIT ( $, .RADIAN. ) );
#8147=CARTESIAN_POINT ( 'NONE',  ( -8.786685647604720373, -47.14957014837338534, -25.35688121747513435 ) ) ;
#8150=CARTESIAN_POINT ( 'NONE',  ( -1.619063947482197729, 2.489035965910159298, -46.30105812165548684 ) ) ;
#8153=CARTESIAN_POINT ( 'NONE',  ( -7.078251931573406708, -5.101176922831029081, -51.82710018979473432 ) ) ;
#8158=VERTEX_POINT ( 'NONE', #26737 ) ;
#8167=EDGE_CURVE ( 'NONE', #21682, #25305, #14387, .T. ) ;
#8169=CARTESIAN_POINT ( 'NONE',  ( -20.57838717382308147, -23.26537097894090778, 18.89542499756525729 ) ) ;
#8171=CARTESIAN_POINT ( 'NONE',  ( 60.46576798286869803, -4.195655488513964285E-16, 1.048913872128491071E-16 ) ) ;
#8179=CARTESIAN_POINT ( 'NONE',  ( -55.24300891470650754, -0.005486913146700035313, 0.008142823778062066586 ) ) ;
#8181=CARTESIAN_POINT ( 'NONE',  ( -8.786685647604894456, 7.199674155859698388, 53.04920435127174017 ) ) ;
#8185=CARTESIAN_POINT ( 'NONE',  ( -16.86833981943424376, -19.19877306373879122, -39.83928801320582380 ) ) ;
#8186=DIRECTION ( 'NONE',  ( 0.000000000000000000, 5.223019709708233256E-21, -1.000000000000000000 ) ) ;
#8192=CARTESIAN_POINT ( 'NONE',  ( -10.86508079875779842, -24.22249093393332231, -45.04061326950863275 ) ) ;
#8200=CARTESIAN_POINT ( 'NONE',  ( -1.045287976400362417, -43.05558670614257721, -15.59869763335051651 ) ) ;
#8201=CARTESIAN_POINT ( 'NONE',  ( -1.048172774974269084, -13.17853518375268074, 43.86067135048633503 ) ) ;
#8206=CARTESIAN_POINT ( 'NONE',  ( -1.045287976400386842, -28.14015102489780062, 36.12803364096639314 ) ) ;
#8212=CARTESIAN_POINT ( 'NONE',  ( -12.82751273423882665, 48.09651489336691554, 8.715310691359739792 ) ) ;
#8219=CARTESIAN_POINT ( 'NONE',  ( -7.078251931573406708, 44.92740138729204347, 26.33626633876174239 ) ) ;
#8225=CARTESIAN_POINT ( 'NONE',  ( -1.259920593601968397, -25.19630221849078211, -38.49623866863340993 ) ) ;
#8227=LINE ( 'NONE', #6078, #11614 ) ;
#8234=AXIS2_PLACEMENT_3D ( 'NONE', #22600, #11077, #17818 ) ;
#8242=ORIENTED_EDGE ( 'NONE', *, *, #18452, .F. ) ;
#8255=CARTESIAN_POINT ( 'NONE',  ( -8.786685647604890903, -25.35688121747466184, 47.14957014837381166 ) ) ;
#8262=EDGE_LOOP ( 'NONE', ( #25798, #3173 ) ) ;
#8264=B_SPLINE_CURVE_WITH_KNOTS ( 'NONE', 3,
 ( #18996, #8077, #16259, #25059, #7788, #5314, #14087, #3309 ),
 .UNSPECIFIED., .F., .F.,
 ( 4, 2, 2, 4 ),
 ( 2.169948783056603995E-16, 0.002761568181852859429, 0.005523136363705502018, 0.01104627272741079240 ),
 .UNSPECIFIED. ) ;
#8265=EDGE_CURVE ( 'NONE', #28137, #1581, #23337, .T. ) ;
#8267=EDGE_CURVE ( 'NONE', #19868, #21344, #11788, .T. ) ;
#8268=CARTESIAN_POINT ( 'NONE',  ( -23.77929240705207192, 4.877832571065432887, 35.93174012244165283 ) ) ;
#8278=CARTESIAN_POINT ( 'NONE',  ( -20.20700224038492010, -8.199606986804138131, 28.44216453106544762 ) ) ;
#8284=CARTESIAN_POINT ( 'NONE',  ( -7.711401346138395674, -35.51061203065555816, -38.61705198405353912 ) ) ;
#8285=DIRECTION ( 'NONE',  ( 0.000000000000000000, 5.223019709707975211E-21, -1.000000000000000000 ) ) ;
#8307=CARTESIAN_POINT ( 'NONE',  ( -1.113427685306993542, 45.82016658690751854, -1.967672929087340261 ) ) ;
#8310=ORIENTED_EDGE ( 'NONE', *, *, #7415, .F. ) ;
#8317=CARTESIAN_POINT ( 'NONE',  ( -4.162674018437130030, 3.424137510344948510, -48.79210541969630555 ) ) ;
#8322=CARTESIAN_POINT ( 'NONE',  ( -2.265401668238147259, 25.45016726748371738, 39.53028715828205009 ) ) ;
#8331=EDGE_CURVE ( 'NONE', #15612, #4924, #7527, .T. ) ;
#8332=CARTESIAN_POINT ( 'NONE',  ( -7.711401346138408108, 51.42722225669434266, 10.36923727626067304 ) ) ;
#8338=ORIENTED_EDGE ( 'NONE', *, *, #7108, .T. ) ;
#8339=EDGE_CURVE ( 'NONE', #8356, #4222, #5097, .T. ) ;
#8341=CARTESIAN_POINT ( 'NONE',  ( -1.113427685306983550, -12.28784199929904730, 44.18561238466750041 ) ) ;
#8344=CARTESIAN_POINT ( 'NONE',  ( -28.41354790283022069, 5.969609727608339966, 22.41474081377994310 ) ) ;
#8348=CARTESIAN_POINT ( 'NONE',  ( -55.24728320129491266, -0.008013189884951492717, -0.01214321324517155139 ) ) ;
#8350=CARTESIAN_POINT ( 'NONE',  ( -1.259920593601978833, -28.82601305773628297, 35.85909937955954518 ) ) ;
#8355=AXIS2_PLACEMENT_3D ( 'NONE', #4771, #4621, #13539 ) ;
#8356=VERTEX_POINT ( 'NONE', #23597 ) ;
#8358=B_SPLINE_CURVE_WITH_KNOTS ( 'NONE', 3,
 ( #20716, #14088, #2730, #24640, #22465, #13805 ),
 .UNSPECIFIED., .F., .F.,
 ( 4, 2, 4 ),
 ( 4.906538933386797396E-18, 0.003570751334075636559, 0.007141502668151274852 ),
 .UNSPECIFIED. ) ;
#8360=CARTESIAN_POINT ( 'NONE',  ( -1.045287976400365970, 15.59869763335156101, 43.05558670614217931 ) ) ;
#8361=CARTESIAN_POINT ( 'NONE',  ( -7.711401346138400115, 38.61705198405368122, -35.51061203065540894 ) ) ;
#8364=CARTESIAN_POINT ( 'NONE',  ( -1.239374126674604337, -25.08410696974269527, -38.61989855450929809 ) ) ;
#8372=CARTESIAN_POINT ( 'NONE',  ( -2.265401668238145483, -36.42007794497270368, -29.73100299756553966 ) ) ;
#8377=VECTOR ( 'NONE', #836, 999.9999999999998863 ) ;
#8382=EDGE_CURVE ( 'NONE', #12154, #3886, #20552, .T. ) ;
#8383=CARTESIAN_POINT ( 'NONE',  ( -55.25719721206881729, -0.009391134844728631428, 0.006045473558784497832 ) ) ;
#8404=EDGE_CURVE ( 'NONE', #5134, #23391, #24335, .T. ) ;
#8407=ADVANCED_FACE ( 'NONE', ( #25739 ), #25073, .F. ) ;
#8409=EDGE_CURVE ( 'NONE', #20822, #6550, #15388, .T. ) ;
#8416=CARTESIAN_POINT ( 'NONE',  ( -1.050231094221210748, 27.12595454131558981, 36.90262059116437854 ) ) ;
#8418=ORIENTED_EDGE ( 'NONE', *, *, #8857, .F. ) ;
#8420=CARTESIAN_POINT ( 'NONE',  ( -1.539760825549688850, 29.16712717142812039, 35.94320866319458219 ) ) ;
#8421=FACE_OUTER_BOUND ( 'NONE', #7454, .T. ) ;
#8431=ORIENTED_EDGE ( 'NONE', *, *, #23327, .T. ) ;
#8432=ORIENTED_EDGE ( 'NONE', *, *, #23079, .T. ) ;
#8433=EDGE_CURVE ( 'NONE', #21416, #12683, #5885, .T. ) ;
#8437=CARTESIAN_POINT ( 'NONE',  ( -8.259864102781676820, 36.24929574824966494, 38.68084189741909995 ) ) ;
#8440=CARTESIAN_POINT ( 'NONE',  ( -1.239374126674604337, 42.99367564261301311, 16.50008610789253893 ) ) ;
#8447=CARTESIAN_POINT ( 'NONE',  ( -55.24390624410018802, -0.009374879212970498032, 0.004572280736701721943 ) ) ;
#8460=CARTESIAN_POINT ( 'NONE',  ( -1.239374126674604337, -42.99367564261267916, 16.50008610789344488 ) ) ;
#8462=VECTOR ( 'NONE', #16494, 1000.000000000000000 ) ;
#8465=CARTESIAN_POINT ( 'NONE',  ( -25.21435515916025594, 1.749597353048488237E-16, -4.373993382621220594E-17 ) ) ;
#8468=CARTESIAN_POINT ( 'NONE',  ( -55.24271866751342941, 0.008433070970614317194, 0.004365563123939311327 ) ) ;
#8471=EDGE_CURVE ( 'NONE', #25254, #18677, #11994, .T. ) ;
#8475=DIRECTION ( 'NONE',  ( 1.000000000000000000, -6.938893903907226837E-18, 1.734723475976806709E-18 ) ) ;
#8479=CARTESIAN_POINT ( 'NONE',  ( -1.113427685307011084, 35.91272432484659305, -28.52429901637181686 ) ) ;
#8480=CARTESIAN_POINT ( 'NONE',  ( -1.045287976400365970, -45.76855895860942525, 1.530335034934587002 ) ) ;
#8484=CARTESIAN_POINT ( 'NONE',  ( -1.045287976400362417, 25.66401692419989899, -37.92705037016767733 ) ) ;
#8493=CARTESIAN_POINT ( 'NONE',  ( -1.113427685306992876, 16.03057832159213092, 42.96952363574816758 ) ) ;
#8497=CARTESIAN_POINT ( 'NONE',  ( -1.619063947482197729, -44.80407745103793360, -11.94059994246142331 ) ) ;
#8502=CARTESIAN_POINT ( 'NONE',  ( -55.24300891470650754, -0.0003472257464211635897, -0.009812809446892990090 ) ) ;
#8504=ADVANCED_FACE ( 'NONE', ( #22263 ), #14184, .F. ) ;
#8505=CARTESIAN_POINT ( 'NONE',  ( -20.47566338032515887, -28.85746366088576664, -7.708089572830313152 ) ) ;
#8506=( BOUNDED_SURFACE ( )  B_SPLINE_SURFACE ( 3, 1, ( 
 ( #11386, #9392 ),
 ( #13974, #736 ),
 ( #2907, #18143 ),
 ( #446, #13681 ) ),
 .UNSPECIFIED., .F., .F., .F. ) 
 B_SPLINE_SURFACE_WITH_KNOTS ( ( 4, 4 ),
 ( 2, 2 ),
 ( 0.000000000000000000, 1.000000000000000000 ),
 ( 0.000000000000000000, 1.000000000000000000 ),
 .UNSPECIFIED. ) 
 GEOMETRIC_REPRESENTATION_ITEM ( )  RATIONAL_B_SPLINE_SURFACE ( (
 ( 1.000000000000000000, 1.000000000000000000),
 ( 0.9934239774497837239, 0.8357310067453919133),
 ( 0.9934239774497837239, 0.8357310067453919133),
 ( 1.000000000000000000, 1.000000000000000000) ) ) 
 REPRESENTATION_ITEM ( '' )  SURFACE ( )  );
#8509=CARTESIAN_POINT ( 'NONE',  ( -6.588769196390752647, 34.04709086065316370, -38.42957692275855663 ) ) ;
#8518=CARTESIAN_POINT ( 'NONE',  ( -55.24198130335446422, 0.006527480770974009895, 0.006617369590171991688 ) ) ;
#8519=CARTESIAN_POINT ( 'NONE',  ( -1.239374126674604337, 11.92219841463891861, 44.48112152129332486 ) ) ;
#8524=CARTESIAN_POINT ( 'NONE',  ( -8.786685647604894456, -23.24040270374358030, 48.22796981442792230 ) ) ;
#8527=CARTESIAN_POINT ( 'NONE',  ( -16.86833981943423666, 7.884812276282103127, -43.51541671545727041 ) ) ;
#8532=ORIENTED_EDGE ( 'NONE', *, *, #12184, .T. ) ;
#8534=ORIENTED_EDGE ( 'NONE', *, *, #24412, .T. ) ;
#8539=EDGE_LOOP ( 'NONE', ( #10875, #5860, #20742, #24172 ) ) ;
#8549=EDGE_CURVE ( 'NONE', #12509, #7528, #3675, .T. ) ;
#8553=EDGE_CURVE ( 'NONE', #27588, #20203, #3025, .T. ) ;
#8561=ORIENTED_EDGE ( 'NONE', *, *, #20953, .T. ) ;
#8568=( BOUNDED_SURFACE ( )  B_SPLINE_SURFACE ( 3, 1, ( 
 ( #10083, #5618 ),
 ( #25761, #19137 ),
 ( #25628, #12645 ),
 ( #14525, #9947 ) ),
 .UNSPECIFIED., .F., .F., .F. ) 
 B_SPLINE_SURFACE_WITH_KNOTS ( ( 4, 4 ),
 ( 2, 2 ),
 ( 0.000000000000000000, 1.000000000000000000 ),
 ( 0.000000000000000000, 1.000000000000000000 ),
 .UNSPECIFIED. ) 
 GEOMETRIC_REPRESENTATION_ITEM ( )  RATIONAL_B_SPLINE_SURFACE ( (
 ( 1.000000000000000000, 1.000000000000000000),
 ( 0.9593753223639863714, 0.9995975284513187731),
 ( 0.9593753223639863714, 0.9995975284513187731),
 ( 1.000000000000000000, 1.000000000000000000) ) ) 
 REPRESENTATION_ITEM ( '' )  SURFACE ( )  );
#8575=FACE_OUTER_BOUND ( 'NONE', #326, .T. ) ;
#8578=EDGE_CURVE ( 'NONE', #6993, #16312, #255, .T. ) ;
#8579=EDGE_LOOP ( 'NONE', ( #21529, #11393, #9639, #1775 ) ) ;
#8582=CARTESIAN_POINT ( 'NONE',  ( -20.57838717382308147, 29.92853265176831812, 1.611677988432465014 ) ) ;
#8586=ORIENTED_EDGE ( 'NONE', *, *, #12675, .F. ) ;
#8600=ORIENTED_EDGE ( 'NONE', *, *, #7105, .T. ) ;
#8603=ORIENTED_EDGE ( 'NONE', *, *, #17825, .T. ) ;
#8613=CARTESIAN_POINT ( 'NONE',  ( -20.57838717382308147, 28.96176188950229502, 7.715628353033378239 ) ) ;
#8625=CARTESIAN_POINT ( 'NONE',  ( -20.57838717382308147, 1.611677988432361097, -29.92853265176831812 ) ) ;
#8633=CARTESIAN_POINT ( 'NONE',  ( -55.24728320129491266, 0.003868537197317429340, 0.01402509393918536899 ) ) ;
#8634=CARTESIAN_POINT ( 'NONE',  ( 7.762687761849954095E-17, 6.048924312129458720E-15, -44.74884827092600403 ) ) ;
#8635=CARTESIAN_POINT ( 'NONE',  ( -28.41354790283022069, 19.47297445639567925, 12.60397206714810814 ) ) ;
#8638=CARTESIAN_POINT ( 'NONE',  ( -1.050230346682677007, 0.0006945978175690684661, -45.79907861045643358 ) ) ;
#8640=ORIENTED_EDGE ( 'NONE', *, *, #25964, .T. ) ;
#8650=CARTESIAN_POINT ( 'NONE',  ( -55.25297051322618813, -0.007247191603131164853, -0.01306918787467609838 ) ) ;
#8658=( BOUNDED_SURFACE ( )  B_SPLINE_SURFACE ( 3, 1, ( 
 ( #6095, #27813 ),
 ( #26069, #8519 ),
 ( #2021, #21468 ),
 ( #8109, #1608 ) ),
 .UNSPECIFIED., .F., .F., .F. ) 
 B_SPLINE_SURFACE_WITH_KNOTS ( ( 4, 4 ),
 ( 2, 2 ),
 ( 0.000000000000000000, 1.000000000000000000 ),
 ( 0.000000000000000000, 1.000000000000000000 ),
 .UNSPECIFIED. ) 
 GEOMETRIC_REPRESENTATION_ITEM ( )  RATIONAL_B_SPLINE_SURFACE ( (
 ( 1.000000000000000000, 1.000000000000000000),
 ( 0.9934239774497837239, 0.8357310067453919133),
 ( 0.9934239774497837239, 0.8357310067453919133),
 ( 1.000000000000000000, 1.000000000000000000) ) ) 
 REPRESENTATION_ITEM ( '' )  SURFACE ( )  );
#8662=CARTESIAN_POINT ( 'NONE',  ( -1.259920593601976613, -44.39818421957808425, 12.06711544331609609 ) ) ;
#8663=CARTESIAN_POINT ( 'NONE',  ( -1.031422197589716205, -28.14735071801769095, -36.13727897780117360 ) ) ;
#8677=EDGE_CURVE ( 'NONE', #4951, #22965, #28103, .T. ) ;
#8685=CARTESIAN_POINT ( 'NONE',  ( -1.046935749539996907, 25.87617179820970748, 37.78548154587966934 ) ) ;
#8686=CARTESIAN_POINT ( 'NONE',  ( -7.733045908741331687, -5.980865481987790666, 52.15131830128831325 ) ) ;
#8691=DIRECTION ( 'NONE',  ( -0.7637818620346801257, 0.02150485345384840416, 0.6451161201712179993 ) ) ;
#8692=CARTESIAN_POINT ( 'NONE',  ( -1.031422197589716205, 36.13727897780129439, -28.14735071801756661 ) ) ;
#8694=CARTESIAN_POINT ( 'NONE',  ( -20.24399999263415850, -29.60996018918693551, -1.282322917263360340 ) ) ;
#8704=ORIENTED_EDGE ( 'NONE', *, *, #9941, .T. ) ;
#8721=CARTESIAN_POINT ( 'NONE',  ( -1.031422197589711764, 37.93675465142472802, -25.67058493451456158 ) ) ;
#8723=VERTEX_POINT ( 'NONE', #8150 ) ;
#8726=CARTESIAN_POINT ( 'NONE',  ( -1.049817751779875907, -27.33161971822171310, 36.75003908324323021 ) ) ;
#8731=CARTESIAN_POINT ( 'NONE',  ( -55.25297051322618813, -0.002853887643042011396, 0.01466904165775133329 ) ) ;
#8733=CARTESIAN_POINT ( 'NONE',  ( -1.323830074806771062, 16.42382241777537644, -43.04593525292974476 ) ) ;
#8737=ORIENTED_EDGE ( 'NONE', *, *, #8549, .T. ) ;
#8741=EDGE_CURVE ( 'NONE', #2685, #13364, #21077, .T. ) ;
#8742=AXIS2_PLACEMENT_3D ( 'NONE', #15247, #20139, #7070 ) ;
#8746=EDGE_CURVE ( 'NONE', #987, #27064, #21232, .T. ) ;
#8748=CARTESIAN_POINT ( 'NONE',  ( -25.21435515916025594, 1.749597353048488237E-16, -4.373993382621220594E-17 ) ) ;
#8762=CARTESIAN_POINT ( 'NONE',  ( -20.20700224038492721, -29.58392382092672790, 0.9908225410481621420 ) ) ;
#8777=CARTESIAN_POINT ( 'NONE',  ( -1.155031165708881646, -42.97366960678589720, 16.13806347973043387 ) ) ;
#8780=VERTEX_POINT ( 'NONE', #16634 ) ;
#8786=ORIENTED_EDGE ( 'NONE', *, *, #15785, .T. ) ;
#8795=CARTESIAN_POINT ( 'NONE',  ( -18.41936578851719730, -37.37524689996168803, 20.09935324538230006 ) ) ;
#8796=CARTESIAN_POINT ( 'NONE',  ( -4.473127245936434626, 37.94261489385718988, -31.51789735524207003 ) ) ;
#8797=VERTEX_POINT ( 'NONE', #14959 ) ;
#8798=DIRECTION ( 'NONE',  ( 1.000000000000000000, -6.938893903907226837E-18, 1.734723475976806709E-18 ) ) ;
#8807=VECTOR ( 'NONE', #21689, 1000.000000000000114 ) ;
#8808=CARTESIAN_POINT ( 'NONE',  ( -20.38016308990357572, -27.81387210821415223, 10.62413300761014945 ) ) ;
#8811=CARTESIAN_POINT ( 'NONE',  ( -25.21435515916043002, 23.92354251275938992, -25.00736669481030106 ) ) ;
#8824=( BOUNDED_SURFACE ( )  B_SPLINE_SURFACE ( 3, 1, ( 
 ( #4834, #9018 ),
 ( #2519, #15329 ),
 ( #13311, #510 ),
 ( #24421, #15185 ) ),
 .UNSPECIFIED., .F., .F., .F. ) 
 B_SPLINE_SURFACE_WITH_KNOTS ( ( 4, 4 ),
 ( 2, 2 ),
 ( 0.000000000000000000, 1.000000000000000000 ),
 ( 0.000000000000000000, 1.000000000000000000 ),
 .UNSPECIFIED. ) 
 GEOMETRIC_REPRESENTATION_ITEM ( )  RATIONAL_B_SPLINE_SURFACE ( (
 ( 1.000000000000000000, 1.000000000000000000),
 ( 0.9934239774497837239, 0.8357310067453919133),
 ( 0.9934239774497837239, 0.8357310067453919133),
 ( 1.000000000000000000, 1.000000000000000000) ) ) 
 REPRESENTATION_ITEM ( '' )  SURFACE ( )  );
#8825=B_SPLINE_CURVE_WITH_KNOTS ( 'NONE', 3,
 ( #23214, #21165, #19156, #22925, #27357, #8225, #10393, #1593, #3329, #25077 ),
 .UNSPECIFIED., .F., .F.,
 ( 4, 2, 2, 2, 4 ),
 ( 2.825996620262520077E-16, 0.0003346187017559037265, 0.0006692374035115249099, 0.001003856105267145931, 0.001338474807022767060 ),
 .UNSPECIFIED. ) ;
#8842=CARTESIAN_POINT ( 'NONE',  ( -8.786685647604896232, 9.545808661481343549, 52.67761315067276229 ) ) ;
#8848=ORIENTED_EDGE ( 'NONE', *, *, #16906, .F. ) ;
#8850=EDGE_CURVE ( 'NONE', #20163, #28300, #620, .T. ) ;
#8852=CARTESIAN_POINT ( 'NONE',  ( -6.574463467970651287, -34.08059230520071736, -38.37705091668365043 ) ) ;
#8853=CARTESIAN_POINT ( 'NONE',  ( -1.031422197589711987, -28.14735071801769095, -36.13727897780115939 ) ) ;
#8857=EDGE_CURVE ( 'NONE', #16496, #19868, #6434, .T. ) ;
#8869=VECTOR ( 'NONE', #23608, 1000.000000000000000 ) ;
#8884=CARTESIAN_POINT ( 'NONE',  ( -6.588769196390761529, 20.50531526814562966, -47.06982923582516065 ) ) ;
#8890=VERTEX_POINT ( 'NONE', #6800 ) ;
#8891=CARTESIAN_POINT ( 'NONE',  ( -55.24340739397742794, 0.008612749836243148785, 0.005344433640974122733 ) ) ;
#8897=CARTESIAN_POINT ( 'NONE',  ( -21.41430102051751660, -25.94791611261628717, -16.60879216503625244 ) ) ;
#8907=ORIENTED_EDGE ( 'NONE', *, *, #2906, .F. ) ;
#8908=CARTESIAN_POINT ( 'NONE',  ( -8.786685647604885574, 6.096987947571466530E-17, -1.524246986892866633E-17 ) ) ;
#8913=ORIENTED_EDGE ( 'NONE', *, *, #20410, .T. ) ;
#8916=CARTESIAN_POINT ( 'NONE',  ( -20.38016308990358993, -29.73560196176845238, 1.509191766064522655 ) ) ;
#8918=ADVANCED_FACE ( 'NONE', ( #596 ), #8506, .F. ) ;
#8923=( BOUNDED_SURFACE ( )  B_SPLINE_SURFACE ( 3, 1, ( 
 ( #14331, #18358 ),
 ( #27141, #4984 ),
 ( #7449, #23148 ),
 ( #16209, #3406 ) ),
 .UNSPECIFIED., .F., .F., .F. ) 
 B_SPLINE_SURFACE_WITH_KNOTS ( ( 4, 4 ),
 ( 2, 2 ),
 ( 0.000000000000000000, 1.000000000000000000 ),
 ( 0.000000000000000000, 1.000000000000000000 ),
 .UNSPECIFIED. ) 
 GEOMETRIC_REPRESENTATION_ITEM ( )  RATIONAL_B_SPLINE_SURFACE ( (
 ( 1.000000000000000000, 1.000000000000000000),
 ( 0.7789835883360578528, 0.9689951854195403280),
 ( 0.7789835883360578528, 0.9689951854195403280),
 ( 1.000000000000000000, 1.000000000000000000) ) ) 
 REPRESENTATION_ITEM ( '' )  SURFACE ( )  );
#8927=FACE_OUTER_BOUND ( 'NONE', #21314, .T. ) ;
#8935=CARTESIAN_POINT ( 'NONE',  ( -25.21435515916043713, 6.169479169075932745, 34.05351380035326514 ) ) ;
#8938=ORIENTED_EDGE ( 'NONE', *, *, #7366, .T. ) ;
#8939=AXIS2_PLACEMENT_3D ( 'NONE', #12180, #20947, #14472 ) ;
#8941=CARTESIAN_POINT ( 'NONE',  ( -55.24271866751342941, -0.008433070970613524425, -0.004365563123939557658 ) ) ;
#8943=CARTESIAN_POINT ( 'NONE',  ( -1.583189561560252701, -16.68617981233673220, 43.29471907393757846 ) ) ;
#8946=CARTESIAN_POINT ( 'NONE',  ( -55.25719721206881729, -0.0006290797159227240433, -0.01115102788683359700 ) ) ;
#8948=CARTESIAN_POINT ( 'NONE',  ( -20.24399999263414429, 10.36954246768245547, -27.76448601145544259 ) ) ;
#8952=CARTESIAN_POINT ( 'NONE',  ( -55.24198130335446422, 0.009190321388310579431, -0.001391250620101621869 ) ) ;
#8960=EDGE_LOOP ( 'NONE', ( #22889, #4038, #15582, #19998 ) ) ;
#8961=ORIENTED_EDGE ( 'NONE', *, *, #9836, .T. ) ;
#8963=CARTESIAN_POINT ( 'NONE',  ( -1.583189561560255143, -29.24830400313138767, 36.01941156322820348 ) ) ;
#8966=ORIENTED_EDGE ( 'NONE', *, *, #24876, .T. ) ;
#8972=EDGE_CURVE ( 'NONE', #4229, #18216, #7915, .T. ) ;
#8982=CARTESIAN_POINT ( 'NONE',  ( -2.265401668238151256, -2.645701981445478079, 46.93990709177546705 ) ) ;
#8991=CARTESIAN_POINT ( 'NONE',  ( -55.24340739397742084, -0.003826481709803442217, 0.009386184976286439385 ) ) ;
#8993=CARTESIAN_POINT ( 'NONE',  ( -1.048996300304511298, 43.31387123529979277, -14.87787369922182990 ) ) ;
#9009=EDGE_CURVE ( 'NONE', #17579, #27510, #10562, .T. ) ;
#9018=CARTESIAN_POINT ( 'NONE',  ( -1.583189561560255143, -38.94740041318274848, 25.21827308671275247 ) ) ;
#9022=CARTESIAN_POINT ( 'NONE',  ( -1.113548883309548376, 45.82026503946953255, 1.968251867499028585 ) ) ;
#9030=EDGE_CURVE ( 'NONE', #15929, #25022, #26010, .T. ) ;
#9036=CARTESIAN_POINT ( 'NONE',  ( -20.47566262905010603, 28.85746289809577547, -7.708089517695290382 ) ) ;
#9045=CARTESIAN_POINT ( 'NONE',  ( -21.41430102051744910, -7.777552968935554034, 29.81033373822135246 ) ) ;
#9052=CARTESIAN_POINT ( 'NONE',  ( -1.239374126674604337, 45.98822239537607004, 2.406737988131282702 ) ) ;
#9056=CARTESIAN_POINT ( 'NONE',  ( -28.13707043255157103, 12.83104814250454062, -18.96624908365850359 ) ) ;
#9058=CARTESIAN_POINT ( 'NONE',  ( -2.911734481061402757, 47.57875121082948766, -2.802366807346352129 ) ) ;
#9065=CARTESIAN_POINT ( 'NONE',  ( -20.38016308990358638, 18.69911008768368532, 23.16952666206563549 ) ) ;
#9070=EDGE_CURVE ( 'NONE', #2795, #14713, #1929, .T. ) ;
#9077=( BOUNDED_SURFACE ( )  B_SPLINE_SURFACE ( 3, 1, ( 
 ( #4388, #26263 ),
 ( #4522, #6558 ),
 ( #22085, #15310 ),
 ( #24561, #2353 ) ),
 .UNSPECIFIED., .F., .F., .F. ) 
 B_SPLINE_SURFACE_WITH_KNOTS ( ( 4, 4 ),
 ( 2, 2 ),
 ( 0.000000000000000000, 1.000000000000000000 ),
 ( 0.000000000000000000, 1.000000000000000000 ),
 .UNSPECIFIED. ) 
 GEOMETRIC_REPRESENTATION_ITEM ( )  RATIONAL_B_SPLINE_SURFACE ( (
 ( 1.000000000000000000, 1.000000000000000000),
 ( 0.9934239774497838349, 0.8357310067453913582),
 ( 0.9934239774497838349, 0.8357310067453913582),
 ( 1.000000000000000000, 1.000000000000000000) ) ) 
 REPRESENTATION_ITEM ( '' )  SURFACE ( )  );
#9084=FACE_OUTER_BOUND ( 'NONE', #24749, .T. ) ;
#9088=CARTESIAN_POINT ( 'NONE',  ( -4.162674018437135359, -25.90909455705140729, -41.48630000627045433 ) ) ;
#9089=CARTESIAN_POINT ( 'NONE',  ( -25.21435515916043713, -31.17620025257576799, 15.02493970636179377 ) ) ;
#9095=CARTESIAN_POINT ( 'NONE',  ( -55.24390624410018802, 0.009374879212971231821, -0.004572280736701976080 ) ) ;
#9097=ORIENTED_EDGE ( 'NONE', *, *, #5338, .T. ) ;
#9098=ORIENTED_EDGE ( 'NONE', *, *, #13247, .F. ) ;
#9099=ORIENTED_EDGE ( 'NONE', *, *, #19572, .F. ) ;
#9103=EDGE_CURVE ( 'NONE', #21211, #10905, #16030, .T. ) ;
#9107=CARTESIAN_POINT ( 'NONE',  ( -20.20700224038492721, 29.58392382092673500, -0.9908225410479557516 ) ) ;
#9115=CARTESIAN_POINT ( 'NONE',  ( -4.780792508754334591, -3.764354093953240277, 49.38761389561005188 ) ) ;
#9117=FACE_OUTER_BOUND ( 'NONE', #27067, .T. ) ;
#9120=CARTESIAN_POINT ( 'NONE',  ( 60.46576798286869803, -12.50000000000000000, 1.048913872128491071E-16 ) ) ;
#9128=CARTESIAN_POINT ( 'NONE',  ( -25.21435515916043357, -6.169479169075226643, 34.05351380035340014 ) ) ;
#9131=CARTESIAN_POINT ( 'NONE',  ( -28.41354790283022069, -14.62505768302787779, 18.00456980371915705 ) ) ;
#9134=CARTESIAN_POINT ( 'NONE',  ( -20.90916690077963835, -38.93431874629077782, -7.054312691028836291 ) ) ;
#9135=VERTEX_POINT ( 'NONE', #2159 ) ;
#9137=CARTESIAN_POINT ( 'NONE',  ( -24.53237795827026346, 16.68575684089495326, -29.54731592868563439 ) ) ;
#9140=CARTESIAN_POINT ( 'NONE',  ( -8.786685647604896232, 23.24040270374459993, 48.22796981442743913 ) ) ;
#9149=CARTESIAN_POINT ( 'NONE',  ( -21.81686047589425570, 33.92779429964205917, -18.24499610240053116 ) ) ;
#9154=B_SPLINE_CURVE_WITH_KNOTS ( 'NONE', 3,
 ( #20498, #786, #9293, #3093, #20640, #27257, #7145, #3231 ),
 .UNSPECIFIED., .F., .F.,
 ( 4, 2, 2, 4 ),
 ( 0.000000000000000000, 0.002761524886576637201, 0.005523049773153274403, 0.01104609954630654707 ),
 .UNSPECIFIED. ) ;
#9157=B_SPLINE_CURVE_WITH_KNOTS ( 'NONE', 3,
 ( #1283, #25190, #27906, #11943, #21289, #25341, #18566, #16968, #1571, #12232, #8078, #27334, #8200 ),
 .UNSPECIFIED., .F., .F.,
 ( 4, 3, 3, 3, 4 ),
 ( 8.673617379884035472E-18, 0.0007657099931970579596, 0.001531419946797923492, 0.002296279302920159471, 0.003061450627205763737 ),
 .UNSPECIFIED. ) ;
#9159=ORIENTED_EDGE ( 'NONE', *, *, #28410, .F. ) ;
#9160=ADVANCED_FACE ( 'NONE', ( #10964 ), #4277, .F. ) ;
#9161=EDGE_CURVE ( 'NONE', #6242, #28150, #21515, .T. ) ;
#9162=CARTESIAN_POINT ( 'NONE',  ( -1.155031165708885199, -35.88345263711027400, 28.62780465193348789 ) ) ;
#9174=CARTESIAN_POINT ( 'NONE',  ( 2.078045971014549723E-18, -1.958632391140620919E-19, 37.50000000000001421 ) ) ;
#9185=CARTESIAN_POINT ( 'NONE',  ( -55.24390624410018802, -0.004896917417131185259, 0.009209468562452437224 ) ) ;
#9190=ORIENTED_EDGE ( 'NONE', *, *, #16402, .T. ) ;
#9199=ORIENTED_EDGE ( 'NONE', *, *, #28410, .T. ) ;
#9208=ORIENTED_EDGE ( 'NONE', *, *, #18279, .F. ) ;
#9210=CARTESIAN_POINT ( 'NONE',  ( -1.019300379054419947, -42.90269154183439326, -16.06793277091975369 ) ) ;
#9219=CARTESIAN_POINT ( 'NONE',  ( -20.57838717382308147, 10.78122205917039977, 27.96569011373074076 ) ) ;
#9220=CARTESIAN_POINT ( 'NONE',  ( -7.078251931573406708, 38.93060825814230697, -34.59014398252930533 ) ) ;
#9221=VERTEX_POINT ( 'NONE', #20733 ) ;
#9222=AXIS2_PLACEMENT_3D ( 'NONE', #12264, #25526, #12129 ) ;
#9223=CARTESIAN_POINT ( 'NONE',  ( -24.53239521893626218, 33.71193723315153790, 3.868435622621383629 ) ) ;
#9225=PLANE ( 'NONE',  #17998 ) ;
#9227=CARTESIAN_POINT ( 'NONE',  ( -28.13707043255157103, 18.06394523322473944, 14.07296284901312688 ) ) ;
#9231=CARTESIAN_POINT ( 'NONE',  ( -8.786685647604887350, -38.68584556812326980, -37.00619870957918778 ) ) ;
#9232=FACE_OUTER_BOUND ( 'NONE', #15746, .T. ) ;
#9236=CARTESIAN_POINT ( 'NONE',  ( -8.786685647604855376, -7.199674155859337787, -53.04920435127184675 ) ) ;
#9237=CARTESIAN_POINT ( 'NONE',  ( -1.045287976400362417, 37.92705037016796155, 25.66401692419947977 ) ) ;
#9245=CIRCLE ( 'NONE', #21661, 34.60786435723138510 ) ;
#9248=CIRCLE ( 'NONE', #20265, 53.53553390275978785 ) ;
#9250=( BOUNDED_SURFACE ( )  B_SPLINE_SURFACE ( 3, 1, ( 
 ( #5817, #16600 ),
 ( #18468, #11993 ),
 ( #16306, #25392 ),
 ( #9548, #905 ) ),
 .UNSPECIFIED., .F., .F., .F. ) 
 B_SPLINE_SURFACE_WITH_KNOTS ( ( 4, 4 ),
 ( 2, 2 ),
 ( 0.000000000000000000, 1.000000000000000000 ),
 ( 0.000000000000000000, 1.000000000000000000 ),
 .UNSPECIFIED. ) 
 GEOMETRIC_REPRESENTATION_ITEM ( )  RATIONAL_B_SPLINE_SURFACE ( (
 ( 1.000000000000000000, 1.000000000000000000),
 ( 0.7789835883360576307, 0.9689951854195403280),
 ( 0.7789835883360576307, 0.9689951854195403280),
 ( 1.000000000000000000, 1.000000000000000000) ) ) 
 REPRESENTATION_ITEM ( '' )  SURFACE ( )  );
#9253=CARTESIAN_POINT ( 'NONE',  ( -55.24300891470650754, -0.008142823778061761275, -0.005486913146700541852 ) ) ;
#9255=CARTESIAN_POINT ( 'NONE',  ( -1.045287976400362417, 43.05558670614268379, 15.59869763335023229 ) ) ;
#9256=CARTESIAN_POINT ( 'NONE',  ( -55.24390624410018802, 0.007503127514278223366, 0.007245494385991344682 ) ) ;
#9259=CIRCLE ( 'NONE', #11552, 34.60786435723138510 ) ;
#9263=CARTESIAN_POINT ( 'NONE',  ( -1.583189561560255143, 25.21827308671289103, 38.94740041318266321 ) ) ;
#9281=CARTESIAN_POINT ( 'NONE',  ( -1.058473599757816963, -28.32531354681309566, -35.99997772736203672 ) ) ;
#9283=CARTESIAN_POINT ( 'NONE',  ( -23.77929240705207192, -35.68044874544700207, -6.464423883190233866 ) ) ;
#9285=EDGE_LOOP ( 'NONE', ( #10671, #7490, #8432, #19051 ) ) ;
#9292=CARTESIAN_POINT ( 'NONE',  ( -1.048171036023497038, -13.17819047681634537, -43.86077206077064261 ) ) ;
#9293=CARTESIAN_POINT ( 'NONE',  ( -7.711401346138374358, 47.70038152767087780, -21.83927363365046048 ) ) ;
#9296=B_SPLINE_CURVE_WITH_KNOTS ( 'NONE', 3,
 ( #15457, #13589, #24408, #2655, #785, #19936, #217, #11439, #498, #22686, #9292, #18051, #4957 ),
 .UNSPECIFIED., .F., .F.,
 ( 4, 3, 3, 3, 4 ),
 ( 6.938893903907227607E-18, 0.0007657099931970527554, 0.001531419946797919806, 0.002296279302920157302, 0.003061450627205762002 ),
 .UNSPECIFIED. ) ;
#9302=CARTESIAN_POINT ( 'NONE',  ( -1.239374126674604337, -2.406737988130801309, 45.98822239537608425 ) ) ;
#9303=FACE_OUTER_BOUND ( 'NONE', #19439, .T. ) ;
#9304=CARTESIAN_POINT ( 'NONE',  ( -20.57838717382308147, -16.28767523336139078, -25.16001208503099917 ) ) ;
#9310=ORIENTED_EDGE ( 'NONE', *, *, #26933, .F. ) ;
#9315=VERTEX_POINT ( 'NONE', #26028 ) ;
#9324=ORIENTED_EDGE ( 'NONE', *, *, #18126, .T. ) ;
#9332=CARTESIAN_POINT ( 'NONE',  ( -1.583189561560256253, -25.21827308671203838, 38.94740041318321744 ) ) ;
#9336=EDGE_CURVE ( 'NONE', #27723, #20203, #19815, .T. ) ;
#9342=EDGE_CURVE ( 'NONE', #20822, #13087, #9259, .T. ) ;
#9344=EDGE_LOOP ( 'NONE', ( #24665, #11800, #24089, #1962 ) ) ;
#9345=CARTESIAN_POINT ( 'NONE',  ( -1.583189561560253589, -44.83405390829680215, -11.94859433442884189 ) ) ;
#9351=CARTESIAN_POINT ( 'NONE',  ( -16.86833981943425442, 30.57013526701963713, 31.95666732167528323 ) ) ;
#9354=CARTESIAN_POINT ( 'NONE',  ( -1.044556982611275497, -15.70482750345265899, -43.01635920718344153 ) ) ;
#9358=ORIENTED_EDGE ( 'NONE', *, *, #27894, .T. ) ;
#9364=CARTESIAN_POINT ( 'NONE',  ( -20.20898977204108604, -0.6607022527615499241, 29.59696883073212703 ) ) ;
#9365=ORIENTED_EDGE ( 'NONE', *, *, #1533, .F. ) ;
#9369=CONICAL_SURFACE ( 'NONE', #10743, 34.60786435723138510, 0.8559913436420825139 ) ;
#9372=CARTESIAN_POINT ( 'NONE',  ( -25.21435515916043713, 15.02493970636190745, 31.17620025257570759 ) ) ;
#9373=B_SPLINE_CURVE_WITH_KNOTS ( 'NONE', 3,
 ( #2988, #11330, #7311, #25026, #22573, #26865 ),
 .UNSPECIFIED., .F., .F.,
 ( 4, 2, 4 ),
 ( 1.734723475976807094E-18, 0.0004335184443140250579, 0.0008670368886280483810 ),
 .UNSPECIFIED. ) ;
#9375=ORIENTED_EDGE ( 'NONE', *, *, #28321, .T. ) ;
#9379=ORIENTED_EDGE ( 'NONE', *, *, #20905, .T. ) ;
#9382=CARTESIAN_POINT ( 'NONE',  ( -21.81686047589426991, -34.70276904128901663, -16.72402253294301744 ) ) ;
#9384=CARTESIAN_POINT ( 'NONE',  ( -7.733045908741315699, 52.15131830128827062, 5.980865481988326238 ) ) ;
#9390=CARTESIAN_POINT ( 'NONE',  ( -1.058197053496178874, 44.07533330186787168, -12.47644286888530019 ) ) ;
#9392=CARTESIAN_POINT ( 'NONE',  ( -1.583189561560255143, -16.68617981233672509, 43.29471907393757846 ) ) ;
#9395=ORIENTED_EDGE ( 'NONE', *, *, #6227, .F. ) ;
#9398=ORIENTED_EDGE ( 'NONE', *, *, #14588, .T. ) ;
#9400=CARTESIAN_POINT ( 'NONE',  ( -1.031422197589716205, 12.69107518035563764, 44.01264471863834160 ) ) ;
#9402=CARTESIAN_POINT ( 'NONE',  ( -8.786685647604885574, 6.096987947571466530E-17, -1.524246986892866633E-17 ) ) ;
#9408=EDGE_CURVE ( 'NONE', #6634, #2788, #17733, .T. ) ;
#9415=CARTESIAN_POINT ( 'NONE',  ( -20.21097721712959938, -23.76068428613694294, -17.67178718142850258 ) ) ;
#9424=CARTESIAN_POINT ( 'NONE',  ( -55.24271866751342941, -0.009388511352197387999, -0.001425019990782294558 ) ) ;
#9426=CARTESIAN_POINT ( 'NONE',  ( -1.464342487929856107, -29.09292098541686755, -35.90631960086405883 ) ) ;
#9429=ORIENTED_EDGE ( 'NONE', *, *, #4579, .T. ) ;
#9443=CARTESIAN_POINT ( 'NONE',  ( -12.82751273423880178, -23.15139349681279057, 43.04932478553559605 ) ) ;
#9459=CARTESIAN_POINT ( 'NONE',  ( -20.20700224038492721, 16.58740185276746359, 24.51628800869029234 ) ) ;
#9467=CARTESIAN_POINT ( 'NONE',  ( -22.23342874802668589, -20.31166691703108285, 24.24669006619395617 ) ) ;
#9474=CARTESIAN_POINT ( 'NONE',  ( -22.23226125620928784, -7.677408153693816573, 30.68305173820434462 ) ) ;
#9476=CARTESIAN_POINT ( 'NONE',  ( -25.21435515916043002, 30.48034229288640162, -16.39063784838753790 ) ) ;
#9479=CARTESIAN_POINT ( 'NONE',  ( -8.786685647604855376, -7.199674155859337787, -53.04920435127184675 ) ) ;
#9480=FACE_OUTER_BOUND ( 'NONE', #24450, .T. ) ;
#9489=CARTESIAN_POINT ( 'NONE',  ( -24.53237795827032741, 29.54731592868594348, 16.68575684089460864 ) ) ;
#9500=ORIENTED_EDGE ( 'NONE', *, *, #12996, .T. ) ;
#9501=EDGE_CURVE ( 'NONE', #2306, #13087, #27724, .T. ) ;
#9511=B_SPLINE_CURVE_WITH_KNOTS ( 'NONE', 3,
 ( #2857, #26883, #13502, #24616, #26594, #20690, #7191 ),
 .UNSPECIFIED., .F., .F.,
 ( 4, 3, 4 ),
 ( 0.000000000000000000, 0.006568092053401831769, 0.02506242213020820619 ),
 .UNSPECIFIED. ) ;
#9513=CARTESIAN_POINT ( 'NONE',  ( -1.044557008772710072, -45.76404748504492659, -1.643388457097728184 ) ) ;
#9516=CARTESIAN_POINT ( 'NONE',  ( -20.57838717382308147, 28.96176188950229502, 7.715628353033378239 ) ) ;
#9526=CARTESIAN_POINT ( 'NONE',  ( -20.57838717382308147, 1.611677988432778319, 29.92853265176829325 ) ) ;
#9533=VERTEX_POINT ( 'NONE', #25290 ) ;
#9537=CARTESIAN_POINT ( 'NONE',  ( -1.031422197589716205, -43.06660437151320053, -15.60268798220621633 ) ) ;
#9539=CARTESIAN_POINT ( 'NONE',  ( -25.21435515916043357, -34.29329011225959079, -4.655591116594231416 ) ) ;
#9541=CARTESIAN_POINT ( 'NONE',  ( -20.57838717382308147, -27.96569011373093971, -10.78122205916989529 ) ) ;
#9545=CARTESIAN_POINT ( 'NONE',  ( -18.41936578851708717, 30.66520733838696344, 29.33493038358041360 ) ) ;
#9546=CARTESIAN_POINT ( 'NONE',  ( -1.539760825549689516, -25.17088484262114179, 38.84664866728805066 ) ) ;
#9548=CARTESIAN_POINT ( 'NONE',  ( -55.25719721206881729, 0.004044147484878754875, 0.01041086141212503938 ) ) ;
#9549=CARTESIAN_POINT ( 'NONE',  ( -1.050231094221207417, -36.90262059116448512, 27.12595454131546191 ) ) ;
#9552=ORIENTED_EDGE ( 'NONE', *, *, #2468, .F. ) ;
#9554=EDGE_CURVE ( 'NONE', #27588, #13723, #14478, .T. ) ;
#9561=ORIENTED_EDGE ( 'NONE', *, *, #19406, .T. ) ;
#9571=B_SPLINE_CURVE_WITH_KNOTS ( 'NONE', 3,
 ( #8206, #16974, #1578, #25765, #6058, #8350, #23623, #21432, #6197, #25499 ),
 .UNSPECIFIED., .F., .F.,
 ( 4, 2, 2, 2, 4 ),
 ( 2.976713740813343128E-16, 0.0003346187017559147311, 0.0006692374035115318488, 0.001003856105267148966, 0.001338474807022765976 ),
 .UNSPECIFIED. ) ;
#9579=CARTESIAN_POINT ( 'NONE',  ( -25.21435515916043357, 6.169479169075458458, -34.05351380035335751 ) ) ;
#9597=ORIENTED_EDGE ( 'NONE', *, *, #7796, .F. ) ;
#9600=CARTESIAN_POINT ( 'NONE',  ( -25.21435515916044423, -16.39063784838720395, 30.48034229288656505 ) ) ;
#9602=CARTESIAN_POINT ( 'NONE',  ( -20.37983603106074071, 28.74620395171562492, -7.753708011498657626 ) ) ;
#9606=DIRECTION ( 'NONE',  ( -1.000000000000000000, 6.938893903907226837E-18, -1.734723475976806709E-18 ) ) ;
#9608=B_SPLINE_CURVE_WITH_KNOTS ( 'NONE', 3,
 ( #14595, #8139, #2478, #467 ),
 .UNSPECIFIED., .F., .F.,
 ( 4, 4 ),
 ( 1.977889076651310254E-16, 0.001982023823822937677 ),
 .UNSPECIFIED. ) ;
#9615=CARTESIAN_POINT ( 'NONE',  ( -1.048994561756802169, 36.59609844253166244, 27.53485040342854262 ) ) ;
#9619=CARTESIAN_POINT ( 'NONE',  ( -1.619063947482197729, -35.99532424477357750, 29.22875152547795707 ) ) ;
#9620=CARTESIAN_POINT ( 'NONE',  ( -55.24300891470650754, 0.007734635432136952211, -0.006048736206179535120 ) ) ;
#9622=CARTESIAN_POINT ( 'NONE',  ( -6.588769196390765970, -50.13301368233292976, 11.07780292579747083 ) ) ;
#9631=EDGE_CURVE ( 'NONE', #16962, #6242, #4724, .T. ) ;
#9634=CARTESIAN_POINT ( 'NONE',  ( -8.786685647604890903, 52.67761315067286176, -9.545808661480789326 ) ) ;
#9636=CARTESIAN_POINT ( 'NONE',  ( -7.078251931573406708, 50.86685171665428840, 11.16394717458623731 ) ) ;
#9638=ADVANCED_FACE ( 'NONE', ( #12321 ), #18056, .F. ) ;
#9639=ORIENTED_EDGE ( 'NONE', *, *, #15225, .F. ) ;
#9644=CARTESIAN_POINT ( 'NONE',  ( -20.24419206586951603, 24.70913649113854049, 16.36655224501340555 ) ) ;
#9645=CARTESIAN_POINT ( 'NONE',  ( -2.265401668238152588, 45.46007138824041505, -11.98901689611057009 ) ) ;
#9648=ADVANCED_FACE ( 'NONE', ( #19506 ), #23063, .F. ) ;
#9650=ORIENTED_EDGE ( 'NONE', *, *, #6227, .T. ) ;
#9652=CARTESIAN_POINT ( 'NONE',  ( -55.24390624410018802, 0.01027195578988056128, 0.001811362924362418811 ) ) ;
#9655=CARTESIAN_POINT ( 'NONE',  ( -55.24271866751342941, -0.009369360294294061531, 0.001545935011626861600 ) ) ;
#9656=LINE ( 'NONE', #20154, #24863 ) ;
#9660=B_SPLINE_CURVE_WITH_KNOTS ( 'NONE', 3,
 ( #26770, #15845, #24652, #11522, #20298, #18719, #23060 ),
 .UNSPECIFIED., .F., .F.,
 ( 4, 3, 4 ),
 ( 0.000000000000000000, 0.009512539173626427882, 0.02506242213020844906 ),
 .UNSPECIFIED. ) ;
#9661=VERTEX_POINT ( 'NONE', #13301 ) ;
#9663=CARTESIAN_POINT ( 'NONE',  ( -1.046936909428679563, -1.275306677858562221, -45.77873603877005593 ) ) ;
#9666=CARTESIAN_POINT ( 'NONE',  ( -6.588769196390754423, -44.25609997968886233, 26.02756986588589072 ) ) ;
#9669=ORIENTED_EDGE ( 'NONE', *, *, #22365, .F. ) ;
#9672=( BOUNDED_SURFACE ( )  B_SPLINE_SURFACE ( 3, 1, ( 
 ( #18969, #27748 ),
 ( #8179, #16520 ),
 ( #5878, #25600 ),
 ( #5585, #25733 ) ),
 .UNSPECIFIED., .F., .F., .F. ) 
 B_SPLINE_SURFACE_WITH_KNOTS ( ( 4, 4 ),
 ( 2, 2 ),
 ( 0.000000000000000000, 1.000000000000000000 ),
 ( 0.000000000000000000, 1.000000000000000000 ),
 .UNSPECIFIED. ) 
 GEOMETRIC_REPRESENTATION_ITEM ( )  RATIONAL_B_SPLINE_SURFACE ( (
 ( 1.000000000000000000, 1.000000000000000000),
 ( 0.9934239774497838349, 0.8357310067453913582),
 ( 0.9934239774497838349, 0.8357310067453913582),
 ( 1.000000000000000000, 1.000000000000000000) ) ) 
 REPRESENTATION_ITEM ( '' )  SURFACE ( )  );
#9701=ORIENTED_EDGE ( 'NONE', *, *, #17304, .F. ) ;
#9702=B_SPLINE_CURVE_WITH_KNOTS ( 'NONE', 3,
 ( #11784, #11480, #24317, #13639, #20407, #20117 ),
 .UNSPECIFIED., .F., .F.,
 ( 4, 2, 4 ),
 ( 1.734723475976807094E-18, 0.0004335151646191503279, 0.0008670303292382989212 ),
 .UNSPECIFIED. ) ;
#9705=VERTEX_POINT ( 'NONE', #1763 ) ;
#9708=ORIENTED_EDGE ( 'NONE', *, *, #350, .T. ) ;
#9713=CARTESIAN_POINT ( 'NONE',  ( -7.078251931573400491, 26.33626633876288636, 44.92740138729136135 ) ) ;
#9720=DIRECTION ( 'NONE',  ( 0.7563875759206388771, 0.4122509917856751471, -0.5078650950445667833 ) ) ;
#9722=CARTESIAN_POINT ( 'NONE',  ( -4.473127245936431073, -45.82513704981557368, -18.25038884639852199 ) ) ;
#9728=CARTESIAN_POINT ( 'NONE',  ( -55.24271866751342941, -0.006671293903668846365, 0.006757859501006202411 ) ) ;
#9731=B_SPLINE_CURVE_WITH_KNOTS ( 'NONE', 3,
 ( #20981, #5752, #14648, #14077, #14510, #3295, #5303, #990, #18834, #3568 ),
 .UNSPECIFIED., .F., .F.,
 ( 4, 2, 2, 2, 4 ),
 ( 2.168404344971008868E-19, 0.0003346267210630925128, 0.0006692534421261848087, 0.001003880163189277159, 0.001338506884252369401 ),
 .UNSPECIFIED. ) ;
#9746=CARTESIAN_POINT ( 'NONE',  ( -55.24340739397742084, -0.01010924026184288269, -0.0007387096945739216438 ) ) ;
#9752=EDGE_CURVE ( 'NONE', #18844, #14777, #12229, .T. ) ;
#9754=CARTESIAN_POINT ( 'NONE',  ( -1.048996300304495310, 14.87787369922229708, 43.31387123529964356 ) ) ;
#9760=AXIS2_PLACEMENT_3D ( 'NONE', #7081, #8798, #13238 ) ;
#9776=CARTESIAN_POINT ( 'NONE',  ( -20.47566338032522637, -18.81547714195493626, -23.19796701701864805 ) ) ;
#9781=CARTESIAN_POINT ( 'NONE',  ( -1.155031165708878094, -16.13806347973029176, -42.97366960678595404 ) ) ;
#9784=CARTESIAN_POINT ( 'NONE',  ( 60.46576798286869803, 12.50000000000000000, 1.635699886147040789E-15 ) ) ;
#9789=CARTESIAN_POINT ( 'NONE',  ( -25.21435515916043002, 34.05351380035335040, -6.169479169075572145 ) ) ;
#9794=ORIENTED_EDGE ( 'NONE', *, *, #3193, .F. ) ;
#9799=CARTESIAN_POINT ( 'NONE',  ( -1.046935749539995131, -15.35946454248365711, 43.14401153755482454 ) ) ;
#9806=CARTESIAN_POINT ( 'NONE',  ( -20.20612091757420004, -27.77903622052264865, -10.22177757278304888 ) ) ;
#9811=CARTESIAN_POINT ( 'NONE',  ( -25.21435515916043713, -31.17620025257598471, -15.02493970636134613 ) ) ;
#9817=ORIENTED_EDGE ( 'NONE', *, *, #2155, .F. ) ;
#9823=CARTESIAN_POINT ( 'NONE',  ( -1.045287976400362417, 43.05558670614268379, 15.59869763335023229 ) ) ;
#9825=CARTESIAN_POINT ( 'NONE',  ( -1.619063947482201282, 44.80407745103784123, -11.94059994246174838 ) ) ;
#9827=ORIENTED_EDGE ( 'NONE', *, *, #8331, .T. ) ;
#9832=VECTOR ( 'NONE', #2127, 1000.000000000000000 ) ;
#9833=ADVANCED_FACE ( 'NONE', ( #5099 ), #4154, .T. ) ;
#9836=EDGE_CURVE ( 'NONE', #21724, #6278, #645, .T. ) ;
#9839=B_SPLINE_CURVE_WITH_KNOTS ( 'NONE', 3,
 ( #20149, #9223, #15841, #24648, #2293, #22874 ),
 .UNSPECIFIED., .F., .F.,
 ( 4, 2, 4 ),
 ( 9.341771812940338307E-18, 0.003576372551510817021, 0.007152745103021624501 ),
 .UNSPECIFIED. ) ;
#9854=EDGE_LOOP ( 'NONE', ( #9965, #6835, #13295, #18106 ) ) ;
#9862=EDGE_CURVE ( 'NONE', #1581, #15484, #9154, .T. ) ;
#9866=CARTESIAN_POINT ( 'NONE',  ( -55.24198130335446422, -0.004163123460802295971, -0.008310594958153156783 ) ) ;
#9870=CARTESIAN_POINT ( 'NONE',  ( -20.21097721712958517, 17.13687106192379161, 24.14932359587270483 ) ) ;
#9871=CARTESIAN_POINT ( 'NONE',  ( -20.38016308990357928, 10.62413300761025425, 27.81387210821410250 ) ) ;
#9873=CARTESIAN_POINT ( 'NONE',  ( -1.619063947482197729, -43.26576862488445130, -16.67502769180545386 ) ) ;
#9881=CARTESIAN_POINT ( 'NONE',  ( -1.044557008772710516, -36.05793264791363129, -28.22896138707358205 ) ) ;
#9887=ORIENTED_EDGE ( 'NONE', *, *, #7796, .T. ) ;
#9899=CARTESIAN_POINT ( 'NONE',  ( -1.259920593601971950, -43.01175804832021043, -16.33409644610535594 ) ) ;
#9900=DIRECTION ( 'NONE',  ( 0.7637818620346800147, 0.2198041754873883424, -0.6068965246771037547 ) ) ;
#9903=CARTESIAN_POINT ( 'NONE',  ( -4.473127245936431073, 31.51789735524192793, -37.94261489385728936 ) ) ;
#9906=ORIENTED_EDGE ( 'NONE', *, *, #153, .T. ) ;
#9908=DIRECTION ( 'NONE',  ( 1.000000000000000000, -6.938893903907226837E-18, 1.734723475976806709E-18 ) ) ;
#9911=ORIENTED_EDGE ( 'NONE', *, *, #23665, .T. ) ;
#9912=ORIENTED_EDGE ( 'NONE', *, *, #26601, .F. ) ;
#9926=CARTESIAN_POINT ( 'NONE',  ( -1.049819825607589685, 13.66706894614437928, -43.71263398674757639 ) ) ;
#9941=EDGE_CURVE ( 'NONE', #15546, #211, #15308, .T. ) ;
#9942=CARTESIAN_POINT ( 'NONE',  ( -1.045287976400365970, -45.76855895860947498, -1.530335034933654859 ) ) ;
#9947=CARTESIAN_POINT ( 'NONE',  ( -1.031422197589716205, 1.530725436378091553, 45.78027046666442601 ) ) ;
#9949=CARTESIAN_POINT ( 'NONE',  ( -2.904412668506679118, 46.12477647685274462, -11.97478724945526629 ) ) ;
#9965=ORIENTED_EDGE ( 'NONE', *, *, #17212, .T. ) ;
#9969=CARTESIAN_POINT ( 'NONE',  ( -20.47566262905010248, -16.24827521404668929, -25.06314747784830388 ) ) ;
#9987=CARTESIAN_POINT ( 'NONE',  ( -4.178947244162635855, 3.367451375481794074, 48.81675275154071869 ) ) ;
#9997=CARTESIAN_POINT ( 'NONE',  ( -1.539760825549678636, 25.17088484262142956, -38.84664866728784460 ) ) ;
#9999=CARTESIAN_POINT ( 'NONE',  ( -20.37983603106074426, 7.753708011498974706, 28.74620395171554321 ) ) ;
#10005=ADVANCED_FACE ( 'NONE', ( #17285 ), #13108, .F. ) ;
#10016=CARTESIAN_POINT ( 'NONE',  ( -20.57838717382308147, 10.78122205917039977, 27.96569011373074076 ) ) ;
#10018=CARTESIAN_POINT ( 'NONE',  ( -6.588769196390761529, -47.06982923582523171, -20.50531526814544847 ) ) ;
#10020=ORIENTED_EDGE ( 'NONE', *, *, #27328, .F. ) ;
#10022=CARTESIAN_POINT ( 'NONE',  ( -1.323439229708139875, 28.92147054731892908, 35.86372896917441722 ) ) ;
#10027=ADVANCED_FACE ( 'NONE', ( #20014 ), #13438, .F. ) ;
#10043=CARTESIAN_POINT ( 'NONE',  ( -28.41354790283022069, -22.41474081377996441, 5.969609727608259142 ) ) ;
#10047=CARTESIAN_POINT ( 'NONE',  ( -4.473127245936431073, 47.80062405537802306, -12.17046501147532567 ) ) ;
#10050=DIRECTION ( 'NONE',  ( 0.000000000000000000, 5.223019709707975211E-21, -1.000000000000000000 ) ) ;
#10061=CARTESIAN_POINT ( 'NONE',  ( -55.24300891470650754, 0.009439835024159288004, 0.002702093572893217704 ) ) ;
#10064=EDGE_CURVE ( 'NONE', #20693, #16059, #11915, .T. ) ;
#10066=CARTESIAN_POINT ( 'NONE',  ( -7.733045908741333463, 45.70676731105722723, -25.81515396910878479 ) ) ;
#10079=CARTESIAN_POINT ( 'NONE',  ( -1.044557008772710516, -1.643388457097570088, 45.76404748504492659 ) ) ;
#10081=CARTESIAN_POINT ( 'NONE',  ( -1.046935749539990468, -45.77872888003169294, -1.275486069320314497 ) ) ;
#10083=CARTESIAN_POINT ( 'NONE',  ( -55.24271866751342941, -0.004365563123935077734, -0.008433070970613952902 ) ) ;
#10084=AXIS2_PLACEMENT_3D ( 'NONE', #21010, #14677, #12936 ) ;
#10086=CARTESIAN_POINT ( 'NONE',  ( -55.24390624410018802, -0.001451500391952595045, 0.01032895241566660592 ) ) ;
#10091=ORIENTED_EDGE ( 'NONE', *, *, #10307, .T. ) ;
#10095=ADVANCED_FACE ( 'NONE', ( #9084 ), #16398, .F. ) ;
#10096=DIRECTION ( 'NONE',  ( 1.000000000000000000, -6.938893903907226837E-18, 1.734723475976806709E-18 ) ) ;
#10104=CARTESIAN_POINT ( 'NONE',  ( -20.20612091757420359, -23.26073043121646933, -18.30568244821369817 ) ) ;
#10118=CARTESIAN_POINT ( 'NONE',  ( 14.74894986621300141, 12.50000000000000000, 1.596046867330078713E-15 ) ) ;
#10127=CARTESIAN_POINT ( 'NONE',  ( -5.986830583229484581, 4.559539818181838733, 50.53158596890435916 ) ) ;
#10147=AXIS2_PLACEMENT_3D ( 'NONE', #27694, #10558, #5969 ) ;
#10152=CARTESIAN_POINT ( 'NONE',  ( -25.21435515916043713, -34.05351380035337883, -6.169479169075319014 ) ) ;
#10157=AXIS2_PLACEMENT_3D ( 'NONE', #20924, #7568, #18323 ) ;
#10164=ORIENTED_EDGE ( 'NONE', *, *, #9501, .T. ) ;
#10168=EDGE_CURVE ( 'NONE', #12213, #14162, #9656, .T. ) ;
#10174=CARTESIAN_POINT ( 'NONE',  ( -1.619063947482194177, 35.99532424477422410, 29.22875152547716482 ) ) ;
#10181=CIRCLE ( 'NONE', #28073, 34.60786435723138510 ) ;
#10185=VECTOR ( 'NONE', #28010, 999.9999999999998863 ) ;
#10187=CARTESIAN_POINT ( 'NONE',  ( -1.619063947482197729, -43.26576862488445130, -16.67502769180545386 ) ) ;
#10214=CARTESIAN_POINT ( 'NONE',  ( -1.323830074806773061, -12.01461446423233781, -44.47857376182264488 ) ) ;
#10215=CARTESIAN_POINT ( 'NONE',  ( -1.044557008772713624, 12.57891310333411106, 44.03203053429556491 ) ) ;
#10218=CARTESIAN_POINT ( 'NONE',  ( -2.904412668506670681, 40.16685646686207889, -25.64203923793588302 ) ) ;
#10238=DIRECTION ( 'NONE',  ( -0.7637818620346801257, 0.6068965246771014233, -0.2198041754873946707 ) ) ;
#10239=CARTESIAN_POINT ( 'NONE',  ( -55.25719721206881729, 0.01041086141212315547, 0.004044147484874825726 ) ) ;
#10256=CARTESIAN_POINT ( 'NONE',  ( -1.239374126674604337, 28.97829083655491544, 35.79060836339782270 ) ) ;
#10263=ORIENTED_EDGE ( 'NONE', *, *, #12637, .F. ) ;
#10264=CARTESIAN_POINT ( 'NONE',  ( -2.904412668506659578, -36.79926976721470311, -30.27712468694973325 ) ) ;
#10265=CARTESIAN_POINT ( 'NONE',  ( -1.619063947482194177, -46.30105812165547974, 2.489035965910640247 ) ) ;
#10267=VERTEX_POINT ( 'NONE', #23061 ) ;
#10281=CARTESIAN_POINT ( 'NONE',  ( -8.259864102781676820, 6.590267880897663133, 52.60025989855196116 ) ) ;
#10293=ORIENTED_EDGE ( 'NONE', *, *, #18, .T. ) ;
#10297=CARTESIAN_POINT ( 'NONE',  ( -25.21435515916025594, 1.749597353048488237E-16, -4.373993382621220594E-17 ) ) ;
#10300=ORIENTED_EDGE ( 'NONE', *, *, #15831, .F. ) ;
#10301=VECTOR ( 'NONE', #10238, 1000.000000000000000 ) ;
#10307=EDGE_CURVE ( 'NONE', #23680, #27723, #7439, .T. ) ;
#10311=CARTESIAN_POINT ( 'NONE',  ( -55.24390624410018802, -0.007245494385991085341, 0.007503127514277716827 ) ) ;
#10315=ORIENTED_EDGE ( 'NONE', *, *, #1801, .F. ) ;
#10326=ORIENTED_EDGE ( 'NONE', *, *, #25831, .F. ) ;
#10329=ORIENTED_EDGE ( 'NONE', *, *, #18214, .F. ) ;
#10341=CYLINDRICAL_SURFACE ( 'NONE', #461, 12.50000000000000000 ) ;
#10343=CARTESIAN_POINT ( 'NONE',  ( -8.786685647604885574, 6.096987947571466530E-17, -1.524246986892866633E-17 ) ) ;
#10348=CARTESIAN_POINT ( 'NONE',  ( -7.711401346138401003, -52.11446537925908018, 6.030154970217441956 ) ) ;
#10349=CARTESIAN_POINT ( 'NONE',  ( -15.02187109954782507, -32.04062513125090561, 33.49412687891607021 ) ) ;
#10355=CARTESIAN_POINT ( 'NONE',  ( -55.24340739397742084, 0.009386184976286932047, 0.003826481709803695053 ) ) ;
#10368=ORIENTED_EDGE ( 'NONE', *, *, #28417, .F. ) ;
#10371=EDGE_CURVE ( 'NONE', #17023, #27443, #18581, .T. ) ;
#10376=B_SPLINE_CURVE_WITH_KNOTS ( 'NONE', 3,
 ( #15541, #17990, #11105, #9088, #26776, #13246, #26629, #2600 ),
 .UNSPECIFIED., .F., .F.,
 ( 4, 2, 2, 4 ),
 ( 2.214340075454938295E-16, 0.002761568181852865067, 0.005523136363705508090, 0.01104627272741079587 ),
 .UNSPECIFIED. ) ;
#10384=ORIENTED_EDGE ( 'NONE', *, *, #11863, .T. ) ;
#10391=ORIENTED_EDGE ( 'NONE', *, *, #3806, .T. ) ;
#10393=CARTESIAN_POINT ( 'NONE',  ( -1.323830074806772616, -25.17121255494502563, -38.58891736138520656 ) ) ;
#10400=EDGE_CURVE ( 'NONE', #24273, #23707, #27294, .T. ) ;
#10415=CARTESIAN_POINT ( 'NONE',  ( -23.77929240705205771, 6.464423883190382192, -35.68044874544699496 ) ) ;
#10420=CARTESIAN_POINT ( 'NONE',  ( -7.711401346138400115, -25.75361633141456608, 45.70592430511747040 ) ) ;
#10437=CARTESIAN_POINT ( 'NONE',  ( -1.239374126674604337, 44.48112152129347407, -11.92219841463844432 ) ) ;
#10441=VERTEX_POINT ( 'NONE', #1854 ) ;
#10443=DIRECTION ( 'NONE',  ( 1.000000000000000000, -6.938893903907226837E-18, 1.734723475976806709E-18 ) ) ;
#10449=LINE ( 'NONE', #19080, #20748 ) ;
#10451=CARTESIAN_POINT ( 'NONE',  ( -1.619063947482197729, -29.22875152547781852, -35.99532424477369830 ) ) ;
#10458=B_SPLINE_CURVE_WITH_KNOTS ( 'NONE', 3,
 ( #17544, #10808, #6485, #11219, #4315, #8777, #17401, #2006, #13092, #19993 ),
 .UNSPECIFIED., .F., .F.,
 ( 4, 2, 2, 2, 4 ),
 ( 1.301042606982605321E-18, 0.0003346267210630944101, 0.0006692534421261875192, 0.001003880163189280628, 0.001338506884252373737 ),
 .UNSPECIFIED. ) ;
#10472=ORIENTED_EDGE ( 'NONE', *, *, #7006, .T. ) ;
#10480=CARTESIAN_POINT ( 'NONE',  ( -25.21435515916043713, -15.02493970636168896, -31.17620025257581062 ) ) ;
#10483=CARTESIAN_POINT ( 'NONE',  ( -20.57838717382308147, 1.611677988432778319, 29.92853265176829325 ) ) ;
#10487=CARTESIAN_POINT ( 'NONE',  ( -15.02187109954783040, -21.95370994985601953, -40.82269973458228662 ) ) ;
#10489=CARTESIAN_POINT ( 'NONE',  ( -55.24390624410018802, -0.009374879212966679906, -0.004572280736703028189 ) ) ;
#10492=CARTESIAN_POINT ( 'NONE',  ( -1.619063947482197729, 44.80407745103800465, 11.94059994246113021 ) ) ;
#10493=ORIENTED_EDGE ( 'NONE', *, *, #12803, .F. ) ;
#10498=CARTESIAN_POINT ( 'NONE',  ( -1.050230347699842692, 5.964912479342754695E-15, -45.79907861674080749 ) ) ;
#10499=CARTESIAN_POINT ( 'NONE',  ( -1.045287976400351981, 36.12803364096590997, -28.14015102489844011 ) ) ;
#10503=B_SPLINE_CURVE_WITH_KNOTS ( 'NONE', 3,
 ( #19106, #19234, #28148, #16667 ),
 .UNSPECIFIED., .F., .F.,
 ( 4, 4 ),
 ( 1.895855152355442610E-16, 0.001982023823822949386 ),
 .UNSPECIFIED. ) ;
#10512=CARTESIAN_POINT ( 'NONE',  ( -8.786685647604896232, 52.67761315067299677, 9.545808661480061019 ) ) ;
#10514=EDGE_CURVE ( 'NONE', #19079, #16076, #7859, .T. ) ;
#10520=CARTESIAN_POINT ( 'NONE',  ( -55.24271866751342941, 0.008433070970614256479, -0.004365563123935527895 ) ) ;
#10522=EDGE_CURVE ( 'NONE', #4222, #20894, #17349, .T. ) ;
#10525=CARTESIAN_POINT ( 'NONE',  ( -8.786685647604890903, -23.24040270374424466, -48.22796981442760256 ) ) ;
#10526=( BOUNDED_SURFACE ( )  B_SPLINE_SURFACE ( 3, 1, ( 
 ( #1146, #13799 ),
 ( #25333, #5608 ),
 ( #14372, #9636 ),
 ( #22757, #27028 ) ),
 .UNSPECIFIED., .F., .F., .F. ) 
 B_SPLINE_SURFACE_WITH_KNOTS ( ( 4, 4 ),
 ( 2, 2 ),
 ( 0.000000000000000000, 1.000000000000000000 ),
 ( 0.000000000000000000, 1.000000000000000000 ),
 .UNSPECIFIED. ) 
 GEOMETRIC_REPRESENTATION_ITEM ( )  RATIONAL_B_SPLINE_SURFACE ( (
 ( 1.000000000000000000, 1.000000000000000000),
 ( 0.7789835883360576307, 0.9689951854195403280),
 ( 0.7789835883360576307, 0.9689951854195403280),
 ( 1.000000000000000000, 1.000000000000000000) ) ) 
 REPRESENTATION_ITEM ( '' )  SURFACE ( )  );
#10527=VERTEX_POINT ( 'NONE', #24754 ) ;
#10531=AXIS2_PLACEMENT_3D ( 'NONE', #5222, #3352, #11555 ) ;
#10541=CARTESIAN_POINT ( 'NONE',  ( -1.619063947482197729, 46.30105812165548684, 2.489035965910320503 ) ) ;
#10545=CARTESIAN_POINT ( 'NONE',  ( -1.048996300304487095, 45.79145529752471333, -0.7649764263853394697 ) ) ;
#10546=CARTESIAN_POINT ( 'NONE',  ( -8.786685647604931759, 47.14957014837394667, 25.35688121747446999 ) ) ;
#10554=VERTEX_POINT ( 'NONE', #20689 ) ;
#10558=DIRECTION ( 'NONE',  ( -1.000000000000000000, 6.938893903907227607E-18, -1.734723475976806902E-18 ) ) ;
#10561=CARTESIAN_POINT ( 'NONE',  ( -20.47566338032525124, 16.24827550219824701, -25.06314818626695740 ) ) ;
#10562=B_SPLINE_CURVE_WITH_KNOTS ( 'NONE', 3,
 ( #17597, #6258, #6683, #23965, #21926, #8416, #2184, #4221, #12849, #14880, #2331, #8685, #10993 ),
 .UNSPECIFIED., .F., .F.,
 ( 4, 3, 3, 3, 4 ),
 ( 1.551583845779545699E-17, 0.0007657099931970509123, 0.001531419946797920456, 0.002296279302920149930, 0.003061450627205759834 ),
 .UNSPECIFIED. ) ;
#10568=ADVANCED_FACE ( 'NONE', ( #14640 ), #28145, .F. ) ;
#10569=CARTESIAN_POINT ( 'NONE',  ( -55.24340739397742794, -0.005344433640973866861, 0.008612749836242647450 ) ) ;
#10581=CARTESIAN_POINT ( 'NONE',  ( -1.239374126674604337, -28.97829083655465254, -35.79060836339803586 ) ) ;
#10585=ORIENTED_EDGE ( 'NONE', *, *, #9752, .T. ) ;
#10588=CARTESIAN_POINT ( 'NONE',  ( -8.786685647604894456, 37.00619870957989832, 38.68584556812258768 ) ) ;
#10595=AXIS2_PLACEMENT_3D ( 'NONE', #19399, #8475, #26027 ) ;
#10602=CARTESIAN_POINT ( 'NONE',  ( -20.20700224038492721, 10.08426345511588984, -27.82980252387822517 ) ) ;
#10614=CARTESIAN_POINT ( 'NONE',  ( -8.786685647604890903, -23.24040270374424466, -48.22796981442760256 ) ) ;
#10620=VECTOR ( 'NONE', #24053, 999.9999999999997726 ) ;
#10625=VECTOR ( 'NONE', #26554, 1000.000000000000114 ) ;
#10627=ORIENTED_EDGE ( 'NONE', *, *, #20311, .F. ) ;
#10635=LINE ( 'NONE', #12499, #25450 ) ;
#10639=CONICAL_SURFACE ( 'NONE', #3762, 28.92774122539760384, 0.7853981625000054922 ) ;
#10643=CARTESIAN_POINT ( 'NONE',  ( -1.049817751779876351, -0.5106138415323642210, 45.79652915392416190 ) ) ;
#10654=CARTESIAN_POINT ( 'NONE',  ( -20.20700224038492721, -23.35150625415671755, -18.19058640100215385 ) ) ;
#10655=CARTESIAN_POINT ( 'NONE',  ( -1.539760825549689294, 16.63252404870416257, 43.19716078875421772 ) ) ;
#10657=CARTESIAN_POINT ( 'NONE',  ( -25.21435515916043713, -34.05351380035328646, 6.169479169075816394 ) ) ;
#10663=CARTESIAN_POINT ( 'NONE',  ( -55.24340739397742794, 0.007744344507854989193, -0.006539691034608598359 ) ) ;
#10669=CARTESIAN_POINT ( 'NONE',  ( -1.619063947482197729, 29.22875152547757338, -35.99532424477389725 ) ) ;
#10671=ORIENTED_EDGE ( 'NONE', *, *, #14722, .T. ) ;
#10672=ORIENTED_EDGE ( 'NONE', *, *, #5422, .F. ) ;
#10675=ADVANCED_FACE ( 'NONE', ( #19524 ), #11975, .T. ) ;
#10680=EDGE_CURVE ( 'NONE', #10554, #9705, #6358, .T. ) ;
#10682=B_SPLINE_CURVE_WITH_KNOTS ( 'NONE', 3,
 ( #19210, #1781, #14463, #3524, #8021, #23273 ),
 .UNSPECIFIED., .F., .F.,
 ( 4, 2, 4 ),
 ( 7.757919228897728493E-18, 0.0004335184443140311294, 0.0008670368886280545610 ),
 .UNSPECIFIED. ) ;
#10686=CARTESIAN_POINT ( 'NONE',  ( -4.473127245936434626, -31.51789735524219438, -37.94261489385706909 ) ) ;
#10691=CARTESIAN_POINT ( 'NONE',  ( -6.574463467970683261, 44.27173031830773908, 25.96726214983142000 ) ) ;
#10705=VECTOR ( 'NONE', #19950, 999.9999999999998863 ) ;
#10710=B_SPLINE_CURVE_WITH_KNOTS ( 'NONE', 3,
 ( #900, #27525, #5220, #20906 ),
 .UNSPECIFIED., .F., .F.,
 ( 4, 4 ),
 ( 1.920770561445796063E-16, 0.001982023823822942447 ),
 .UNSPECIFIED. ) ;
#10711=LINE ( 'NONE', #23688, #22685 ) ;
#10712=CARTESIAN_POINT ( 'NONE',  ( -20.38016308990357928, 7.753479680700950283, -28.74660391518346714 ) ) ;
#10713=CARTESIAN_POINT ( 'NONE',  ( -8.786685647604890903, 38.68584556812300690, -37.00619870957947910 ) ) ;
#10714=CARTESIAN_POINT ( 'NONE',  ( -4.780792508754329262, 45.80716263181262349, 18.84172549606824987 ) ) ;
#10718=( BOUNDED_SURFACE ( )  B_SPLINE_SURFACE ( 3, 1, ( 
 ( #22258, #2516 ),
 ( #15910, #9302 ),
 ( #7581, #18497 ),
 ( #18199, #26842 ) ),
 .UNSPECIFIED., .F., .F., .F. ) 
 B_SPLINE_SURFACE_WITH_KNOTS ( ( 4, 4 ),
 ( 2, 2 ),
 ( 0.000000000000000000, 1.000000000000000000 ),
 ( 0.000000000000000000, 1.000000000000000000 ),
 .UNSPECIFIED. ) 
 GEOMETRIC_REPRESENTATION_ITEM ( )  RATIONAL_B_SPLINE_SURFACE ( (
 ( 1.000000000000000000, 1.000000000000000000),
 ( 0.9934239774497837239, 0.8357310067453919133),
 ( 0.9934239774497837239, 0.8357310067453919133),
 ( 1.000000000000000000, 1.000000000000000000) ) ) 
 REPRESENTATION_ITEM ( '' )  SURFACE ( )  );
#10725=DIRECTION ( 'NONE',  ( 5.541455922705463698E-20, -5.223019709708320524E-21, 1.000000000000000000 ) ) ;
#10726=CARTESIAN_POINT ( 'NONE',  ( -55.25719721206881729, 0.01115102788683387629, -0.0006290797159233242576 ) ) ;
#10731=CARTESIAN_POINT ( 'NONE',  ( -5.986830583229486358, -33.39046620690942291, -38.20088153919488860 ) ) ;
#10743=AXIS2_PLACEMENT_3D ( 'NONE', #3331, #18276, #16282 ) ;
#10744=CARTESIAN_POINT ( 'NONE',  ( -55.24340739397742794, 0.009386184976285603249, -0.003826481709800144074 ) ) ;
#10746=CARTESIAN_POINT ( 'NONE',  ( -1.019300379054419947, 42.90269154183450695, 16.06793277091947658 ) ) ;
#10749=CARTESIAN_POINT ( 'NONE',  ( -1.031422197589716205, -25.67058493451416368, 37.93675465142500514 ) ) ;
#10750=DIRECTION ( 'NONE',  ( -0.7071067818211357325, 4.902845705138444274E-18, 0.7071067805519594129 ) ) ;
#10755=CARTESIAN_POINT ( 'NONE',  ( -1.044556982611268614, 45.76404732357880079, -1.643392503292874895 ) ) ;
#10761=CARTESIAN_POINT ( 'NONE',  ( -18.41936578851709783, 37.37524689996197935, -20.09935324538209045 ) ) ;
#10762=CARTESIAN_POINT ( 'NONE',  ( -25.21435515916042647, 25.00736669481023355, -23.92354251275945742 ) ) ;
#10763=CARTESIAN_POINT ( 'NONE',  ( -7.711401346138397450, -47.70038152767074990, 21.83927363365083707 ) ) ;
#10764=CARTESIAN_POINT ( 'NONE',  ( -20.21097721650786738, 8.835581399095163491, -28.26295598655176633 ) ) ;
#10765=CIRCLE ( 'NONE', #13433, 44.74884827092600403 ) ;
#10789=DIRECTION ( 'NONE',  ( 0.000000000000000000, 5.223019709707975211E-21, -1.000000000000000000 ) ) ;
#10795=CARTESIAN_POINT ( 'NONE',  ( -1.048172774974293064, -43.23017713506512649, 15.11899685083868761 ) ) ;
#10796=FACE_OUTER_BOUND ( 'NONE', #17937, .T. ) ;
#10799=CARTESIAN_POINT ( 'NONE',  ( -25.21435515916025594, 34.29329011225976132, 4.655591116594488099 ) ) ;
#10808=CARTESIAN_POINT ( 'NONE',  ( -1.539760825549689516, -43.19716078875427456, 16.63252404870400269 ) ) ;
#10820=FACE_OUTER_BOUND ( 'NONE', #4431, .T. ) ;
#10822=FACE_OUTER_BOUND ( 'NONE', #27118, .T. ) ;
#10823=EDGE_CURVE ( 'NONE', #4924, #27145, #17045, .T. ) ;
#10824=CARTESIAN_POINT ( 'NONE',  ( -8.786685647604890903, 37.00619870957935120, -38.68584556812312059 ) ) ;
#10830=CARTESIAN_POINT ( 'NONE',  ( -12.82751273423881599, 8.715310691360238948, -48.09651489336683738 ) ) ;
#10831=CARTESIAN_POINT ( 'NONE',  ( -1.583189561560253589, 2.490696082060518624, 46.33203782964458384 ) ) ;
#10845=PRODUCT_DEFINITION_SHAPE ( 'NONE', 'NONE',  #25506 ) ;
#10854=CARTESIAN_POINT ( 'NONE',  ( -25.21435515916043357, 31.17620025257608418, 15.02493970636113474 ) ) ;
#10858=CARTESIAN_POINT ( 'NONE',  ( -28.13707043255157103, -0.7675454997508607269, -22.88591869784690402 ) ) ;
#10864=VERTEX_POINT ( 'NONE', #23271 ) ;
#10866=LINE ( 'NONE', #28260, #18439 ) ;
#10875=ORIENTED_EDGE ( 'NONE', *, *, #10064, .F. ) ;
#10889=ORIENTED_EDGE ( 'NONE', *, *, #2500, .T. ) ;
#10894=EDGE_CURVE ( 'NONE', #26453, #9221, #14291, .T. ) ;
#10895=CARTESIAN_POINT ( 'NONE',  ( -4.178947244162633190, -45.38689110596704523, 18.28784278438497068 ) ) ;
#10897=CARTESIAN_POINT ( 'NONE',  ( -4.780792508754318604, 18.84172549606871883, -45.80716263181242454 ) ) ;
#10903=CARTESIAN_POINT ( 'NONE',  ( -55.25297051322618813, -0.01354497706059463319, 0.006313402748432140991 ) ) ;
#10905=VERTEX_POINT ( 'NONE', #3106 ) ;
#10912=ORIENTED_EDGE ( 'NONE', *, *, #8409, .T. ) ;
#10913=CARTESIAN_POINT ( 'NONE',  ( -1.045287976400362417, -12.68782741917263657, 44.00138577190661948 ) ) ;
#10928=CARTESIAN_POINT ( 'NONE',  ( -1.050230346682675231, -43.55772679531839486, 14.15203301556477378 ) ) ;
#10931=CARTESIAN_POINT ( 'NONE',  ( -1.463510566862832984, 43.13857742234528558, 16.57250862017374970 ) ) ;
#10934=CARTESIAN_POINT ( 'NONE',  ( -1.045287976400362417, 25.66401692419989899, -37.92705037016767733 ) ) ;
#10937=CARTESIAN_POINT ( 'NONE',  ( -20.57838717382308147, 25.16001208503129760, 16.28767523336092893 ) ) ;
#10948=CARTESIAN_POINT ( 'NONE',  ( -1.583189561560252701, -2.490696082059551397, 46.33203782964464068 ) ) ;
#10949=CARTESIAN_POINT ( 'NONE',  ( -55.24390624410018802, -0.004896917417127438256, -0.009209468562451287102 ) ) ;
#10954=CARTESIAN_POINT ( 'NONE',  ( -20.57838717382308147, -7.715628353033886278, -28.96176188950215646 ) ) ;
#10957=EDGE_CURVE ( 'NONE', #4229, #7217, #23952, .T. ) ;
#10964=FACE_OUTER_BOUND ( 'NONE', #23567, .T. ) ;
#10970=CARTESIAN_POINT ( 'NONE',  ( -1.056502255334264895, -27.33667001641194361, -36.75727364034722200 ) ) ;
#10987=CARTESIAN_POINT ( 'NONE',  ( -1.583189561560256253, 38.94740041318330981, 25.21827308671188916 ) ) ;
#10989=CARTESIAN_POINT ( 'NONE',  ( -4.473127245936431073, 3.196405119333807221, -49.22197550883368677 ) ) ;
#10991=CARTESIAN_POINT ( 'NONE',  ( -16.86833981943425442, 20.94590537750608661, -38.94907963570727816 ) ) ;
#10993=CARTESIAN_POINT ( 'NONE',  ( -1.045287976400362417, 25.66401692420069125, 37.92705037016716574 ) ) ;
#10994=CARTESIAN_POINT ( 'NONE',  ( -1.619063947482197729, -2.489035965909835557, 46.30105812165550816 ) ) ;
#10995=VERTEX_POINT ( 'NONE', #8278 ) ;
#11008=ORIENTED_EDGE ( 'NONE', *, *, #5063, .F. ) ;
#11010=CARTESIAN_POINT ( 'NONE',  ( 60.46576798286869803, -4.195655488513964285E-16, 1.048913872128491071E-16 ) ) ;
#11011=EDGE_LOOP ( 'NONE', ( #13497, #14290, #8532, #21778 ) ) ;
#11014=VERTEX_POINT ( 'NONE', #15148 ) ;
#11016=CARTESIAN_POINT ( 'NONE',  ( -55.24390624410018802, 0.009209468562451588944, -0.004896917417127890151 ) ) ;
#11017=VERTEX_POINT ( 'NONE', #21369 ) ;
#11018=CARTESIAN_POINT ( 'NONE',  ( -55.24390624410018802, 0.004896917417131886954, -0.009209468562452662738 ) ) ;
#11020=CARTESIAN_POINT ( 'NONE',  ( -25.21435515916025594, 1.749597353048488237E-16, -4.373993382621220594E-17 ) ) ;
#11027=B_SPLINE_CURVE_WITH_KNOTS ( 'NONE', 3,
 ( #294, #2595, #13821, #24926, #24497, #13381, #18137, #3043 ),
 .UNSPECIFIED., .F., .F.,
 ( 4, 2, 2, 4 ),
 ( 0.000000000000000000, 0.002761524886576660186, 0.005523049773153320373, 0.01104609954630662340 ),
 .UNSPECIFIED. ) ;
#11032=CARTESIAN_POINT ( 'NONE',  ( -1.046935749539997573, -27.93995161054667875, 36.28605774377793125 ) ) ;
#11035=CARTESIAN_POINT ( 'NONE',  ( -1.539763995773685723, 11.93465967526358185, 44.72359274866469292 ) ) ;
#11040=ORIENTED_EDGE ( 'NONE', *, *, #18793, .F. ) ;
#11052=CYLINDRICAL_SURFACE ( 'NONE', #5566, 37.50000000000001421 ) ;
#11061=ORIENTED_EDGE ( 'NONE', *, *, #4002, .T. ) ;
#11064=CARTESIAN_POINT ( 'NONE',  ( -1.046936909428679341, -27.93981068760648157, -36.28616897897442328 ) ) ;
#11070=CARTESIAN_POINT ( 'NONE',  ( -20.90916690077962770, 27.35210456531415346, 28.59207721780114753 ) ) ;
#11073=CARTESIAN_POINT ( 'NONE',  ( -21.41430102051751305, 25.94791611261640085, 16.60879216503605704 ) ) ;
#11077=DIRECTION ( 'NONE',  ( 1.000000000000000000, -6.938893903907226837E-18, 1.734723475976806709E-18 ) ) ;
#11078=LINE ( 'NONE', #8635, #12125 ) ;
#11090=CARTESIAN_POINT ( 'NONE',  ( -1.056502255334265339, 45.80535052436398047, 0.5104472526221617290 ) ) ;
#11094=DIRECTION ( 'NONE',  ( 0.7563875759206388771, 0.2351350468682867345, -0.6104009704506935252 ) ) ;
#11095=( BOUNDED_SURFACE ( )  B_SPLINE_SURFACE ( 3, 1, ( 
 ( #20004, #1879 ),
 ( #19448, #28216 ),
 ( #8518, #12958 ),
 ( #21753, #15836 ) ),
 .UNSPECIFIED., .F., .F., .F. ) 
 B_SPLINE_SURFACE_WITH_KNOTS ( ( 4, 4 ),
 ( 2, 2 ),
 ( 0.000000000000000000, 1.000000000000000000 ),
 ( 0.000000000000000000, 1.000000000000000000 ),
 .UNSPECIFIED. ) 
 GEOMETRIC_REPRESENTATION_ITEM ( )  RATIONAL_B_SPLINE_SURFACE ( (
 ( 1.000000000000000000, 1.000000000000000000),
 ( 0.9593753223639863714, 0.9995975284513187731),
 ( 0.9593753223639863714, 0.9995975284513187731),
 ( 1.000000000000000000, 1.000000000000000000) ) ) 
 REPRESENTATION_ITEM ( '' )  SURFACE ( )  );
#11101=CARTESIAN_POINT ( 'NONE',  ( -1.056502255334265339, -43.72121397317214786, 13.66916755949895546 ) ) ;
#11105=CARTESIAN_POINT ( 'NONE',  ( -2.904412668506659578, -25.64203923793602868, -40.16685646686200073 ) ) ;
#11113=ORIENTED_EDGE ( 'NONE', *, *, #13247, .T. ) ;
#11115=ADVANCED_FACE ( 'NONE', ( #24824 ), #26894, .F. ) ;
#11137=CARTESIAN_POINT ( 'NONE',  ( -55.24340739397742794, 0.006539691034608862037, 0.007744344507854531226 ) ) ;
#11143=CARTESIAN_POINT ( 'NONE',  ( -55.24271866751342941, -0.001545935011630304593, 0.009369360294295640129 ) ) ;
#11162=CARTESIAN_POINT ( 'NONE',  ( -20.20700224038492721, -27.82980252387826781, -10.08426345511578504 ) ) ;
#11166=CIRCLE ( 'NONE', #27247, 34.60786435723138510 ) ;
#11172=ORIENTED_EDGE ( 'NONE', *, *, #13583, .F. ) ;
#11174=CARTESIAN_POINT ( 'NONE',  ( -1.046936909428682005, -25.87632113675133283, 37.78538189376536849 ) ) ;
#11177=VERTEX_POINT ( 'NONE', #14276 ) ;
#11179=CARTESIAN_POINT ( 'NONE',  ( -1.463510566862831430, 46.14841196428341163, 2.430838777910348192 ) ) ;
#11184=EDGE_CURVE ( 'NONE', #4432, #5699, #3493, .T. ) ;
#11195=CARTESIAN_POINT ( 'NONE',  ( -25.21435515916025594, 1.749597353048488237E-16, -4.373993382621220594E-17 ) ) ;
#11196=CARTESIAN_POINT ( 'NONE',  ( -1.050229599974474404, -0.2556477501656316820, 45.79907399707867199 ) ) ;
#11198=DIRECTION ( 'NONE',  ( 0.000000000000000000, 5.223019709708233256E-21, -1.000000000000000000 ) ) ;
#11201=CARTESIAN_POINT ( 'NONE',  ( -2.911734481061403645, 17.36785190846042681, 44.38410240830284437 ) ) ;
#11203=ORIENTED_EDGE ( 'NONE', *, *, #10064, .T. ) ;
#11205=CARTESIAN_POINT ( 'NONE',  ( -1.050229599974477734, -26.71319688967661676, -37.20249516760164710 ) ) ;
#11206=CARTESIAN_POINT ( 'NONE',  ( -55.24390624410018802, 0.001451500391953283731, -0.01032895241566680888 ) ) ;
#11215=CARTESIAN_POINT ( 'NONE',  ( -21.81686047589425215, 16.72402253294313823, -34.70276904128894557 ) ) ;
#11217=ADVANCED_FACE ( 'NONE', ( #765 ), #9250, .F. ) ;
#11219=CARTESIAN_POINT ( 'NONE',  ( -1.323439229708139431, -43.04565903621273293, 16.42345129173381935 ) ) ;
#11238=DIRECTION ( 'NONE',  ( -6.938893903907226837E-18, -1.000000000000000000, 0.000000000000000000 ) ) ;
#11246=CARTESIAN_POINT ( 'NONE',  ( -4.473127245936434626, -45.82513704981530367, 18.25038884639918280 ) ) ;
#11255=DIRECTION ( 'NONE',  ( -0.7563875759206389882, 0.03500244528123006016, 0.6531865459554675457 ) ) ;
#11261=ORIENTED_EDGE ( 'NONE', *, *, #6532, .F. ) ;
#11264=CARTESIAN_POINT ( 'NONE',  ( -25.21435515916043713, 16.39063784838786475, 30.48034229288620622 ) ) ;
#11269=CARTESIAN_POINT ( 'NONE',  ( -1.050229599974464634, 43.47850826583074735, 14.39582765040416668 ) ) ;
#11279=CARTESIAN_POINT ( 'NONE',  ( -6.574463467970653952, -50.12924290857544918, -11.01561683920031776 ) ) ;
#11283=CARTESIAN_POINT ( 'NONE',  ( -8.786685647604890903, -37.00619870957961410, -38.68584556812286479 ) ) ;
#11291=CARTESIAN_POINT ( 'NONE',  ( -25.21435515916043713, -31.17620025257598471, -15.02493970636134613 ) ) ;
#11295=EDGE_CURVE ( 'NONE', #18231, #6949, #18093, .T. ) ;
#11298=CARTESIAN_POINT ( 'NONE',  ( -28.13707043255157103, 14.07296284901359051, 18.06394523322437706 ) ) ;
#11311=CARTESIAN_POINT ( 'NONE',  ( -25.21435515916043713, -23.92354251275954979, -25.00736669481013053 ) ) ;
#11320=CARTESIAN_POINT ( 'NONE',  ( -1.019300379054419947, -12.21833869579496579, -44.15350047934394695 ) ) ;
#11330=CARTESIAN_POINT ( 'NONE',  ( -20.20612092514785019, -10.22177639105880864, -27.77903665678161360 ) ) ;
#11336=ORIENTED_EDGE ( 'NONE', *, *, #15225, .T. ) ;
#11343=ORIENTED_EDGE ( 'NONE', *, *, #1046, .F. ) ;
#11344=CARTESIAN_POINT ( 'NONE',  ( -1.048996300304501972, -43.31387123529967909, 14.87787369922214076 ) ) ;
#11345=CARTESIAN_POINT ( 'NONE',  ( -55.24340739397742794, -0.007744344507854267548, 0.006539691034608354631 ) ) ;
#11353=CARTESIAN_POINT ( 'NONE',  ( -55.24390624410018802, 0.004572280736703349113, -0.009374879212967143077 ) ) ;
#11373=CARTESIAN_POINT ( 'NONE',  ( -20.57838717382308147, 10.78122205917000365, -27.96569011373090063 ) ) ;
#11381=B_SPLINE_CURVE_WITH_KNOTS ( 'NONE', 3,
 ( #6099, #10281, #23089, #3775, #10127, #9987, #12686, #19038 ),
 .UNSPECIFIED., .F., .F.,
 ( 4, 2, 2, 4 ),
 ( 0.000000000000000000, 0.002761524886576651946, 0.005523049773153303893, 0.01104609954630660952 ),
 .UNSPECIFIED. ) ;
#11383=CARTESIAN_POINT ( 'NONE',  ( -55.25297051322618813, 0.01483298743815085648, 0.001818774723749092123 ) ) ;
#11384=CARTESIAN_POINT ( 'NONE',  ( -20.38016308990357217, -7.753479680700753107, 28.74660391518353109 ) ) ;
#11386=CARTESIAN_POINT ( 'NONE',  ( -55.24390624410018802, -0.004896917417127438256, -0.009209468562451287102 ) ) ;
#11387=CARTESIAN_POINT ( 'NONE',  ( -55.24271866751342941, 0.001425019990779444407, 0.009388511352200054269 ) ) ;
#11388=ORIENTED_EDGE ( 'NONE', *, *, #5697, .F. ) ;
#11392=B_SPLINE_CURVE_WITH_KNOTS ( 'NONE', 3,
 ( #16932, #3541, #27293, #14053, #21249, #19097, #25295, #14185, #23287, #14481 ),
 .UNSPECIFIED., .F., .F.,
 ( 4, 2, 2, 2, 4 ),
 ( 7.961322465290408245E-18, 0.0003346267210630986927, 0.0006692534421261893624, 0.001003880163189280195, 0.001338506884252370919 ),
 .UNSPECIFIED. ) ;
#11393=ORIENTED_EDGE ( 'NONE', *, *, #8471, .F. ) ;
#11398=B_SPLINE_CURVE_WITH_KNOTS ( 'NONE', 3,
 ( #3031, #9645, #9949, #20578, #18711, #27187, #7502, #1157 ),
 .UNSPECIFIED., .F., .F.,
 ( 4, 2, 2, 4 ),
 ( 2.299172327962918193E-16, 0.002761568181852868970, 0.005523136363705508090, 0.01104627272741078720 ),
 .UNSPECIFIED. ) ;
#11399=CARTESIAN_POINT ( 'NONE',  ( -55.24340739397742084, 0.01010924026184365637, 0.0007387096945736542795 ) ) ;
#11404=CARTESIAN_POINT ( 'NONE',  ( -1.050230346682668126, 43.55729751025884156, 14.15335421912537583 ) ) ;
#11415=( BOUNDED_SURFACE ( )  B_SPLINE_SURFACE ( 3, 1, ( 
 ( #17452, #24107 ),
 ( #11137, #17874 ),
 ( #4370, #13143 ),
 ( #26658, #6976 ) ),
 .UNSPECIFIED., .F., .F., .F. ) 
 B_SPLINE_SURFACE_WITH_KNOTS ( ( 4, 4 ),
 ( 2, 2 ),
 ( 0.000000000000000000, 1.000000000000000000 ),
 ( 0.000000000000000000, 1.000000000000000000 ),
 .UNSPECIFIED. ) 
 GEOMETRIC_REPRESENTATION_ITEM ( )  RATIONAL_B_SPLINE_SURFACE ( (
 ( 1.000000000000000000, 1.000000000000000000),
 ( 0.9934239774497837239, 0.8357310067453919133),
 ( 0.9934239774497837239, 0.8357310067453919133),
 ( 1.000000000000000000, 1.000000000000000000) ) ) 
 REPRESENTATION_ITEM ( '' )  SURFACE ( )  );
#11424=ORIENTED_EDGE ( 'NONE', *, *, #3394, .F. ) ;
#11428=LINE ( 'NONE', #9131, #19477 ) ;
#11433=VECTOR ( 'NONE', #4194, 999.9999999999998863 ) ;
#11439=CARTESIAN_POINT ( 'NONE',  ( -1.050229599974470185, -13.90955673306158147, -43.63650726458059381 ) ) ;
#11445=ORIENTED_EDGE ( 'NONE', *, *, #23419, .F. ) ;
#11447=CARTESIAN_POINT ( 'NONE',  ( -1.050231094221210526, -26.71409683968590798, 37.20185272688488709 ) ) ;
#11450=EDGE_CURVE ( 'NONE', #12565, #2306, #15334, .T. ) ;
#11460=EDGE_CURVE ( 'NONE', #28478, #16899, #11931, .T. ) ;
#11476=CARTESIAN_POINT ( 'NONE',  ( -24.53239521893645048, 29.54733954334105661, -16.68574937150984638 ) ) ;
#11478=ORIENTED_EDGE ( 'NONE', *, *, #24590, .T. ) ;
#11480=CARTESIAN_POINT ( 'NONE',  ( -20.47566262905010248, -10.72601569609877536, 27.87687924095557435 ) ) ;
#11483=CARTESIAN_POINT ( 'NONE',  ( -7.733045908741323693, -52.15131830128827062, -5.980865481987962085 ) ) ;
#11484=LINE ( 'NONE', #15949, #9832 ) ;
#11496=CARTESIAN_POINT ( 'NONE',  ( -20.57838717382308147, 29.92853265176831812, -1.611677988432464126 ) ) ;
#11498=ORIENTED_EDGE ( 'NONE', *, *, #6111, .T. ) ;
#11503=EDGE_CURVE ( 'NONE', #20579, #3264, #8134, .T. ) ;
#11506=ADVANCED_FACE ( 'NONE', ( #12491 ), #15108, .F. ) ;
#11508=AXIS2_PLACEMENT_3D ( 'NONE', #21540, #12617, #3852 ) ;
#11511=CARTESIAN_POINT ( 'NONE',  ( -20.20612091757420359, 23.26073043121660433, 18.30568244821352408 ) ) ;
#11514=CONICAL_SURFACE ( 'NONE', #3263, 34.60786435723138510, 0.8559913436420825139 ) ;
#11517=ORIENTED_EDGE ( 'NONE', *, *, #11866, .F. ) ;
#11518=CIRCLE ( 'NONE', #10595, 34.60786435723138510 ) ;
#11522=CARTESIAN_POINT ( 'NONE',  ( -15.02187109954782507, 41.75590530176335591, 20.12219089991046772 ) ) ;
#11530=CARTESIAN_POINT ( 'NONE',  ( -20.20700224038492010, -8.199606986804138131, 28.44216453106544762 ) ) ;
#11537=ORIENTED_EDGE ( 'NONE', *, *, #5500, .T. ) ;
#11538=VECTOR ( 'NONE', #10750, 1000.000000000000114 ) ;
#11539=DIRECTION ( 'NONE',  ( 1.000000000000000000, -6.938893903907226837E-18, 1.734723475976806709E-18 ) ) ;
#11540=CARTESIAN_POINT ( 'NONE',  ( -1.539763995773681060, -2.469814354917172494, 46.22267697748607418 ) ) ;
#11546=CARTESIAN_POINT ( 'NONE',  ( -25.21435515916043713, -31.17620025257576799, 15.02493970636179377 ) ) ;
#11548=CARTESIAN_POINT ( 'NONE',  ( -8.786685647604896232, 52.67761315067299677, 9.545808661480061019 ) ) ;
#11549=CARTESIAN_POINT ( 'NONE',  ( -1.583189561560252701, 2.490696082059875138, -46.33203782964461936 ) ) ;
#11552=AXIS2_PLACEMENT_3D ( 'NONE', #8748, #17515, #15350 ) ;
#11555=DIRECTION ( 'NONE',  ( 0.000000000000000000, 5.223019709708233256E-21, -1.000000000000000000 ) ) ;
#11559=DIRECTION ( 'NONE',  ( -0.7563875759206387661, -0.5078650950445656731, 0.4122509917856767570 ) ) ;
#11560=CARTESIAN_POINT ( 'NONE',  ( -1.056502255334265339, 0.5104472526220019679, -45.80535052436397336 ) ) ;
#11561=LINE ( 'NONE', #26950, #25923 ) ;
#11566=ORIENTED_EDGE ( 'NONE', *, *, #20372, .T. ) ;
#11573=CARTESIAN_POINT ( 'NONE',  ( -16.86833981943421890, -43.51541671545732015, -7.884812276281936150 ) ) ;
#11577=FACE_OUTER_BOUND ( 'NONE', #22910, .T. ) ;
#11591=CARTESIAN_POINT ( 'NONE',  ( -25.21435515916042647, 15.02493970636146692, -31.17620025257592786 ) ) ;
#11606=ADVANCED_FACE ( 'NONE', ( #26151 ), #12900, .T. ) ;
#11608=CARTESIAN_POINT ( 'NONE',  ( -1.045287976400365970, 1.530335034934747318, 45.76855895860941814 ) ) ;
#11611=EDGE_LOOP ( 'NONE', ( #24083, #25854, #7222, #16353 ) ) ;
#11614=VECTOR ( 'NONE', #23645, 999.9999999999998863 ) ;
#11623=ORIENTED_EDGE ( 'NONE', *, *, #24948, .T. ) ;
#11634=CARTESIAN_POINT ( 'NONE',  ( -9.156249394959713683, -24.29252099376526530, -48.78605533024730789 ) ) ;
#11636=VECTOR ( 'NONE', #1495, 1000.000000000000000 ) ;
#11638=CARTESIAN_POINT ( 'NONE',  ( -4.162674018437145129, -47.46216648493545875, 11.82104147411610207 ) ) ;
#11641=DIRECTION ( 'NONE',  ( 1.000000000000000000, -6.938893903907226837E-18, 1.734723475976806709E-18 ) ) ;
#11642=CARTESIAN_POINT ( 'NONE',  ( -1.539760825549692402, -16.63252404870386059, -43.19716078875433851 ) ) ;
#11644=LINE ( 'NONE', #20417, #4181 ) ;
#11648=ORIENTED_EDGE ( 'NONE', *, *, #23883, .F. ) ;
#11652=ORIENTED_EDGE ( 'NONE', *, *, #9631, .T. ) ;
#11663=CARTESIAN_POINT ( 'NONE',  ( -20.20612091757425333, -24.59769958242376120, 16.46550228026422502 ) ) ;
#11666=LINE ( 'NONE', #863, #26947 ) ;
#11670=CARTESIAN_POINT ( 'NONE',  ( -55.24728320129491266, 0.01137345571547128398, 0.009072670231978179414 ) ) ;
#11677=ORIENTED_EDGE ( 'NONE', *, *, #4093, .T. ) ;
#11678=CARTESIAN_POINT ( 'NONE',  ( -1.259920593601978833, 44.39818421957814820, -12.06711544331578168 ) ) ;
#11679=CARTESIAN_POINT ( 'NONE',  ( -1.049819078601898825, -0.5100232645223283789, -45.79653735114490587 ) ) ;
#11683=CARTESIAN_POINT ( 'NONE',  ( -25.21435515916025594, 1.749597353048488237E-16, -4.373993382621220594E-17 ) ) ;
#11688=ORIENTED_EDGE ( 'NONE', *, *, #11460, .T. ) ;
#11695=EDGE_CURVE ( 'NONE', #27740, #6545, #24726, .T. ) ;
#11712=CARTESIAN_POINT ( 'NONE',  ( -1.049817751779871688, -37.35030165458155693, 26.50542916749608580 ) ) ;
#11714=CARTESIAN_POINT ( 'NONE',  ( -8.786685647604890903, -9.545808661480982948, -52.67761315067281913 ) ) ;
#11719=CARTESIAN_POINT ( 'NONE',  ( -1.583189561560255143, 36.01941156322830295, 29.24830400313125267 ) ) ;
#11729=CARTESIAN_POINT ( 'NONE',  ( -55.24271866751342941, -0.008488649505342596782, -0.004256484107795601053 ) ) ;
#11737=CARTESIAN_POINT ( 'NONE',  ( -1.044556982611271279, -1.643392503293034768, -45.76404732357878657 ) ) ;
#11738=EDGE_CURVE ( 'NONE', #20356, #14085, #24278, .T. ) ;
#11741=CARTESIAN_POINT ( 'NONE',  ( -1.619063947482197729, 11.94059994246222622, 44.80407745103770623 ) ) ;
#11748=CARTESIAN_POINT ( 'NONE',  ( -1.155001620486255431, -35.88346938217574689, -28.62773628245655644 ) ) ;
#11759=VERTEX_POINT ( 'NONE', #25281 ) ;
#11760=FACE_OUTER_BOUND ( 'NONE', #18032, .T. ) ;
#11762=ORIENTED_EDGE ( 'NONE', *, *, #17276, .F. ) ;
#11768=EDGE_CURVE ( 'NONE', #19215, #5961, #17026, .T. ) ;
#11776=EDGE_CURVE ( 'NONE', #7508, #976, #14467, .T. ) ;
#11784=CARTESIAN_POINT ( 'NONE',  ( -20.57838717382308147, -10.78122205916981358, 27.96569011373096814 ) ) ;
#11788=LINE ( 'NONE', #5442, #8377 ) ;
#11791=CARTESIAN_POINT ( 'NONE',  ( -20.20700224038492721, 28.44216453106536946, -8.199606986804427677 ) ) ;
#11792=CARTESIAN_POINT ( 'NONE',  ( -1.058473599757830286, -15.81436910992550438, -42.99101666105224240 ) ) ;
#11798=CARTESIAN_POINT ( 'NONE',  ( -21.41427618760448581, 7.777551129310475098, 29.81030852927058206 ) ) ;
#11800=ORIENTED_EDGE ( 'NONE', *, *, #2500, .F. ) ;
#11803=CARTESIAN_POINT ( 'NONE',  ( -1.048172774974307053, -45.78636862970790133, 1.020161070261597303 ) ) ;
#11807=ADVANCED_FACE ( 'NONE', ( #21082 ), #23652, .F. ) ;
#11809=CARTESIAN_POINT ( 'NONE',  ( 0.000000000000000000, 0.000000000000000000, 0.000000000000000000 ) ) ;
#11813=DIRECTION ( 'NONE',  ( -0.7637818620346800147, -0.5345501402766327237, -0.3617919495470695579 ) ) ;
#11816=EDGE_LOOP ( 'NONE', ( #4310, #13955, #21732, #18892 ) ) ;
#11819=CARTESIAN_POINT ( 'NONE',  ( -6.588769196390758864, 51.10255870850473769, 4.956336548259831609 ) ) ;
#11824=VERTEX_POINT ( 'NONE', #3956 ) ;
#11825=CARTESIAN_POINT ( 'NONE',  ( -55.24198130335446422, -0.004276389980779660843, 0.008252882783648829434 ) ) ;
#11844=B_SPLINE_CURVE_WITH_KNOTS ( 'NONE', 3,
 ( #4264, #19383, #6173, #8317, #4126, #13046, #14919, #28292 ),
 .UNSPECIFIED., .F., .F.,
 ( 4, 2, 2, 4 ),
 ( 2.251264292202123005E-16, 0.002761568181852863766, 0.005523136363705502885, 0.01104627272741079413 ),
 .UNSPECIFIED. ) ;
#11845=CARTESIAN_POINT ( 'NONE',  ( -21.81686047589426636, 27.83628745321488296, 26.62923599424938459 ) ) ;
#11857=EDGE_LOOP ( 'NONE', ( #4809, #10329, #14147, #18113 ) ) ;
#11863=EDGE_CURVE ( 'NONE', #243, #12327, #23580, .T. ) ;
#11865=CARTESIAN_POINT ( 'NONE',  ( -20.20700224038492010, 27.82980252387833886, 10.08426345511560207 ) ) ;
#11866=EDGE_CURVE ( 'NONE', #7658, #21416, #209, .T. ) ;
#11870=DIRECTION ( 'NONE',  ( -0.7071067818211355105, 9.150583771627656306E-17, -0.7071067805519596350 ) ) ;
#11884=CARTESIAN_POINT ( 'NONE',  ( -1.259920593601977057, -35.85909937955943860, -28.82601305773640732 ) ) ;
#11887=CARTESIAN_POINT ( 'NONE',  ( -1.463510566862832096, 35.90603835816546763, 29.09194585123793786 ) ) ;
#11888=CARTESIAN_POINT ( 'NONE',  ( -1.539763995773682614, -38.84665165401045073, 25.17088606276588791 ) ) ;
#11892=VECTOR ( 'NONE', #12439, 1000.000000000000000 ) ;
#11894=CARTESIAN_POINT ( 'NONE',  ( -1.539760825549686185, 2.469813586483733392, 46.22267384399377477 ) ) ;
#11896=EDGE_CURVE ( 'NONE', #22323, #24458, #10866, .T. ) ;
#11903=ORIENTED_EDGE ( 'NONE', *, *, #4608, .F. ) ;
#11915=B_SPLINE_CURVE_WITH_KNOTS ( 'NONE', 3,
 ( #8524, #6234, #4615, #13383, #17422, #6360, #22182 ),
 .UNSPECIFIED., .F., .F.,
 ( 4, 3, 4 ),
 ( 1.298148181579757605E-17, 0.009512539173626401862, 0.02506242213020844906 ),
 .UNSPECIFIED. ) ;
#11917=CARTESIAN_POINT ( 'NONE',  ( -1.046936909428679785, 37.78538189376546086, 25.87632113675119427 ) ) ;
#11918=CARTESIAN_POINT ( 'NONE',  ( -20.20700224038492010, -0.9908225410480588913, -29.58392382092672435 ) ) ;
#11920=CARTESIAN_POINT ( 'NONE',  ( -1.056502255334264895, 37.35734037467673119, 26.51074901220462721 ) ) ;
#11923=CARTESIAN_POINT ( 'NONE',  ( -1.239374126674604337, -11.92219841463799135, 44.48112152129359487 ) ) ;
#11924=CARTESIAN_POINT ( 'NONE',  ( -12.82751273423882843, 44.03362901247002981, -21.21958768041810117 ) ) ;
#11931=LINE ( 'NONE', #9784, #975 ) ;
#11939=ORIENTED_EDGE ( 'NONE', *, *, #10371, .T. ) ;
#11942=CARTESIAN_POINT ( 'NONE',  ( -1.048171036023517466, -45.78635789057865679, -1.020520027228972504 ) ) ;
#11943=CARTESIAN_POINT ( 'NONE',  ( -1.048996300304493978, -43.78665266739846373, -13.42280206896960060 ) ) ;
#11965=CARTESIAN_POINT ( 'NONE',  ( -1.539760825549679080, 38.84664866728813593, 25.17088484262099612 ) ) ;
#11967=EDGE_CURVE ( 'NONE', #5205, #25606, #6053, .T. ) ;
#11971=EDGE_CURVE ( 'NONE', #5935, #2087, #10181, .T. ) ;
#11975=CONICAL_SURFACE ( 'NONE', #11508, 34.60786435723138510, 0.8559913436420825139 ) ;
#11986=CARTESIAN_POINT ( 'NONE',  ( -15.02187109954780553, 33.49412687891621232, 32.04062513125082035 ) ) ;
#11991=CIRCLE ( 'NONE', #17919, 34.60786435723138510 ) ;
#11993=CARTESIAN_POINT ( 'NONE',  ( -4.473127245936434626, -26.34600523034507802, 41.70021447285083127 ) ) ;
#11994=B_SPLINE_CURVE_WITH_KNOTS ( 'NONE', 3,
 ( #12343, #10215, #18976, #8056, #23444, #3706, #19797, #2524, #11035, #4544 ),
 .UNSPECIFIED., .F., .F.,
 ( 4, 2, 2, 2, 4 ),
 ( 2.847672227753435151E-16, 0.0003346187017559034554, 0.0006692374035115221994, 0.001003856105267140727, 0.001338474807022759470 ),
 .UNSPECIFIED. ) ;
#11998=EDGE_CURVE ( 'NONE', #3886, #25165, #2378, .T. ) ;
#12004=CARTESIAN_POINT ( 'NONE',  ( -1.050229599974473516, 43.63650726458064355, -13.90955673306141627 ) ) ;
#12006=ORIENTED_EDGE ( 'NONE', *, *, #21785, .T. ) ;
#12007=ORIENTED_EDGE ( 'NONE', *, *, #17438, .T. ) ;
#12015=CARTESIAN_POINT ( 'NONE',  ( -1.031422197589716205, 25.67058493451498080, 37.93675465142445091 ) ) ;
#12024=EDGE_CURVE ( 'NONE', #14776, #17694, #26232, .T. ) ;
#12025=ORIENTED_EDGE ( 'NONE', *, *, #18654, .T. ) ;
#12036=EDGE_CURVE ( 'NONE', #12242, #17470, #13053, .T. ) ;
#12044=CIRCLE ( 'NONE', #28106, 34.60786435723138510 ) ;
#12048=ORIENTED_EDGE ( 'NONE', *, *, #681, .F. ) ;
#12057=CARTESIAN_POINT ( 'NONE',  ( -7.078251931573400491, 50.86685171665412497, -11.16394717458693897 ) ) ;
#12061=ORIENTED_EDGE ( 'NONE', *, *, #6087, .T. ) ;
#12063=EDGE_LOOP ( 'NONE', ( #15500, #25036, #13353, #21827 ) ) ;
#12065=CARTESIAN_POINT ( 'NONE',  ( -1.045287976400383290, -44.00138577190632816, 12.68782741917368106 ) ) ;
#12069=CARTESIAN_POINT ( 'NONE',  ( -20.57838717382308147, -7.715628353033886278, -28.96176188950215646 ) ) ;
#12072=ORIENTED_EDGE ( 'NONE', *, *, #10168, .F. ) ;
#12077=CARTESIAN_POINT ( 'NONE',  ( -1.019300379054419725, -38.21680004809182662, -25.26451264419630860 ) ) ;
#12083=CARTESIAN_POINT ( 'NONE',  ( -21.41427618760447871, 29.81030852927067443, -7.777551129310157130 ) ) ;
#12093=CARTESIAN_POINT ( 'NONE',  ( -55.24198130335446422, -0.004163123460805480056, 0.008310594958150618883 ) ) ;
#12097=CARTESIAN_POINT ( 'NONE',  ( -28.41354790283022069, -14.62505768302813713, -18.00456980371894744 ) ) ;
#12103=CARTESIAN_POINT ( 'NONE',  ( -15.02187109954782862, -41.75590530176324222, -20.12219089991075904 ) ) ;
#12104=CARTESIAN_POINT ( 'NONE',  ( -8.786685647604885574, 6.096987947571466530E-17, -1.524246986892866633E-17 ) ) ;
#12112=CARTESIAN_POINT ( 'NONE',  ( -28.41354790283022069, 8.345538364877384652, 21.64275480268738860 ) ) ;
#12118=CARTESIAN_POINT ( 'NONE',  ( -2.904412668506658246, -40.16685646686189415, 25.64203923793618145 ) ) ;
#12121=CARTESIAN_POINT ( 'NONE',  ( -7.078251931573406708, -11.16394717458641850, 50.86685171665422445 ) ) ;
#12122=CARTESIAN_POINT ( 'NONE',  ( -21.41427618760458884, -28.68857606049974862, -11.22988868156173581 ) ) ;
#12125=VECTOR ( 'NONE', #6769, 1000.000000000000000 ) ;
#12128=EDGE_CURVE ( 'NONE', #12494, #27772, #4797, .T. ) ;
#12129=DIRECTION ( 'NONE',  ( 0.000000000000000000, 5.223019709708233256E-21, -1.000000000000000000 ) ) ;
#12136=CARTESIAN_POINT ( 'NONE',  ( -20.57838717382308147, 18.89542499756533545, 23.26537097894084383 ) ) ;
#12139=CARTESIAN_POINT ( 'NONE',  ( -23.79248802219730052, 24.83956736572410051, -22.01156985585177495 ) ) ;
#12149=CARTESIAN_POINT ( 'NONE',  ( -1.045287976400362417, 25.66401692419989899, -37.92705037016767733 ) ) ;
#12153=ORIENTED_EDGE ( 'NONE', *, *, #27850, .F. ) ;
#12154=VERTEX_POINT ( 'NONE', #12698 ) ;
#12155=ORIENTED_EDGE ( 'NONE', *, *, #22267, .T. ) ;
#12166=CARTESIAN_POINT ( 'NONE',  ( -2.265401668238147259, -43.82493763960398070, -17.02144111536863136 ) ) ;
#12180=CARTESIAN_POINT ( 'NONE',  ( -25.21435515916025594, 1.749597353048488237E-16, -4.373993382621220594E-17 ) ) ;
#12182=ORIENTED_EDGE ( 'NONE', *, *, #6532, .T. ) ;
#12183=CARTESIAN_POINT ( 'NONE',  ( -55.24271866751342941, -0.009388511352199774979, 0.001425019990778928110 ) ) ;
#12184=EDGE_CURVE ( 'NONE', #15111, #21211, #17033, .T. ) ;
#12187=CARTESIAN_POINT ( 'NONE',  ( -22.34422965417125795, 33.39267070835848017, 17.95715691811010828 ) ) ;
#12188=EDGE_CURVE ( 'NONE', #19755, #10995, #21620, .T. ) ;
#12195=LINE ( 'NONE', #27442, #28088 ) ;
#12213=VERTEX_POINT ( 'NONE', #1899 ) ;
#12219=CARTESIAN_POINT ( 'NONE',  ( -12.94347594948481373, -23.08810053288719999, -42.93165645342850212 ) ) ;
#12229=B_SPLINE_CURVE_WITH_KNOTS ( 'NONE', 3,
 ( #13164, #21953, #6710, #12874, #21669, #4679 ),
 .UNSPECIFIED., .F., .F.,
 ( 4, 2, 4 ),
 ( 1.734723475976806902E-18, 0.0004335151646191491353, 0.0008670303292382965359 ),
 .UNSPECIFIED. ) ;
#12231=CARTESIAN_POINT ( 'NONE',  ( -1.056502255334264895, 26.51074901220504643, -37.35734037467642565 ) ) ;
#12232=CARTESIAN_POINT ( 'NONE',  ( -1.048994561756802169, -43.31369460697986540, -14.87838255483240246 ) ) ;
#12240=CARTESIAN_POINT ( 'NONE',  ( -20.37983603106074426, -27.81368274044719868, -10.62371319148630455 ) ) ;
#12241=ORIENTED_EDGE ( 'NONE', *, *, #1846, .F. ) ;
#12242=VERTEX_POINT ( 'NONE', #22195 ) ;
#12253=CARTESIAN_POINT ( 'NONE',  ( -20.20700224038492721, -24.51628800869059432, -16.58740185276701951 ) ) ;
#12261=VERTEX_POINT ( 'NONE', #6805 ) ;
#12264=CARTESIAN_POINT ( 'NONE',  ( -8.786685647604885574, 6.096987947571466530E-17, -1.524246986892866633E-17 ) ) ;
#12265=EDGE_CURVE ( 'NONE', #12820, #10995, #15807, .T. ) ;
#12266=CARTESIAN_POINT ( 'NONE',  ( -8.786685647604885574, 6.096987947571466530E-17, -1.524246986892866633E-17 ) ) ;
#12279=DIRECTION ( 'NONE',  ( 1.000000000000000000, -6.938893903907226837E-18, -5.541455922705464902E-20 ) ) ;
#12284=CARTESIAN_POINT ( 'NONE',  ( -20.24399999263415140, 7.930419334766598993, 28.55700515887712854 ) ) ;
#12292=CARTESIAN_POINT ( 'NONE',  ( -12.82751273423878757, -33.78816682541312844, -35.32125660155435298 ) ) ;
#12295=CARTESIAN_POINT ( 'NONE',  ( -55.24390624410018802, 0.004896917417128144288, 0.009209468562451129242 ) ) ;
#12297=CARTESIAN_POINT ( 'NONE',  ( -2.904412668506655582, -44.35433137608953302, -17.42365698954681719 ) ) ;
#12300=CARTESIAN_POINT ( 'NONE',  ( -8.786685647604896232, 9.545808661481343549, 52.67761315067276229 ) ) ;
#12301=CARTESIAN_POINT ( 'NONE',  ( -4.178947244162533714, -41.47292084251643729, -25.96944194166775333 ) ) ;
#12307=CARTESIAN_POINT ( 'NONE',  ( -28.13707043255157103, 21.52861750560939313, -7.802116958609079056 ) ) ;
#12320=CARTESIAN_POINT ( 'NONE',  ( -1.113548883309555482, -42.96943836789115778, -16.03115934825511957 ) ) ;
#12321=FACE_OUTER_BOUND ( 'NONE', #22959, .T. ) ;
#12327=VERTEX_POINT ( 'NONE', #4628 ) ;
#12339=CARTESIAN_POINT ( 'NONE',  ( -55.24271866751342941, -0.004256484107792937385, -0.008488649505346276131 ) ) ;
#12342=EDGE_LOOP ( 'NONE', ( #23785, #23266, #12619, #10368 ) ) ;
#12343=CARTESIAN_POINT ( 'NONE',  ( -1.045287976400383290, 12.68782741917383738, 44.00138577190627842 ) ) ;
#12345=ORIENTED_EDGE ( 'NONE', *, *, #6565, .F. ) ;
#12348=CARTESIAN_POINT ( 'NONE',  ( -20.20700224038492721, -10.08426345511609235, -27.82980252387815767 ) ) ;
#12356=CARTESIAN_POINT ( 'NONE',  ( -20.57838717382308147, -1.611677988432151709, 29.92853265176832878 ) ) ;
#12357=EDGE_CURVE ( 'NONE', #9135, #8797, #17577, .T. ) ;
#12361=CARTESIAN_POINT ( 'NONE',  ( -55.24390624410018802, 0.009374879212967415429, 0.004572280736702902422 ) ) ;
#12362=CARTESIAN_POINT ( 'NONE',  ( -55.24271866751342941, -0.001425019990781919424, 0.009388511352197656881 ) ) ;
#12364=CARTESIAN_POINT ( 'NONE',  ( -1.050230346682671678, -14.15335421912552860, 43.55729751025877761 ) ) ;
#12368=CARTESIAN_POINT ( 'NONE',  ( -55.25297051322618813, 0.001818774723749727032, -0.01483298743815054943 ) ) ;
#12376=CARTESIAN_POINT ( 'NONE',  ( -1.464342487929860992, 11.94843286121917814, -44.64187261869783896 ) ) ;
#12378=ORIENTED_EDGE ( 'NONE', *, *, #17705, .F. ) ;
#12381=CARTESIAN_POINT ( 'NONE',  ( -20.57838717382308147, -23.26537097894118133, -18.89542499756491978 ) ) ;
#12382=ADVANCED_FACE ( 'NONE', ( #2307 ), #16983, .F. ) ;
#12390=VERTEX_POINT ( 'NONE', #9825 ) ;
#12393=ORIENTED_EDGE ( 'NONE', *, *, #8549, .F. ) ;
#12397=CARTESIAN_POINT ( 'NONE',  ( -55.24728320129491266, 0.01214321324516798306, 0.008013189884950450148 ) ) ;
#12411=CARTESIAN_POINT ( 'NONE',  ( -20.57838717382308147, -10.78122205916981358, 27.96569011373096814 ) ) ;
#12430=VECTOR ( 'NONE', #27515, 999.9999999999998863 ) ;
#12433=( NAMED_UNIT ( * ) SI_UNIT ( $, .STERADIAN. ) SOLID_ANGLE_UNIT ( ) );
#12439=DIRECTION ( 'NONE',  ( 0.7563875759206388771, -0.1685564395263385584, -0.6320336713238493553 ) ) ;
#12446=CARTESIAN_POINT ( 'NONE',  ( -1.539763995773681504, 35.94321074656937753, 29.16712963492422617 ) ) ;
#12449=VERTEX_POINT ( 'NONE', #21315 ) ;
#12463=DIRECTION ( 'NONE',  ( 0.7637818620346800147, -0.5345501402766247301, 0.3617919495470812152 ) ) ;
#12468=EDGE_CURVE ( 'NONE', #21344, #18869, #23685, .T. ) ;
#12472=CARTESIAN_POINT ( 'NONE',  ( -1.045287976400383290, -12.68782741917353185, -44.00138577190637079 ) ) ;
#12475=CARTESIAN_POINT ( 'NONE',  ( -20.21097721712958872, 8.835581498567860237, 28.26295595852175779 ) ) ;
#12479=EDGE_CURVE ( 'NONE', #22454, #5205, #19878, .T. ) ;
#12484=DIRECTION ( 'NONE',  ( 1.000000000000000000, -6.938893903907226837E-18, 1.734723475976806709E-18 ) ) ;
#12489=CARTESIAN_POINT ( 'NONE',  ( -1.048171036023517688, 15.11933492062827966, -43.23005599774305807 ) ) ;
#12491=FACE_OUTER_BOUND ( 'NONE', #1904, .T. ) ;
#12493=CARTESIAN_POINT ( 'NONE',  ( -20.57838717382308147, -1.611677988432151709, 29.92853265176832878 ) ) ;
#12494=VERTEX_POINT ( 'NONE', #19435 ) ;
#12499=CARTESIAN_POINT ( 'NONE',  ( -28.41354790283022069, 21.64275480268759821, 8.345538364876851745 ) ) ;
#12509=VERTEX_POINT ( 'NONE', #19023 ) ;
#12518=CARTESIAN_POINT ( 'NONE',  ( -1.583189561560255143, -25.21827308671260326, -38.94740041318284796 ) ) ;
#12523=CARTESIAN_POINT ( 'NONE',  ( -1.031422197589716205, -12.69107518035472637, 44.01264471863859740 ) ) ;
#12530=CARTESIAN_POINT ( 'NONE',  ( -7.733045908741311258, -38.67583825854175217, -35.49239760110661024 ) ) ;
#12533=B_SPLINE_CURVE_WITH_KNOTS ( 'NONE', 3,
 ( #14194, #7758, #16516, #20681, #4863, #13634 ),
 .UNSPECIFIED., .F., .F.,
 ( 4, 2, 4 ),
 ( 0.000000000000000000, 0.0004335184443140241905, 0.0008670368886280483810 ),
 .UNSPECIFIED. ) ;
#12534=VERTEX_POINT ( 'NONE', #16992 ) ;
#12542=AXIS2_PLACEMENT_3D ( 'NONE', #27753, #14641, #3704 ) ;
#12546=EDGE_CURVE ( 'NONE', #7068, #20579, #2694, .T. ) ;
#12551=CARTESIAN_POINT ( 'NONE',  ( -1.239374126674604337, 28.97829083655439675, -35.79060836339822060 ) ) ;
#12556=CARTESIAN_POINT ( 'NONE',  ( -1.056502255334265339, -45.80535052436398757, -0.5104472526218417627 ) ) ;
#12558=CARTESIAN_POINT ( 'NONE',  ( -19.53423201713129842, 1.550869255229030165E-16, 28.92774122539760384 ) ) ;
#12564=ORIENTED_EDGE ( 'NONE', *, *, #27284, .T. ) ;
#12565=VERTEX_POINT ( 'NONE', #22311 ) ;
#12571=CARTESIAN_POINT ( 'NONE',  ( -1.619063947482201282, 43.26576862488434472, -16.67502769180576649 ) ) ;
#12579=CARTESIAN_POINT ( 'NONE',  ( -1.464342487929857439, 29.09292098541713401, 35.90631960086386698 ) ) ;
#12582=DIRECTION ( 'NONE',  ( 1.000000000000000000, -6.938893903907226837E-18, 1.734723475976806709E-18 ) ) ;
#12589=ORIENTED_EDGE ( 'NONE', *, *, #24803, .T. ) ;
#12591=DIRECTION ( 'NONE',  ( 0.000000000000000000, 5.223019709707975211E-21, -1.000000000000000000 ) ) ;
#12593=ORIENTED_EDGE ( 'NONE', *, *, #11998, .F. ) ;
#12594=( BOUNDED_SURFACE ( )  B_SPLINE_SURFACE ( 3, 1, ( 
 ( #27306, #9345 ),
 ( #2852, #5002 ),
 ( #27160, #25167 ),
 ( #13926, #7187 ) ),
 .UNSPECIFIED., .F., .F., .F. ) 
 B_SPLINE_SURFACE_WITH_KNOTS ( ( 4, 4 ),
 ( 2, 2 ),
 ( 0.000000000000000000, 1.000000000000000000 ),
 ( 0.000000000000000000, 1.000000000000000000 ),
 .UNSPECIFIED. ) 
 GEOMETRIC_REPRESENTATION_ITEM ( )  RATIONAL_B_SPLINE_SURFACE ( (
 ( 1.000000000000000000, 1.000000000000000000),
 ( 0.7789835883360576307, 0.9689951854195403280),
 ( 0.7789835883360576307, 0.9689951854195403280),
 ( 1.000000000000000000, 1.000000000000000000) ) ) 
 REPRESENTATION_ITEM ( '' )  SURFACE ( )  );
#12607=EDGE_CURVE ( 'NONE', #4240, #27443, #3069, .T. ) ;
#12616=CARTESIAN_POINT ( 'NONE',  ( -20.20700224038492010, 27.82980252387833886, 10.08426345511560207 ) ) ;
#12617=DIRECTION ( 'NONE',  ( 1.000000000000000000, -6.938893903907226837E-18, 1.734723475976806709E-18 ) ) ;
#12619=ORIENTED_EDGE ( 'NONE', *, *, #14257, .F. ) ;
#12620=CARTESIAN_POINT ( 'NONE',  ( -25.21435515916043713, -30.48034229288627017, 16.39063784838775462 ) ) ;
#12626=CARTESIAN_POINT ( 'NONE',  ( -25.21435515916043713, 23.92354251275973809, 25.00736669480994934 ) ) ;
#12629=CARTESIAN_POINT ( 'NONE',  ( -55.25719721206881729, -0.007063345920776780730, 0.008651607285660046359 ) ) ;
#12636=ORIENTED_EDGE ( 'NONE', *, *, #58, .T. ) ;
#12637=EDGE_CURVE ( 'NONE', #5935, #12494, #16796, .T. ) ;
#12642=EDGE_CURVE ( 'NONE', #11017, #26529, #19358, .T. ) ;
#12645=CARTESIAN_POINT ( 'NONE',  ( -1.056502255334264895, 0.5104472526226292439, 45.80535052436395915 ) ) ;
#12647=DIRECTION ( 'NONE',  ( 0.7563875759206388771, 0.6531865459554678788, 0.03500244528122787441 ) ) ;
#12658=LINE ( 'NONE', #6618, #4561 ) ;
#12660=CARTESIAN_POINT ( 'NONE',  ( -1.464342487929863212, 43.13914623307960738, -16.57334911911526731 ) ) ;
#12665=CARTESIAN_POINT ( 'NONE',  ( -55.24198130335446422, 0.001391250620105636670, -0.009190321388309047670 ) ) ;
#12671=CARTESIAN_POINT ( 'NONE',  ( -2.904412668506657358, 30.27712468694988601, -36.79926976721460363 ) ) ;
#12675=EDGE_CURVE ( 'NONE', #3917, #23740, #17474, .T. ) ;
#12676=VERTEX_POINT ( 'NONE', #1275 ) ;
#12682=DIRECTION ( 'NONE',  ( 0.000000000000000000, 5.223019709708233256E-21, -1.000000000000000000 ) ) ;
#12683=VERTEX_POINT ( 'NONE', #18560 ) ;
#12686=CARTESIAN_POINT ( 'NONE',  ( -2.911734481061392987, 2.802366807346851285, 47.57875121082947345 ) ) ;
#12690=CARTESIAN_POINT ( 'NONE',  ( -55.24271866751342941, -0.001425019990781919424, 0.009388511352197656881 ) ) ;
#12698=CARTESIAN_POINT ( 'NONE',  ( -25.21435515916043713, -15.02493970636168896, -31.17620025257581062 ) ) ;
#12700=ORIENTED_EDGE ( 'NONE', *, *, #12546, .F. ) ;
#12711=CARTESIAN_POINT ( 'NONE',  ( -22.34422965417122242, 27.39717383755282043, -26.20925041532862920 ) ) ;
#12714=( LENGTH_UNIT ( ) NAMED_UNIT ( * ) SI_UNIT ( .MILLI., .METRE. ) );
#12724=CARTESIAN_POINT ( 'NONE',  ( -1.583189561560253589, -2.490696082060195327, -46.33203782964460515 ) ) ;
#12727=CARTESIAN_POINT ( 'NONE',  ( -28.13707043255157103, 22.88591869784691113, -0.7675454997507807908 ) ) ;
#12728=EDGE_LOOP ( 'NONE', ( #15157, #21173, #4949, #27880 ) ) ;
#12730=EDGE_CURVE ( 'NONE', #987, #15703, #26060, .T. ) ;
#12732=DIRECTION ( 'NONE',  ( 1.000000000000000000, -6.938893903907226837E-18, 1.734723475976806709E-18 ) ) ;
#12738=EDGE_CURVE ( 'NONE', #9533, #28300, #28269, .T. ) ;
#12742=CARTESIAN_POINT ( 'NONE',  ( -55.24271866751342941, 0.001425019990782615698, -0.009388511352197861579 ) ) ;
#12752=CARTESIAN_POINT ( 'NONE',  ( -55.24340739397742084, -0.005344433640972736689, -0.008612749836246649457 ) ) ;
#12757=CARTESIAN_POINT ( 'NONE',  ( -23.77929240705206837, -15.74261278740695502, -32.66578242509739027 ) ) ;
#12773=CARTESIAN_POINT ( 'NONE',  ( -1.259920593601986383, 38.49623866863347388, -25.19630221849063290 ) ) ;
#12777=CARTESIAN_POINT ( 'NONE',  ( -25.21435515916043713, -23.92354251275918031, 25.00736669481048224 ) ) ;
#12781=CARTESIAN_POINT ( 'NONE',  ( -1.583189561560253589, 43.29471907393742214, -16.68617981233717629 ) ) ;
#12786=FACE_OUTER_BOUND ( 'NONE', #16238, .T. ) ;
#12800=CARTESIAN_POINT ( 'NONE',  ( -1.056502255334265339, -14.64009593116072949, 43.40574022158788381 ) ) ;
#12801=CARTESIAN_POINT ( 'NONE',  ( -1.049819825607600121, -37.34982882986862052, -26.50610175068254293 ) ) ;
#12803=EDGE_CURVE ( 'NONE', #21106, #27239, #24706, .T. ) ;
#12809=CARTESIAN_POINT ( 'NONE',  ( -1.050230347699842692, 5.964912479342754695E-15, -45.79907861674080749 ) ) ;
#12812=AXIS2_PLACEMENT_3D ( 'NONE', #13420, #6535, #20044 ) ;
#12820=VERTEX_POINT ( 'NONE', #23846 ) ;
#12831=ORIENTED_EDGE ( 'NONE', *, *, #25225, .F. ) ;
#12832=ORIENTED_EDGE ( 'NONE', *, *, #9862, .F. ) ;
#12836=ORIENTED_EDGE ( 'NONE', *, *, #28375, .T. ) ;
#12840=CARTESIAN_POINT ( 'NONE',  ( -8.786685647604890903, -37.00619870957961410, -38.68584556812286479 ) ) ;
#12843=EDGE_CURVE ( 'NONE', #21851, #8890, #23328, .T. ) ;
#12846=CARTESIAN_POINT ( 'NONE',  ( -7.733045908741337016, 47.75066202881826882, 21.80378472388440514 ) ) ;
#12849=CARTESIAN_POINT ( 'NONE',  ( -1.049817751779889008, 26.50542916749622080, 37.35030165458145746 ) ) ;
#12851=VERTEX_POINT ( 'NONE', #21246 ) ;
#12874=CARTESIAN_POINT ( 'NONE',  ( -20.24399999263415140, 27.76448601145554562, 10.36954246768216059 ) ) ;
#12883=ORIENTED_EDGE ( 'NONE', *, *, #21632, .T. ) ;
#12885=CARTESIAN_POINT ( 'NONE',  ( -1.155031165708874097, 45.85732438018715129, -2.068616213631106593 ) ) ;
#12891=CARTESIAN_POINT ( 'NONE',  ( -1.155001620486246994, 25.28075036143276932, 38.31519699443472859 ) ) ;
#12896=CARTESIAN_POINT ( 'NONE',  ( -28.41354790283022069, 12.60397206714832663, -19.47297445639553715 ) ) ;
#12900=CONICAL_SURFACE ( 'NONE', #7412, 53.53553390275978785, 0.7853981625000051592 ) ;
#12904=STYLED_ITEM('',(#28500),#7750);
#12905=ORIENTED_EDGE ( 'NONE', *, *, #23940, .T. ) ;
#12908=ORIENTED_EDGE ( 'NONE', *, *, #24732, .T. ) ;
#12919=CARTESIAN_POINT ( 'NONE',  ( -1.619063947482194177, -46.30105812165547974, 2.489035965910640247 ) ) ;
#12922=CARTESIAN_POINT ( 'NONE',  ( -55.25719721206881729, 0.002847566758683125598, -0.01079965405819887508 ) ) ;
#12924=VECTOR ( 'NONE', #19077, 1000.000000000000000 ) ;
#12926=DIRECTION ( 'NONE',  ( 1.000000000000000000, -6.938893903907226837E-18, 1.734723475976806709E-18 ) ) ;
#12933=ORIENTED_EDGE ( 'NONE', *, *, #8267, .F. ) ;
#12936=DIRECTION ( 'NONE',  ( 0.000000000000000000, 5.223019709708190374E-21, -1.000000000000000000 ) ) ;
#12943=CARTESIAN_POINT ( 'NONE',  ( -6.574463467970655728, 51.07975593197905795, -5.014313797967199449 ) ) ;
#12958=CARTESIAN_POINT ( 'NONE',  ( -1.056502255334264895, -37.35734037467652513, -26.51074901220491498 ) ) ;
#12961=ORIENTED_EDGE ( 'NONE', *, *, #1235, .T. ) ;
#12970=VECTOR ( 'NONE', #5106, 999.9999999999998863 ) ;
#12973=CARTESIAN_POINT ( 'NONE',  ( -7.733045908741344121, 10.42750254442610114, 51.44704017882764191 ) ) ;
#12979=EDGE_LOOP ( 'NONE', ( #13831, #7340 ) ) ;
#12981=CARTESIAN_POINT ( 'NONE',  ( -28.13707043255157103, -6.342158660426852279, 22.00298671236746273 ) ) ;
#12986=B_SPLINE_CURVE_WITH_KNOTS ( 'NONE', 3,
 ( #2486, #6977, #13423, #11279, #26814, #6689, #15727, #7122 ),
 .UNSPECIFIED., .F., .F.,
 ( 4, 2, 2, 4 ),
 ( 0.000000000000000000, 0.002761524886576652380, 0.005523049773153304760, 0.01104609954630660952 ),
 .UNSPECIFIED. ) ;
#12987=ADVANCED_FACE ( 'NONE', ( #183 ), #19917, .F. ) ;
#12996=EDGE_CURVE ( 'NONE', #25305, #24670, #22968, .T. ) ;
#13003=CARTESIAN_POINT ( 'NONE',  ( -1.045287976400351981, 36.12803364096590997, -28.14015102489844011 ) ) ;
#13004=ORIENTED_EDGE ( 'NONE', *, *, #22614, .F. ) ;
#13012=ORIENTED_EDGE ( 'NONE', *, *, #15755, .T. ) ;
#13014=CIRCLE ( 'NONE', #20365, 12.50000000000000000 ) ;
#13022=CARTESIAN_POINT ( 'NONE',  ( -28.13707043255157103, 22.88591869784691113, 0.7675454997507791255 ) ) ;
#13027=CARTESIAN_POINT ( 'NONE',  ( -55.24340739397742084, 0.003826481709804142178, -0.009386184976286654491 ) ) ;
#13032=CARTESIAN_POINT ( 'NONE',  ( -1.045287976400383290, -36.12803364096628655, -28.14015102489793918 ) ) ;
#13039=CARTESIAN_POINT ( 'NONE',  ( -20.20700224038492721, -29.58392382092672790, 0.9908225410481621420 ) ) ;
#13043=CARTESIAN_POINT ( 'NONE',  ( -1.463510566862821660, 25.15876608740871490, 38.76366072687751796 ) ) ;
#13046=CARTESIAN_POINT ( 'NONE',  ( -6.588769196390762417, 4.956336548259653974, -51.10255870850470217 ) ) ;
#13047=CARTESIAN_POINT ( 'NONE',  ( -2.265401668238149036, 17.02144111536879123, -43.82493763960390254 ) ) ;
#13049=CARTESIAN_POINT ( 'NONE',  ( -1.058197053496171325, 15.81317659443684143, -42.99116279335158453 ) ) ;
#13050=CARTESIAN_POINT ( 'NONE',  ( -7.733045908741342345, 25.81515396910926086, 45.70676731105690749 ) ) ;
#13053=B_SPLINE_CURVE_WITH_KNOTS ( 'NONE', 3,
 ( #13289, #205, #483, #8993, #4664, #13431, #25547, #12004, #18475, #21050, #1064, #18911, #27538 ),
 .UNSPECIFIED., .F., .F.,
 ( 4, 3, 3, 3, 4 ),
 ( 8.673617379884035472E-18, 0.0007657099931970570922, 0.001531419946797920890, 0.002296279302920155134, 0.003061450627205761568 ),
 .UNSPECIFIED. ) ;
#13064=ADVANCED_FACE ( 'NONE', ( #5498 ), #21776, .F. ) ;
#13067=CARTESIAN_POINT ( 'NONE',  ( -1.058473599757806971, -12.47539220917832914, 44.07591602137168252 ) ) ;
#13069=CARTESIAN_POINT ( 'NONE',  ( -1.058473599757834283, 35.99997772736212198, -28.32531354681296420 ) ) ;
#13075=CARTESIAN_POINT ( 'NONE',  ( -25.21435515916025594, 1.749597353048488237E-16, -4.373993382621220594E-17 ) ) ;
#13079=ORIENTED_EDGE ( 'NONE', *, *, #26660, .T. ) ;
#13080=CARTESIAN_POINT ( 'NONE',  ( -20.47566338032520861, -29.82700953060484395, 1.586617869344197018 ) ) ;
#13086=CARTESIAN_POINT ( 'NONE',  ( -23.79223135445719706, -24.83942264280416978, -22.01133905265676916 ) ) ;
#13087=VERTEX_POINT ( 'NONE', #11546 ) ;
#13092=CARTESIAN_POINT ( 'NONE',  ( -1.044556982611267948, -43.01635920718339179, 15.70482750345280820 ) ) ;
#13096=CARTESIAN_POINT ( 'NONE',  ( -20.20997486282892552, 1.395963739018065216E-16, 29.60348406988233450 ) ) ;
#13102=EDGE_LOOP ( 'NONE', ( #7712, #3032, #16416, #10326 ) ) ;
#13103=ADVANCED_FACE ( 'NONE', ( #16741 ), #17724, .F. ) ;
#13104=CARTESIAN_POINT ( 'NONE',  ( -1.031422197589716205, 45.78027046666444733, 1.530725436377623927 ) ) ;
#13107=CARTESIAN_POINT ( 'NONE',  ( -10.86508079875812705, -45.04061326950857591, 24.22249093393325836 ) ) ;
#13108=( BOUNDED_SURFACE ( )  B_SPLINE_SURFACE ( 3, 1, ( 
 ( #24211, #19454 ),
 ( #24351, #4467 ),
 ( #26072, #13242 ),
 ( #6504, #28222 ) ),
 .UNSPECIFIED., .F., .F., .F. ) 
 B_SPLINE_SURFACE_WITH_KNOTS ( ( 4, 4 ),
 ( 2, 2 ),
 ( 0.000000000000000000, 1.000000000000000000 ),
 ( 0.000000000000000000, 1.000000000000000000 ),
 .UNSPECIFIED. ) 
 GEOMETRIC_REPRESENTATION_ITEM ( )  RATIONAL_B_SPLINE_SURFACE ( (
 ( 1.000000000000000000, 1.000000000000000000),
 ( 0.9593753223639863714, 0.9995975284513187731),
 ( 0.9593753223639863714, 0.9995975284513187731),
 ( 1.000000000000000000, 1.000000000000000000) ) ) 
 REPRESENTATION_ITEM ( '' )  SURFACE ( )  );
#13111=DIRECTION ( 'NONE',  ( 1.000000000000000000, -6.938893903907226837E-18, 1.734723475976806709E-18 ) ) ;
#13113=CARTESIAN_POINT ( 'NONE',  ( -55.24271866751342941, 0.006671293903669565407, -0.006757859501006440936 ) ) ;
#13117=CARTESIAN_POINT ( 'NONE',  ( -9.156249394959713683, 25.18996226954615736, -48.32878616081018208 ) ) ;
#13135=FACE_OUTER_BOUND ( 'NONE', #21623, .T. ) ;
#13142=ORIENTED_EDGE ( 'NONE', *, *, #26660, .F. ) ;
#13143=CARTESIAN_POINT ( 'NONE',  ( -1.019300379054419947, 2.023851374322675589, -45.76814864815091255 ) ) ;
#13152=CARTESIAN_POINT ( 'NONE',  ( -25.21435515916025594, 1.749597353048488237E-16, -4.373993382621220594E-17 ) ) ;
#13155=EDGE_CURVE ( 'NONE', #3917, #8101, #22611, .T. ) ;
#13164=CARTESIAN_POINT ( 'NONE',  ( -20.57838717382308147, 27.96569011373101077, 10.78122205916971055 ) ) ;
#13168=CARTESIAN_POINT ( 'NONE',  ( -1.031422197589711987, 12.69107518035501414, -44.01264471863851213 ) ) ;
#13172=CARTESIAN_POINT ( 'NONE',  ( -1.045287976400365970, -25.66401692419961833, 37.92705037016786918 ) ) ;
#13185=CARTESIAN_POINT ( 'NONE',  ( -1.031422197589711764, -12.69107518035532856, -44.01264471863841266 ) ) ;
#13195=CARTESIAN_POINT ( 'NONE',  ( -1.058473599757823846, -45.77379534793241334, 1.755404039369906188 ) ) ;
#13198=CARTESIAN_POINT ( 'NONE',  ( -9.156249394959713683, 48.78605533024740737, -24.29252099376508056 ) ) ;
#13204=EDGE_LOOP ( 'NONE', ( #3403, #18664, #12061, #4943 ) ) ;
#13207=ORIENTED_EDGE ( 'NONE', *, *, #1801, .T. ) ;
#13214=ADVANCED_FACE ( 'NONE', ( #10822 ), #6153, .F. ) ;
#13218=CARTESIAN_POINT ( 'NONE',  ( -25.21435515916025594, 1.749597353048488237E-16, -4.373993382621220594E-17 ) ) ;
#13227=ORIENTED_EDGE ( 'NONE', *, *, #28235, .T. ) ;
#13229=VERTEX_POINT ( 'NONE', #10954 ) ;
#13236=ORIENTED_EDGE ( 'NONE', *, *, #17373, .T. ) ;
#13237=EDGE_CURVE ( 'NONE', #17251, #20822, #27474, .T. ) ;
#13238=DIRECTION ( 'NONE',  ( 0.000000000000000000, 5.223019709708233256E-21, -1.000000000000000000 ) ) ;
#13242=CARTESIAN_POINT ( 'NONE',  ( -1.056502255334264895, -14.64009593116132457, -43.40574022158768486 ) ) ;
#13244=CARTESIAN_POINT ( 'NONE',  ( -55.24728320129491266, 0.003868537197317211632, -0.01402509393918151964 ) ) ;
#13245=CARTESIAN_POINT ( 'NONE',  ( -21.81686047589426636, -27.83628745321466624, -26.62923599424956933 ) ) ;
#13246=CARTESIAN_POINT ( 'NONE',  ( -6.588769196390752647, -26.02756986588571309, -44.25609997968896892 ) ) ;
#13247=EDGE_CURVE ( 'NONE', #12534, #12509, #4604, .T. ) ;
#13255=CLOSED_SHELL ( 'NONE', ( #13734, #24560, #15064, #13610, #5239, #9833, #15513, #3708, #22270, #24950, #10675, #882, #16044, #26327, #26758, #26163, #21169, #20605, #2570, #22238, #21537, #15423, #27465, #5944, #17996, #18522, #11606, #1653, #27949, #20037, #23519, #13064, #2425, #27501, #13486, #27938, #14653, #18598, #6133, #6942, #7643, #14483, #1770, #25159, #18796, #9160, #17725, #28252, #13103, #5903, #20247, #27621, #2998, #27058, #19527, #26317, #18391, #11115, #14186, #1311, #4242, #19715, #10005, #23393, #10095, #8120, #23145, #3612, #13214, #27370, #26067, #19199, #13277, #25792, #18185, #2317, #10568, #16784, #7901, #19061, #19028, #22865, #5968, #19058, #18766, #12987, #8407, #10027, #23593, #20925, #26631, #14881, #5709, #14488, #11217, #21356, #16039, #25299, #16933, #12382, #8918, #22164, #19030, #15004, #2878, #18601, #11807, #17139, #683, #13640, #6861, #9638, #14118, #15438, #164, #2601, #18995, #26835, #11506, #24075, #21030, #6573, #1332, #8504, #4936, #9648, #18303, #980, #17247, #2080, #14832, #20850 ) ) ;
#13257=CARTESIAN_POINT ( 'NONE',  ( -28.41354790283022069, -1.249099604787238249, -23.16239616762930353 ) ) ;
#13258=CARTESIAN_POINT ( 'NONE',  ( -1.031422197589711764, -28.14735071801717226, 36.13727897780157150 ) ) ;
#13277=ADVANCED_FACE ( 'NONE', ( #2439 ), #11095, .F. ) ;
#13279=EDGE_LOOP ( 'NONE', ( #27607, #25107, #14376, #7320 ) ) ;
#13282=CARTESIAN_POINT ( 'NONE',  ( -55.24271866751342941, 0.004365563123935787236, 0.008433070970613791573 ) ) ;
#13288=ORIENTED_EDGE ( 'NONE', *, *, #23880, .F. ) ;
#13289=CARTESIAN_POINT ( 'NONE',  ( -1.045287976400351981, 43.05558670614237116, -15.59869763335110449 ) ) ;
#13291=DIRECTION ( 'NONE',  ( -0.7637818620346800147, -0.6451161201712181104, 0.02150485345384613861 ) ) ;
#13292=ORIENTED_EDGE ( 'NONE', *, *, #12607, .T. ) ;
#13295=ORIENTED_EDGE ( 'NONE', *, *, #18, .F. ) ;
#13301=CARTESIAN_POINT ( 'NONE',  ( -1.045287976400365970, 1.530335034934747318, 45.76855895860941814 ) ) ;
#13309=ORIENTED_EDGE ( 'NONE', *, *, #26437, .T. ) ;
#13311=CARTESIAN_POINT ( 'NONE',  ( -55.24300891470648622, 0.003362556190415182372, -0.009225237711098200136 ) ) ;
#13315=CARTESIAN_POINT ( 'NONE',  ( -55.24728320129491266, -0.008013189884950039019, 0.01214321324516758234 ) ) ;
#13329=ORIENTED_EDGE ( 'NONE', *, *, #17056, .T. ) ;
#13341=EDGE_CURVE ( 'NONE', #6550, #26453, #14418, .T. ) ;
#13343=CARTESIAN_POINT ( 'NONE',  ( -20.20898977204109670, 0.6607022527616891461, -29.59696883073212348 ) ) ;
#13346=CARTESIAN_POINT ( 'NONE',  ( -1.050231094221210526, -27.12595454131532691, -36.90262059116457038 ) ) ;
#13353=ORIENTED_EDGE ( 'NONE', *, *, #11971, .T. ) ;
#13356=DIRECTION ( 'NONE',  ( -0.7563875759206388771, 0.2351350468682910366, 0.6104009704506918599 ) ) ;
#13360=EDGE_LOOP ( 'NONE', ( #26322, #26895, #23223, #17873 ) ) ;
#13363=ORIENTED_EDGE ( 'NONE', *, *, #22167, .F. ) ;
#13364=VERTEX_POINT ( 'NONE', #7504 ) ;
#13365=VERTEX_POINT ( 'NONE', #25064 ) ;
#13371=CONICAL_SURFACE ( 'NONE', #19807, 28.92774122539760384, 0.7853981625000054922 ) ;
#13374=CARTESIAN_POINT ( 'NONE',  ( -7.078251931573400491, -38.93060825814254144, -34.59014398252902112 ) ) ;
#13375=CARTESIAN_POINT ( 'NONE',  ( -25.21435515916043713, -34.29329011225952684, 4.655591116594705703 ) ) ;
#13381=CARTESIAN_POINT ( 'NONE',  ( -4.178947244162636743, -3.367451375481460563, -48.81675275154075422 ) ) ;
#13383=CARTESIAN_POINT ( 'NONE',  ( -15.02187109954783040, -20.12219089991063825, 41.75590530176331328 ) ) ;
#13386=CARTESIAN_POINT ( 'NONE',  ( -28.41354790283022069, -12.60397206714846341, -19.47297445639544833 ) ) ;
#13390=DIRECTION ( 'NONE',  ( 1.000000000000000000, -6.938893903907226837E-18, 1.734723475976806709E-18 ) ) ;
#13395=ORIENTED_EDGE ( 'NONE', *, *, #18214, .T. ) ;
#13397=CARTESIAN_POINT ( 'NONE',  ( -55.24300891470648622, 0.0003472257464250210184, -0.009812809446890590967 ) ) ;
#13402=CARTESIAN_POINT ( 'NONE',  ( -20.20612092514784308, -1.137292630518264680, -29.57813644637189299 ) ) ;
#13407=ORIENTED_EDGE ( 'NONE', *, *, #8382, .F. ) ;
#13410=CARTESIAN_POINT ( 'NONE',  ( -20.21097721712958872, 29.61001327235739566, 0.3305963429843793433 ) ) ;
#13413=VECTOR ( 'NONE', #7400, 1000.000000000000114 ) ;
#13414=CARTESIAN_POINT ( 'NONE',  ( -55.24300891470650754, -0.003362556190412219030, -0.009225237711101438864 ) ) ;
#13419=CARTESIAN_POINT ( 'NONE',  ( -15.02187109954787303, 21.95370994985631086, 40.82269973458213030 ) ) ;
#13420=CARTESIAN_POINT ( 'NONE',  ( -25.21435515916025594, 1.749597353048488237E-16, -4.373993382621220594E-17 ) ) ;
#13423=CARTESIAN_POINT ( 'NONE',  ( -7.711401346138398338, -51.42722225669428582, -10.36923727626100522 ) ) ;
#13431=CARTESIAN_POINT ( 'NONE',  ( -1.050231094221206973, 43.47885872350356351, -14.39477892760314326 ) ) ;
#13432=FACE_OUTER_BOUND ( 'NONE', #1038, .T. ) ;
#13433=AXIS2_PLACEMENT_3D ( 'NONE', #6990, #15740, #14251 ) ;
#13434=EDGE_LOOP ( 'NONE', ( #3370, #3636, #23920, #9912 ) ) ;
#13438=( BOUNDED_SURFACE ( )  B_SPLINE_SURFACE ( 3, 1, ( 
 ( #13113, #21899 ),
 ( #17562, #11101 ),
 ( #8952, #19871 ),
 ( #26352, #161 ) ),
 .UNSPECIFIED., .F., .F., .F. ) 
 B_SPLINE_SURFACE_WITH_KNOTS ( ( 4, 4 ),
 ( 2, 2 ),
 ( 0.000000000000000000, 1.000000000000000000 ),
 ( 0.000000000000000000, 1.000000000000000000 ),
 .UNSPECIFIED. ) 
 GEOMETRIC_REPRESENTATION_ITEM ( )  RATIONAL_B_SPLINE_SURFACE ( (
 ( 1.000000000000000000, 1.000000000000000000),
 ( 0.9593753223639863714, 0.9995975284513187731),
 ( 0.9593753223639863714, 0.9995975284513187731),
 ( 1.000000000000000000, 1.000000000000000000) ) ) 
 REPRESENTATION_ITEM ( '' )  SURFACE ( )  );
#13447=B_SPLINE_CURVE_WITH_KNOTS ( 'NONE', 3,
 ( #26918, #17263, #21450, #5789, #14962, #21310 ),
 .UNSPECIFIED., .F., .F.,
 ( 4, 2, 4 ),
 ( 0.000000000000000000, 0.0004335151646191513579, 0.0008670303292383027159 ),
 .UNSPECIFIED. ) ;
#13455=B_SPLINE_CURVE_WITH_KNOTS ( 'NONE', 3,
 ( #24101, #2050, #17594, #26100, #10991, #4218, #2479 ),
 .UNSPECIFIED., .F., .F.,
 ( 4, 3, 4 ),
 ( 0.000000000000000000, 0.006568092053401780595, 0.02506242213020846640 ),
 .UNSPECIFIED. ) ;
#13456=VECTOR ( 'NONE', #14191, 999.9999999999998863 ) ;
#13459=CARTESIAN_POINT ( 'NONE',  ( -8.786685647604890903, 25.35688121747502066, -47.14957014837363403 ) ) ;
#13464=CARTESIAN_POINT ( 'NONE',  ( -20.20700224038492721, 10.08426345511588984, -27.82980252387822517 ) ) ;
#13483=CARTESIAN_POINT ( 'NONE',  ( -25.21435515916043713, -30.48034229288650820, -16.39063784838731053 ) ) ;
#13486=ADVANCED_FACE ( 'NONE', ( #16550 ), #2073, .F. ) ;
#13496=VERTEX_POINT ( 'NONE', #15214 ) ;
#13497=ORIENTED_EDGE ( 'NONE', *, *, #23327, .F. ) ;
#13500=CARTESIAN_POINT ( 'NONE',  ( -7.078251931573406708, -20.86696228105259365, -47.71415099571797924 ) ) ;
#13502=CARTESIAN_POINT ( 'NONE',  ( -22.34422965417106965, 37.57019010019570260, -5.100074259622762618 ) ) ;
#13504=LINE ( 'NONE', #9056, #21756 ) ;
#13507=CARTESIAN_POINT ( 'NONE',  ( 6.505213034913034000E-17, 4.541450660883840889E-15, -37.50000000000001421 ) ) ;
#13526=CARTESIAN_POINT ( 'NONE',  ( -20.57838717382308147, -18.89542499756482741, 23.26537097894125594 ) ) ;
#13532=CARTESIAN_POINT ( 'NONE',  ( -25.21435515916043713, -30.48034229288627017, 16.39063784838775462 ) ) ;
#13539=DIRECTION ( 'NONE',  ( 0.000000000000000000, 5.223019709707975211E-21, -1.000000000000000000 ) ) ;
#13540=CARTESIAN_POINT ( 'NONE',  ( -20.90916690077964546, -35.64494649500671386, 17.17795951644694341 ) ) ;
#13542=CARTESIAN_POINT ( 'NONE',  ( -20.90916690077966322, -5.322316104228261402, -39.20864005633521998 ) ) ;
#13543=CARTESIAN_POINT ( 'NONE',  ( -1.323439229708135434, 38.58845475799802927, 25.17120723334049970 ) ) ;
#13546=EDGE_CURVE ( 'NONE', #1788, #18960, #4077, .T. ) ;
#13564=CARTESIAN_POINT ( 'NONE',  ( -21.81686047589427702, 18.24499610240089353, 33.92779429964183890 ) ) ;
#13565=CARTESIAN_POINT ( 'NONE',  ( -55.24271866751342941, -0.008488649505342596782, -0.004256484107795601053 ) ) ;
#13567=VERTEX_POINT ( 'NONE', #26443 ) ;
#13571=DIRECTION ( 'NONE',  ( 0.000000000000000000, -5.223019709708190374E-21, 1.000000000000000000 ) ) ;
#13575=ORIENTED_EDGE ( 'NONE', *, *, #25842, .F. ) ;
#13583=EDGE_CURVE ( 'NONE', #8797, #13496, #1725, .T. ) ;
#13587=CARTESIAN_POINT ( 'NONE',  ( -21.41430102051752016, 16.60879216503635547, -25.94791611261620545 ) ) ;
#13589=CARTESIAN_POINT ( 'NONE',  ( -1.046936909428682894, -15.35929614323696413, -43.14407378092988665 ) ) ;
#13590=DIRECTION ( 'NONE',  ( 0.000000000000000000, 5.223019709707975211E-21, -1.000000000000000000 ) ) ;
#13599=CARTESIAN_POINT ( 'NONE',  ( -25.21435515916043357, 16.39063784838743132, -30.48034229288645136 ) ) ;
#13610=ADVANCED_FACE ( 'NONE', ( #26720 ), #10639, .F. ) ;
#13615=ORIENTED_EDGE ( 'NONE', *, *, #24034, .F. ) ;
#13631=ORIENTED_EDGE ( 'NONE', *, *, #10371, .F. ) ;
#13634=CARTESIAN_POINT ( 'NONE',  ( -20.57838717382308502, 23.26537097894105699, -18.89542499756508320 ) ) ;
#13635=ORIENTED_EDGE ( 'NONE', *, *, #9103, .F. ) ;
#13639=CARTESIAN_POINT ( 'NONE',  ( -20.24399999263415140, -10.36954246768226717, 27.76448601145551009 ) ) ;
#13640=ADVANCED_FACE ( 'NONE', ( #4859 ), #77, .F. ) ;
#13642=DIRECTION ( 'NONE',  ( 1.000000000000000000, -6.938893903907226837E-18, 1.734723475976806709E-18 ) ) ;
#13651=CARTESIAN_POINT ( 'NONE',  ( -12.94347594948482083, 21.16159467081353540, -43.91326021875521946 ) ) ;
#13661=CARTESIAN_POINT ( 'NONE',  ( -55.24300891470648622, 0.009439835024157980023, -0.002702093572889658051 ) ) ;
#13677=CARTESIAN_POINT ( 'NONE',  ( -1.583189561560253589, 25.21827308671232259, -38.94740041318303270 ) ) ;
#13679=EDGE_CURVE ( 'NONE', #9661, #14713, #20960, .T. ) ;
#13681=CARTESIAN_POINT ( 'NONE',  ( -1.031422197589711764, -15.60268798220608488, 43.06660437151322895 ) ) ;
#13683=CARTESIAN_POINT ( 'NONE',  ( -8.786685647604890903, 37.00619870957935120, -38.68584556812312059 ) ) ;
#13685=CARTESIAN_POINT ( 'NONE',  ( -20.20700224038492010, -10.08426345511570332, 27.82980252387829623 ) ) ;
#13687=ORIENTED_EDGE ( 'NONE', *, *, #5871, .F. ) ;
#13698=EDGE_CURVE ( 'NONE', #22671, #15612, #12195, .T. ) ;
#13721=ORIENTED_EDGE ( 'NONE', *, *, #12357, .T. ) ;
#13723=VERTEX_POINT ( 'NONE', #3692 ) ;
#13725=( BOUNDED_SURFACE ( )  B_SPLINE_SURFACE ( 3, 1, ( 
 ( #2160, #10831 ),
 ( #17566, #2599 ),
 ( #11383, #26354 ),
 ( #17712, #20156 ) ),
 .UNSPECIFIED., .F., .F., .F. ) 
 B_SPLINE_SURFACE_WITH_KNOTS ( ( 4, 4 ),
 ( 2, 2 ),
 ( 0.000000000000000000, 1.000000000000000000 ),
 ( 0.000000000000000000, 1.000000000000000000 ),
 .UNSPECIFIED. ) 
 GEOMETRIC_REPRESENTATION_ITEM ( )  RATIONAL_B_SPLINE_SURFACE ( (
 ( 1.000000000000000000, 1.000000000000000000),
 ( 0.7789835883360576307, 0.9689951854195403280),
 ( 0.7789835883360576307, 0.9689951854195403280),
 ( 1.000000000000000000, 1.000000000000000000) ) ) 
 REPRESENTATION_ITEM ( '' )  SURFACE ( )  );
#13726=EDGE_LOOP ( 'NONE', ( #7814, #26726, #13721, #23126 ) ) ;
#13727=B_SPLINE_CURVE_WITH_KNOTS ( 'NONE', 3,
 ( #17177, #6255, #19614, #17310, #26099, #6387, #23959 ),
 .UNSPECIFIED., .F., .F.,
 ( 4, 3, 4 ),
 ( 1.734723475976807094E-18, 0.009512539173626382780, 0.02506242213020817150 ),
 .UNSPECIFIED. ) ;
#13734=ADVANCED_FACE ( 'NONE', ( #18529 ), #10341, .T. ) ;
#13735=CARTESIAN_POINT ( 'NONE',  ( -8.259864102781671491, 9.986657004933631399, -52.06232470801713674 ) ) ;
#13740=CARTESIAN_POINT ( 'NONE',  ( -55.24271866751342941, -0.009369360294295350430, -0.001545935011630812216 ) ) ;
#13745=CARTESIAN_POINT ( 'NONE',  ( -1.619063947482197729, -35.99532424477401094, -29.22875152547743838 ) ) ;
#13753=CARTESIAN_POINT ( 'NONE',  ( -1.259972190295304939, 2.243354636026407611, 45.95417440459613800 ) ) ;
#13759=CARTESIAN_POINT ( 'NONE',  ( -22.23226125620943705, -29.33577758406442726, 11.82389163795241593 ) ) ;
#13769=ORIENTED_EDGE ( 'NONE', *, *, #25949, .T. ) ;
#13778=CARTESIAN_POINT ( 'NONE',  ( -1.050230346682684113, 37.05182464822020449, 26.92058491724826297 ) ) ;
#13782=CARTESIAN_POINT ( 'NONE',  ( -8.259864102781492079, -38.68084189741939127, 36.24929574824932388 ) ) ;
#13783=CARTESIAN_POINT ( 'NONE',  ( -55.24271866751342941, 0.006757859501010507128, -0.006671293903668127322 ) ) ;
#13784=CARTESIAN_POINT ( 'NONE',  ( -16.86833981943425087, -31.95666732167541113, 30.57013526701953054 ) ) ;
#13785=CARTESIAN_POINT ( 'NONE',  ( -8.786685647604890903, -52.67761315067279781, 9.545808661481174795 ) ) ;
#13797=CARTESIAN_POINT ( 'NONE',  ( -21.81686047589426991, 37.90526371014259155, -6.867757412720813193 ) ) ;
#13799=CARTESIAN_POINT ( 'NONE',  ( -1.583189561560253589, 44.83405390829688741, 11.94859433442854701 ) ) ;
#13805=CARTESIAN_POINT ( 'NONE',  ( -25.21435515916043713, -34.05351380035337883, -6.169479169075319014 ) ) ;
#13807=VECTOR ( 'NONE', #11870, 1000.000000000000114 ) ;
#13814=CARTESIAN_POINT ( 'NONE',  ( -28.13707043255157103, -7.802116958608856123, 21.52861750560947129 ) ) ;
#13817=AXIS2_PLACEMENT_3D ( 'NONE', #9402, #7683, #18449 ) ;
#13818=EDGE_LOOP ( 'NONE', ( #4670, #7290, #6469, #25188 ) ) ;
#13821=CARTESIAN_POINT ( 'NONE',  ( -7.711401346138398338, -6.030154970217270538, -52.11446537925909439 ) ) ;
#13826=CARTESIAN_POINT ( 'NONE',  ( -1.031422197589716205, 15.60268798220638509, -43.06660437151315080 ) ) ;
#13831=ORIENTED_EDGE ( 'NONE', *, *, #21155, .F. ) ;
#13837=ORIENTED_EDGE ( 'NONE', *, *, #2413, .F. ) ;
#13838=VECTOR ( 'NONE', #21668, 999.9999999999998863 ) ;
#13839=CARTESIAN_POINT ( 'NONE',  ( -1.259920593601972838, -2.243284667987463621, 45.95412615877144447 ) ) ;
#13840=B_SPLINE_CURVE_WITH_KNOTS ( 'NONE', 3,
 ( #22126, #8897, #27403, #16323, #20096, #13483 ),
 .UNSPECIFIED., .F., .F.,
 ( 4, 2, 4 ),
 ( 1.552747097607904257E-16, 0.003570751334075639161, 0.007141502668151123064 ),
 .UNSPECIFIED. ) ;
#13842=CARTESIAN_POINT ( 'NONE',  ( -1.031422197589711987, -36.13727897780105991, 28.14735071801782595 ) ) ;
#13843=DIRECTION ( 'NONE',  ( 0.000000000000000000, 1.000000000000000000, 0.000000000000000000 ) ) ;
#13860=CARTESIAN_POINT ( 'NONE',  ( -55.24390624410018802, -0.009374879212970498032, 0.004572280736701721943 ) ) ;
#13862=CARTESIAN_POINT ( 'NONE',  ( -1.619063947482201282, -11.94059994246191359, -44.80407745103779860 ) ) ;
#13873=B_SPLINE_CURVE_WITH_KNOTS ( 'NONE', 3,
 ( #12616, #8053, #14639, #25602 ),
 .UNSPECIFIED., .F., .F.,
 ( 4, 4 ),
 ( 1.892757412642747770E-16, 0.001982023823822945049 ),
 .UNSPECIFIED. ) ;
#13879=CARTESIAN_POINT ( 'NONE',  ( -25.21435515916025594, 1.749597353048488237E-16, -4.373993382621220594E-17 ) ) ;
#13909=ORIENTED_EDGE ( 'NONE', *, *, #9752, .F. ) ;
#13923=EDGE_LOOP ( 'NONE', ( #1346, #14965, #13309, #23768, #4667, #26570, #18415, #27879, #2235, #27469, #18875, #16045, #15803, #2515, #5131, #1735, #2537, #14900, #17923, #12636, #14507, #8913, #12908, #21049, #7503, #9358, #10585, #15586, #9650, #28396, #2703, #20870, #16589, #9190, #13292, #4732, #11008, #14950, #13236, #24703, #381, #3827, #24635, #8938, #16105, #18618, #7201, #14587, #25546, #22583, #8966, #5347, #21488, #3499, #829, #19427, #14252, #23384, #580, #6213, #23042, #3180, #2938, #12883 ) ) ;
#13926=CARTESIAN_POINT ( 'NONE',  ( -55.25719721206881729, -0.008651607285660899843, 0.007063345920781139223 ) ) ;
#13929=CARTESIAN_POINT ( 'NONE',  ( -55.24198130335446422, -0.006527480770973291720, -0.006617369590172134802 ) ) ;
#13930=CARTESIAN_POINT ( 'NONE',  ( 0.000000000000000000, 0.000000000000000000, 0.000000000000000000 ) ) ;
#13938=CARTESIAN_POINT ( 'NONE',  ( -23.79223135445719706, 32.40779366744838796, -7.157574570129257907 ) ) ;
#13943=CARTESIAN_POINT ( 'NONE',  ( -20.20612091757424267, 16.46550228026431384, 24.59769958242370436 ) ) ;
#13948=EDGE_LOOP ( 'NONE', ( #16875, #3830, #1252, #13909 ) ) ;
#13949=EDGE_LOOP ( 'NONE', ( #16782, #1782, #23342, #13982 ) ) ;
#13951=AXIS2_PLACEMENT_3D ( 'NONE', #22635, #25081, #14110 ) ;
#13953=CARTESIAN_POINT ( 'NONE',  ( -20.38016308990357217, 24.94368798801375675, 16.25718651464953624 ) ) ;
#13954=LINE ( 'NONE', #12097, #26858 ) ;
#13955=ORIENTED_EDGE ( 'NONE', *, *, #26611, .T. ) ;
#13958=LINE ( 'NONE', #25198, #24553 ) ;
#13960=B_SPLINE_CURVE_WITH_KNOTS ( 'NONE', 3,
 ( #567, #9364, #15241, #13096 ),
 .UNSPECIFIED., .F., .F.,
 ( 4, 4 ),
 ( 1.906343156168367839E-16, 0.0009910334943225120648 ),
 .UNSPECIFIED. ) ;
#13974=CARTESIAN_POINT ( 'NONE',  ( -55.24340739397742794, -0.003826481709799693914, -0.009386184976285299672 ) ) ;
#13982=ORIENTED_EDGE ( 'NONE', *, *, #3783, .F. ) ;
#13988=CARTESIAN_POINT ( 'NONE',  ( -20.57838717382308147, -23.26537097894090778, 18.89542499756525729 ) ) ;
#13989=CARTESIAN_POINT ( 'NONE',  ( -15.02187109954795119, 6.234056423739480657, -45.93032478317444856 ) ) ;
#13990=CARTESIAN_POINT ( 'NONE',  ( -1.619063947482197729, -16.67502769180532596, 43.26576862488450104 ) ) ;
#13994=CARTESIAN_POINT ( 'NONE',  ( -23.79223135445719350, 16.82181692922858929, 28.60983116549946814 ) ) ;
#13995=CARTESIAN_POINT ( 'NONE',  ( -1.155031165708884311, -25.28071330859858534, 38.31525684316168423 ) ) ;
#14005=ORIENTED_EDGE ( 'NONE', *, *, #3454, .F. ) ;
#14016=B_SPLINE_CURVE_WITH_KNOTS ( 'NONE', 3,
 ( #14679, #23483, #3748, #21305, #1587, #25776, #6068, #10931, #19695, #4581 ),
 .UNSPECIFIED., .F., .F.,
 ( 4, 2, 2, 2, 4 ),
 ( 2.913600445039318278E-16, 0.0003346187017559067080, 0.0006692374035115219826, 0.001003856105267137474, 0.001338474807022752748 ),
 .UNSPECIFIED. ) ;
#14023=CARTESIAN_POINT ( 'NONE',  ( -9.156249394959706578, -48.78605533024757079, -24.29252099376471818 ) ) ;
#14028=CARTESIAN_POINT ( 'NONE',  ( -25.21435515916044423, -16.39063784838720395, 30.48034229288656505 ) ) ;
#14029=CARTESIAN_POINT ( 'NONE',  ( -55.24271866751342941, 0.009388511352198142604, 0.001425019990782173561 ) ) ;
#14033=B_SPLINE_CURVE_WITH_KNOTS ( 'NONE', 3,
 ( #7659, #18717, #27045, #12103, #16272, #9382, #9811 ),
 .UNSPECIFIED., .F., .F.,
 ( 4, 3, 4 ),
 ( 1.868354362588067661E-17, 0.009512539173626417474, 0.02506242213020845253 ),
 .UNSPECIFIED. ) ;
#14035=CARTESIAN_POINT ( 'NONE',  ( -1.058197053496161999, -36.00048521498973031, -28.32422455455065347 ) ) ;
#14038=CARTESIAN_POINT ( 'NONE',  ( -1.323830074806771506, 46.01435746200691312, 2.318057800980871885 ) ) ;
#14039=CARTESIAN_POINT ( 'NONE',  ( -1.323830074806762402, -38.58891736138512840, 25.17121255494518550 ) ) ;
#14048=ORIENTED_EDGE ( 'NONE', *, *, #19086, .T. ) ;
#14053=CARTESIAN_POINT ( 'NONE',  ( -1.323439229708128106, -44.47813215539053999, -12.01475235539429143 ) ) ;
#14055=CARTESIAN_POINT ( 'NONE',  ( -9.156249394959713683, 24.29252099376560281, 48.78605533024713026 ) ) ;
#14062=EDGE_CURVE ( 'NONE', #23391, #22454, #929, .T. ) ;
#14064=ORIENTED_EDGE ( 'NONE', *, *, #17194, .T. ) ;
#14068=LINE ( 'NONE', #24891, #14845 ) ;
#14072=CARTESIAN_POINT ( 'NONE',  ( -20.20612092514784308, -18.30568145913859368, -23.26073121129629939 ) ) ;
#14077=CARTESIAN_POINT ( 'NONE',  ( -1.323439229708132769, 44.47813215539063947, 12.01475235539399300 ) ) ;
#14083=CARTESIAN_POINT ( 'NONE',  ( -20.20700224038492721, 16.58740185276746359, 24.51628800869029234 ) ) ;
#14085=VERTEX_POINT ( 'NONE', #10541 ) ;
#14087=CARTESIAN_POINT ( 'NONE',  ( -7.733045908741338792, -21.80378472388456501, 47.75066202881817645 ) ) ;
#14088=CARTESIAN_POINT ( 'NONE',  ( -21.41430102051745266, -29.81033373822133470, -7.777552968935644628 ) ) ;
#14091=DIRECTION ( 'NONE',  ( 1.000000000000000000, -6.938893903907226837E-18, 1.734723475976806709E-18 ) ) ;
#14092=VERTEX_POINT ( 'NONE', #11264 ) ;
#14093=CARTESIAN_POINT ( 'NONE',  ( -20.57838717382308147, -25.16001208503093522, 16.28767523336148315 ) ) ;
#14105=CARTESIAN_POINT ( 'NONE',  ( -1.113548883309562587, 44.18588492042589166, -12.28732181966532622 ) ) ;
#14110=DIRECTION ( 'NONE',  ( 0.000000000000000000, 5.223019709707975211E-21, -1.000000000000000000 ) ) ;
#14118=ADVANCED_FACE ( 'NONE', ( #7243 ), #3943, .F. ) ;
#14121=CARTESIAN_POINT ( 'NONE',  ( -1.619063947482197729, -11.94059994246129008, 44.80407745103795492 ) ) ;
#14127=LINE ( 'NONE', #27379, #25327 ) ;
#14128=EDGE_CURVE ( 'NONE', #18960, #27540, #5075, .T. ) ;
#14129=CARTESIAN_POINT ( 'NONE',  ( -20.24399999263416561, 24.70869149526203401, -16.36687688782867411 ) ) ;
#14131=CARTESIAN_POINT ( 'NONE',  ( -1.045287976400365970, -25.66401692419961833, 37.92705037016786918 ) ) ;
#14133=DIRECTION ( 'NONE',  ( -0.7637818620346800147, 0.2198041754873925890, 0.6068965246771022004 ) ) ;
#14137=ORIENTED_EDGE ( 'NONE', *, *, #26722, .F. ) ;
#14147=ORIENTED_EDGE ( 'NONE', *, *, #7038, .T. ) ;
#14162=VERTEX_POINT ( 'NONE', #23326 ) ;
#14165=CARTESIAN_POINT ( 'NONE',  ( -24.53239521893646469, 14.09666242510788337, -30.86654523348667567 ) ) ;
#14172=CARTESIAN_POINT ( 'NONE',  ( -1.045287976400383290, 36.12803364096649972, 28.14015102489766917 ) ) ;
#14176=CIRCLE ( 'NONE', #10084, 37.50000000000001421 ) ;
#14180=EDGE_CURVE ( 'NONE', #25022, #22293, #23318, .T. ) ;
#14182=B_SPLINE_CURVE_WITH_KNOTS ( 'NONE', 3,
 ( #26555, #20216, #6858, #15602 ),
 .UNSPECIFIED., .F., .F.,
 ( 4, 4 ),
 ( 1.906343156168368086E-16, 0.001982023823822943315 ),
 .UNSPECIFIED. ) ;
#14184=( BOUNDED_SURFACE ( )  B_SPLINE_SURFACE ( 3, 1, ( 
 ( #21967, #17641 ),
 ( #8731, #6723 ),
 ( #13315, #21832 ),
 ( #2230, #4694 ) ),
 .UNSPECIFIED., .F., .F., .F. ) 
 B_SPLINE_SURFACE_WITH_KNOTS ( ( 4, 4 ),
 ( 2, 2 ),
 ( 0.000000000000000000, 1.000000000000000000 ),
 ( 0.000000000000000000, 1.000000000000000000 ),
 .UNSPECIFIED. ) 
 GEOMETRIC_REPRESENTATION_ITEM ( )  RATIONAL_B_SPLINE_SURFACE ( (
 ( 1.000000000000000000, 1.000000000000000000),
 ( 0.7789835883360578528, 0.9689951854195403280),
 ( 0.7789835883360578528, 0.9689951854195403280),
 ( 1.000000000000000000, 1.000000000000000000) ) ) 
 REPRESENTATION_ITEM ( '' )  SURFACE ( )  );
#14185=CARTESIAN_POINT ( 'NONE',  ( -1.058473599757822292, -44.07591602137166831, -12.47539220917846237 ) ) ;
#14186=ADVANCED_FACE ( 'NONE', ( #6187 ), #3035, .F. ) ;
#14187=CARTESIAN_POINT ( 'NONE',  ( -1.050231094221219408, 14.39477892760360689, 43.47885872350340009 ) ) ;
#14190=ORIENTED_EDGE ( 'NONE', *, *, #25842, .T. ) ;
#14191=DIRECTION ( 'NONE',  ( -0.7563875759206388771, -0.4122509917856824191, -0.5078650950445610102 ) ) ;
#14194=CARTESIAN_POINT ( 'NONE',  ( -20.20700224038492721, 23.35150625415659320, -18.19058640100232438 ) ) ;
#14198=CARTESIAN_POINT ( 'NONE',  ( -1.049819825607596568, 37.34982882986881236, 26.50610175068227292 ) ) ;
#14200=DIRECTION ( 'NONE',  ( -0.7071067818211355105, 4.902845705138443504E-18, 0.7071067805519596350 ) ) ;
#14201=CARTESIAN_POINT ( 'NONE',  ( -1.239374126674604337, -44.48112152129355934, -11.92219841463812280 ) ) ;
#14207=FACE_OUTER_BOUND ( 'NONE', #19341, .T. ) ;
#14208=CARTESIAN_POINT ( 'NONE',  ( -1.045287976400365970, 15.59869763335068171, -43.05558670614252037 ) ) ;
#14213=ORIENTED_EDGE ( 'NONE', *, *, #16759, .T. ) ;
#14217=ORIENTED_EDGE ( 'NONE', *, *, #11738, .F. ) ;
#14222=CARTESIAN_POINT ( 'NONE',  ( -1.049819825607609225, -45.79654196517396514, 0.5097917909113501844 ) ) ;
#14229=ORIENTED_EDGE ( 'NONE', *, *, #5270, .T. ) ;
#14251=DIRECTION ( 'NONE',  ( -5.541455922705464902E-20, 5.223019709708320524E-21, -1.000000000000000000 ) ) ;
#14252=ORIENTED_EDGE ( 'NONE', *, *, #25554, .T. ) ;
#14257=EDGE_CURVE ( 'NONE', #10864, #7492, #3726, .T. ) ;
#14263=CARTESIAN_POINT ( 'NONE',  ( -55.24271866751342941, -0.008433070970613520956, -0.004365563123939561994 ) ) ;
#14264=CARTESIAN_POINT ( 'NONE',  ( -25.21435515916043713, -25.00736669481004526, 23.92354251275963861 ) ) ;
#14268=DIRECTION ( 'NONE',  ( 0.7637818620346801257, -0.02150485345383945993, 0.6451161201712183324 ) ) ;
#14269=CARTESIAN_POINT ( 'NONE',  ( -1.619063947482197729, 38.92136151114943488, 25.20140673341330739 ) ) ;
#14270=CARTESIAN_POINT ( 'NONE',  ( -22.23342874802668589, 16.78332232459680640, 26.81018246605520972 ) ) ;
#14276=CARTESIAN_POINT ( 'NONE',  ( -8.786685647604898008, 38.68584556812353981, 37.00619870957891777 ) ) ;
#14282=ORIENTED_EDGE ( 'NONE', *, *, #24487, .F. ) ;
#14284=CONICAL_SURFACE ( 'NONE', #22144, 34.60786435723138510, 0.8559913436420825139 ) ;
#14290=ORIENTED_EDGE ( 'NONE', *, *, #6771, .T. ) ;
#14291=B_SPLINE_CURVE_WITH_KNOTS ( 'NONE', 3,
 ( #22987, #27418, #3248, #20938 ),
 .UNSPECIFIED., .F., .F.,
 ( 4, 4 ),
 ( 1.895855152355442610E-16, 0.001982023823822945917 ),
 .UNSPECIFIED. ) ;
#14312=CARTESIAN_POINT ( 'NONE',  ( -55.24340739397742794, 0.01010924026184123470, -0.0007387096945706978770 ) ) ;
#14316=CARTESIAN_POINT ( 'NONE',  ( -21.41427618760458174, 23.81423075802610967, 19.54551635498102158 ) ) ;
#14317=EDGE_LOOP ( 'NONE', ( #11113, #27448, #15409, #15520 ) ) ;
#14331=CARTESIAN_POINT ( 'NONE',  ( -55.25719721206881729, -0.01115102788682980142, -0.0006290797159206544097 ) ) ;
#14348=AXIS2_PLACEMENT_3D ( 'NONE', #10297, #20918, #7999 ) ;
#14357=CARTESIAN_POINT ( 'NONE',  ( -8.786685647604706162, -38.68584556812290032, 37.00619870957955015 ) ) ;
#14363=CARTESIAN_POINT ( 'NONE',  ( -1.583189561560252701, 36.01941156322829585, 29.24830400313125978 ) ) ;
#14364=DIRECTION ( 'NONE',  ( 1.000000000000000000, -6.938893903907226837E-18, 1.734723475976806709E-18 ) ) ;
#14367=ORIENTED_EDGE ( 'NONE', *, *, #17373, .F. ) ;
#14372=CARTESIAN_POINT ( 'NONE',  ( -55.25297051322618813, 0.006313402748433540913, -0.01354497706059917470 ) ) ;
#14376=ORIENTED_EDGE ( 'NONE', *, *, #5270, .F. ) ;
#14378=ORIENTED_EDGE ( 'NONE', *, *, #3783, .T. ) ;
#14380=CARTESIAN_POINT ( 'NONE',  ( -1.048994561756806165, -45.79144455904140898, -0.7655149579821828310 ) ) ;
#14384=CARTESIAN_POINT ( 'NONE',  ( -9.156249394959706578, 48.32878616081010392, -25.18996226954632078 ) ) ;
#14385=ORIENTED_EDGE ( 'NONE', *, *, #23499, .F. ) ;
#14387=B_SPLINE_CURVE_WITH_KNOTS ( 'NONE', 3,
 ( #6761, #28462, #22299, #7051, #15648, #24465, #11483, #2412 ),
 .UNSPECIFIED., .F., .F.,
 ( 4, 2, 2, 4 ),
 ( 2.324173423859648542E-16, 0.002761568181852869404, 0.005523136363705506355, 0.01104627272741079066 ),
 .UNSPECIFIED. ) ;
#14390=CARTESIAN_POINT ( 'NONE',  ( -20.20700224038492721, -18.19058640100206503, 23.35150625415678860 ) ) ;
#14394=CARTESIAN_POINT ( 'NONE',  ( -4.473127245936431073, -26.34600523034567487, -41.70021447285044047 ) ) ;
#14396=CARTESIAN_POINT ( 'NONE',  ( -1.259972190295312267, 12.06706380853692551, -44.39825172539698883 ) ) ;
#14399=CARTESIAN_POINT ( 'NONE',  ( -1.058197053496163109, 1.754224732379551011, -45.77356582045591438 ) ) ;
#14404=CARTESIAN_POINT ( 'NONE',  ( -20.24399999263414429, -23.20123049637379253, -18.44171895251388094 ) ) ;
#14415=( BOUNDED_SURFACE ( )  B_SPLINE_SURFACE ( 3, 1, ( 
 ( #1786, #8853 ),
 ( #17614, #17049 ),
 ( #4512, #10581 ),
 ( #23706, #28221 ) ),
 .UNSPECIFIED., .F., .F., .F. ) 
 B_SPLINE_SURFACE_WITH_KNOTS ( ( 4, 4 ),
 ( 2, 2 ),
 ( 0.000000000000000000, 1.000000000000000000 ),
 ( 0.000000000000000000, 1.000000000000000000 ),
 .UNSPECIFIED. ) 
 GEOMETRIC_REPRESENTATION_ITEM ( )  RATIONAL_B_SPLINE_SURFACE ( (
 ( 1.000000000000000000, 1.000000000000000000),
 ( 0.9934239774497838349, 0.8357310067453913582),
 ( 0.9934239774497838349, 0.8357310067453913582),
 ( 1.000000000000000000, 1.000000000000000000) ) ) 
 REPRESENTATION_ITEM ( '' )  SURFACE ( )  );
#14418=B_SPLINE_CURVE_WITH_KNOTS ( 'NONE', 3,
 ( #14093, #22470, #4756, #2886, #11663, #7350 ),
 .UNSPECIFIED., .F., .F.,
 ( 4, 2, 4 ),
 ( 0.000000000000000000, 0.0004335151646191496774, 0.0008670303292382993549 ),
 .UNSPECIFIED. ) ;
#14426=CARTESIAN_POINT ( 'NONE',  ( -20.20700224038492010, 16.58740185276710832, -24.51628800869052682 ) ) ;
#14438=FACE_OUTER_BOUND ( 'NONE', #7101, .T. ) ;
#14447=ORIENTED_EDGE ( 'NONE', *, *, #4445, .T. ) ;
#14453=CARTESIAN_POINT ( 'NONE',  ( -1.619063947482197729, 29.22875152547757338, -35.99532424477389725 ) ) ;
#14463=CARTESIAN_POINT ( 'NONE',  ( -20.24419206586952313, -16.36655224501349437, 24.70913649113847299 ) ) ;
#14467=LINE ( 'NONE', #19082, #19333 ) ;
#14472=DIRECTION ( 'NONE',  ( 0.000000000000000000, 5.223019709707975211E-21, -1.000000000000000000 ) ) ;
#14473=ORIENTED_EDGE ( 'NONE', *, *, #12468, .T. ) ;
#14477=CARTESIAN_POINT ( 'NONE',  ( -1.045287976400362417, -43.05558670614257721, -15.59869763335051651 ) ) ;
#14478=LINE ( 'NONE', #20821, #6468 ) ;
#14481=CARTESIAN_POINT ( 'NONE',  ( -1.045287976400362417, -44.00138577190658395, -12.68782741917276446 ) ) ;
#14483=ADVANCED_FACE ( 'NONE', ( #26994 ), #25819, .F. ) ;
#14488=ADVANCED_FACE ( 'NONE', ( #11760 ), #8923, .F. ) ;
#14490=CARTESIAN_POINT ( 'NONE',  ( -25.21435515916025594, 1.749597353048488237E-16, -4.373993382621220594E-17 ) ) ;
#14498=CARTESIAN_POINT ( 'NONE',  ( -1.583189561560256253, 44.83405390829688741, 11.94859433442855412 ) ) ;
#14501=CARTESIAN_POINT ( 'NONE',  ( -25.21435515916043713, -6.169479169075696490, -34.05351380035330777 ) ) ;
#14502=CARTESIAN_POINT ( 'NONE',  ( -55.24390624410018802, 0.004572280736702236288, 0.009374879212970765180 ) ) ;
#14507=ORIENTED_EDGE ( 'NONE', *, *, #6034, .T. ) ;
#14508=CARTESIAN_POINT ( 'NONE',  ( -20.20700224038492721, -29.58392382092674211, -0.9908225410477480288 ) ) ;
#14510=CARTESIAN_POINT ( 'NONE',  ( -1.259972190295307382, 44.39825172539712383, 12.06706380853646188 ) ) ;
#14521=CARTESIAN_POINT ( 'NONE',  ( -1.113548883309555704, 38.22628252420811634, -25.34012683631568308 ) ) ;
#14523=CARTESIAN_POINT ( 'NONE',  ( -1.045287976400365970, -45.76855895860942525, 1.530335034934587002 ) ) ;
#14525=CARTESIAN_POINT ( 'NONE',  ( -55.24271866751342941, 0.004365563123939758886, -0.008433070970614048312 ) ) ;
#14535=ORIENTED_EDGE ( 'NONE', *, *, #24418, .F. ) ;
#14540=CARTESIAN_POINT ( 'NONE',  ( -1.619063947482197729, 16.67502769180622835, 43.26576862488415287 ) ) ;
#14542=CARTESIAN_POINT ( 'NONE',  ( -20.20700224038492721, -24.51628800869059432, -16.58740185276701951 ) ) ;
#14543=CARTESIAN_POINT ( 'NONE',  ( -55.24728320129491266, 0.005114031043468944375, -0.01362040845703405695 ) ) ;
#14549=B_SPLINE_CURVE_WITH_KNOTS ( 'NONE', 3,
 ( #684, #9045, #9474, #17801, #16077, #26723 ),
 .UNSPECIFIED., .F., .F.,
 ( 4, 2, 4 ),
 ( 0.000000000000000000, 0.003570751334075638293, 0.007141502668151276587 ),
 .UNSPECIFIED. ) ;
#14550=CARTESIAN_POINT ( 'NONE',  ( -20.20612092514785019, -24.59769888281546102, -16.46550332780518033 ) ) ;
#14571=CARTESIAN_POINT ( 'NONE',  ( -1.049819825607581691, 45.79654196517400777, -0.5097917909110309953 ) ) ;
#14576=CARTESIAN_POINT ( 'NONE',  ( -1.155001620486255209, -44.25209926692301110, 12.20337535396725492 ) ) ;
#14578=CARTESIAN_POINT ( 'NONE',  ( -23.79248802219730052, 30.42578156345387086, -13.25839849636368584 ) ) ;
#14581=( BOUNDED_SURFACE ( )  B_SPLINE_SURFACE ( 3, 1, ( 
 ( #12295, #16473 ),
 ( #25267, #24993 ),
 ( #22690, #18328 ),
 ( #27110, #16185 ) ),
 .UNSPECIFIED., .F., .F., .F. ) 
 B_SPLINE_SURFACE_WITH_KNOTS ( ( 4, 4 ),
 ( 2, 2 ),
 ( 0.000000000000000000, 1.000000000000000000 ),
 ( 0.000000000000000000, 1.000000000000000000 ),
 .UNSPECIFIED. ) 
 GEOMETRIC_REPRESENTATION_ITEM ( )  RATIONAL_B_SPLINE_SURFACE ( (
 ( 1.000000000000000000, 1.000000000000000000),
 ( 0.9934239774497837239, 0.8357310067453919133),
 ( 0.9934239774497837239, 0.8357310067453919133),
 ( 1.000000000000000000, 1.000000000000000000) ) ) 
 REPRESENTATION_ITEM ( '' )  SURFACE ( )  );
#14587=ORIENTED_EDGE ( 'NONE', *, *, #15674, .T. ) ;
#14588=EDGE_CURVE ( 'NONE', #25953, #20961, #17057, .T. ) ;
#14595=CARTESIAN_POINT ( 'NONE',  ( -20.20700224038492365, 23.35150625415685255, 18.19058640100197977 ) ) ;
#14614=LINE ( 'NONE', #23144, #8462 ) ;
#14622=VERTEX_POINT ( 'NONE', #6846 ) ;
#14623=CARTESIAN_POINT ( 'NONE',  ( -16.86833981943426508, 38.94907963570754106, 20.94590537750566028 ) ) ;
#14631=CARTESIAN_POINT ( 'NONE',  ( -55.24390624410018802, -0.004572280736702649152, 0.009374879212966917563 ) ) ;
#14638=CARTESIAN_POINT ( 'NONE',  ( -20.20898968516257810, -0.6607166829021660082, -29.59696826051172280 ) ) ;
#14639=CARTESIAN_POINT ( 'NONE',  ( -20.21097721650787093, 28.26295598655185515, 8.835581399094868615 ) ) ;
#14640=FACE_OUTER_BOUND ( 'NONE', #24859, .T. ) ;
#14641=DIRECTION ( 'NONE',  ( 1.000000000000000000, -6.938893903907226837E-18, 1.734723475976806709E-18 ) ) ;
#14648=CARTESIAN_POINT ( 'NONE',  ( -1.464342487929851222, 44.64187261869797396, 11.94843286121871273 ) ) ;
#14649=CARTESIAN_POINT ( 'NONE',  ( -22.23226125620943705, 20.31044300692207472, 24.24619897613454000 ) ) ;
#14653=ADVANCED_FACE ( 'NONE', ( #22244 ), #9077, .F. ) ;
#14663=CARTESIAN_POINT ( 'NONE',  ( -20.47566262905010603, -7.708089517695397852, -28.85746289809576126 ) ) ;
#14670=CARTESIAN_POINT ( 'NONE',  ( -4.473127245936434626, 49.22197550883368677, -3.196405119333975087 ) ) ;
#14677=DIRECTION ( 'NONE',  ( 1.000000000000000000, -6.938893903907226837E-18, 1.734723475976806709E-18 ) ) ;
#14679=CARTESIAN_POINT ( 'NONE',  ( -1.045287976400362417, 43.05558670614268379, 15.59869763335023229 ) ) ;
#14681=CARTESIAN_POINT ( 'NONE',  ( -1.049817751779888342, 27.33161971822197955, -36.75003908324300994 ) ) ;
#14684=CARTESIAN_POINT ( 'NONE',  ( -1.045287976400362417, -1.530335034933495653, 45.76855895860946788 ) ) ;
#14692=EDGE_CURVE ( 'NONE', #12683, #18593, #23619, .T. ) ;
#14694=ORIENTED_EDGE ( 'NONE', *, *, #25789, .T. ) ;
#14697=CARTESIAN_POINT ( 'NONE',  ( -55.24728320129491266, -0.01214321324516726489, -0.008013189884950557701 ) ) ;
#14699=CARTESIAN_POINT ( 'NONE',  ( -25.21435515916043002, 23.92354251275938992, -25.00736669481030106 ) ) ;
#14706=CARTESIAN_POINT ( 'NONE',  ( -20.20997486282892552, 1.395963739018065216E-16, 29.60348406988233450 ) ) ;
#14713=VERTEX_POINT ( 'NONE', #1936 ) ;
#14720=ORIENTED_EDGE ( 'NONE', *, *, #23794, .T. ) ;
#14722=EDGE_CURVE ( 'NONE', #3497, #20356, #26406, .T. ) ;
#14727=CARTESIAN_POINT ( 'NONE',  ( -8.786685647604885574, 6.096987947571466530E-17, -1.524246986892866633E-17 ) ) ;
#14737=( BOUNDED_SURFACE ( )  B_SPLINE_SURFACE ( 3, 1, ( 
 ( #21903, #13677 ),
 ( #19876, #24081 ),
 ( #24502, #4339 ),
 ( #165, #13117 ) ),
 .UNSPECIFIED., .F., .F., .F. ) 
 B_SPLINE_SURFACE_WITH_KNOTS ( ( 4, 4 ),
 ( 2, 2 ),
 ( 0.000000000000000000, 1.000000000000000000 ),
 ( 0.000000000000000000, 1.000000000000000000 ),
 .UNSPECIFIED. ) 
 GEOMETRIC_REPRESENTATION_ITEM ( )  RATIONAL_B_SPLINE_SURFACE ( (
 ( 1.000000000000000000, 1.000000000000000000),
 ( 0.7789835883360576307, 0.9689951854195403280),
 ( 0.7789835883360576307, 0.9689951854195403280),
 ( 1.000000000000000000, 1.000000000000000000) ) ) 
 REPRESENTATION_ITEM ( '' )  SURFACE ( )  );
#14742=CARTESIAN_POINT ( 'NONE',  ( -1.045287976400365970, 28.14015102489882736, 36.12803364096558312 ) ) ;
#14755=B_SPLINE_CURVE_WITH_KNOTS ( 'NONE', 3,
 ( #9219, #17976, #578, #18131, #14812, #23472 ),
 .UNSPECIFIED., .F., .F.,
 ( 4, 2, 4 ),
 ( 1.447636874611986795E-16, 0.003570751334075636125, 0.007141502668151127400 ),
 .UNSPECIFIED. ) ;
#14767=CARTESIAN_POINT ( 'NONE',  ( -1.045287976400365970, 15.59869763335156101, 43.05558670614217931 ) ) ;
#14776=VERTEX_POINT ( 'NONE', #26964 ) ;
#14777=VERTEX_POINT ( 'NONE', #11865 ) ;
#14803=CARTESIAN_POINT ( 'NONE',  ( -10.86508079875780552, -6.877801422380434460, 50.67624451685642839 ) ) ;
#14807=CARTESIAN_POINT ( 'NONE',  ( -1.050229599974468409, -14.39582765040431944, 43.47850826583067629 ) ) ;
#14809=CARTESIAN_POINT ( 'NONE',  ( -20.20612091757425688, 18.30568244821375501, -23.26073043121635919 ) ) ;
#14812=CARTESIAN_POINT ( 'NONE',  ( -24.53237795827032031, 14.09663893005633284, 30.86653739599985968 ) ) ;
#14813=DIRECTION ( 'NONE',  ( 0.000000000000000000, -1.000000000000000000, 0.000000000000000000 ) ) ;
#14815=ORIENTED_EDGE ( 'NONE', *, *, #17158, .T. ) ;
#14818=CARTESIAN_POINT ( 'NONE',  ( -1.619063947482194177, 29.22875152547808852, 35.99532424477347092 ) ) ;
#14819=CARTESIAN_POINT ( 'NONE',  ( -1.155031165708876317, 16.13806347973058664, 42.97366960678581194 ) ) ;
#14820=CARTESIAN_POINT ( 'NONE',  ( -8.786685647604890903, 38.68584556812300690, -37.00619870957947910 ) ) ;
#14824=CARTESIAN_POINT ( 'NONE',  ( -1.046936909428678675, 25.87632113675161349, -37.78538189376516954 ) ) ;
#14832=ADVANCED_FACE ( 'NONE', ( #11577 ), #643, .T. ) ;
#14837=ORIENTED_EDGE ( 'NONE', *, *, #9501, .F. ) ;
#14843=AXIS2_PLACEMENT_3D ( 'NONE', #8465, #21548, #4268 ) ;
#14845=VECTOR ( 'NONE', #14200, 1000.000000000000114 ) ;
#14859=CARTESIAN_POINT ( 'NONE',  ( -1.463510566862838091, -44.64091840826481672, 11.94877850058549029 ) ) ;
#14862=CARTESIAN_POINT ( 'NONE',  ( -4.178947244162637631, -25.96944194166761832, 41.47292084251660782 ) ) ;
#14871=ORIENTED_EDGE ( 'NONE', *, *, #2568, .T. ) ;
#14874=CARTESIAN_POINT ( 'NONE',  ( -20.47566338032527966, 27.87687989047307013, -10.72601609985035331 ) ) ;
#14880=CARTESIAN_POINT ( 'NONE',  ( -1.048994561756802391, 26.29622118251734619, 37.49601524795380669 ) ) ;
#14881=ADVANCED_FACE ( 'NONE', ( #24523 ), #18485, .F. ) ;
#14883=ORIENTED_EDGE ( 'NONE', *, *, #1268, .T. ) ;
#14893=ORIENTED_EDGE ( 'NONE', *, *, #24199, .T. ) ;
#14898=ORIENTED_EDGE ( 'NONE', *, *, #14180, .T. ) ;
#14900=ORIENTED_EDGE ( 'NONE', *, *, #11503, .T. ) ;
#14902=( BOUNDED_SURFACE ( )  B_SPLINE_SURFACE ( 3, 1, ( 
 ( #26500, #8963 ),
 ( #2754, #17855 ),
 ( #13397, #453 ),
 ( #18001, #13258 ) ),
 .UNSPECIFIED., .F., .F., .F. ) 
 B_SPLINE_SURFACE_WITH_KNOTS ( ( 4, 4 ),
 ( 2, 2 ),
 ( 0.000000000000000000, 1.000000000000000000 ),
 ( 0.000000000000000000, 1.000000000000000000 ),
 .UNSPECIFIED. ) 
 GEOMETRIC_REPRESENTATION_ITEM ( )  RATIONAL_B_SPLINE_SURFACE ( (
 ( 1.000000000000000000, 1.000000000000000000),
 ( 0.9934239774497837239, 0.8357310067453919133),
 ( 0.9934239774497837239, 0.8357310067453919133),
 ( 1.000000000000000000, 1.000000000000000000) ) ) 
 REPRESENTATION_ITEM ( '' )  SURFACE ( )  );
#14914=VERTEX_POINT ( 'NONE', #23225 ) ;
#14915=CARTESIAN_POINT ( 'NONE',  ( -8.786685647604892679, -53.04920435127177569, 7.199674155859498548 ) ) ;
#14916=CARTESIAN_POINT ( 'NONE',  ( -18.41936578851709783, -29.33493038358050242, 30.66520733838684265 ) ) ;
#14918=CARTESIAN_POINT ( 'NONE',  ( -5.986830583229481917, -46.64941882410784757, 19.95149887249902321 ) ) ;
#14919=CARTESIAN_POINT ( 'NONE',  ( -7.733045908741336127, 5.980865481988145937, -52.15131830128824220 ) ) ;
#14923=ORIENTED_EDGE ( 'NONE', *, *, #1536, .F. ) ;
#14928=CARTESIAN_POINT ( 'NONE',  ( -55.24728320129491266, -0.01453410071985230222, 0.0006547948648737443372 ) ) ;
#14939=FACE_OUTER_BOUND ( 'NONE', #7782, .T. ) ;
#14944=CARTESIAN_POINT ( 'NONE',  ( -55.24390624410018802, -0.007245494385991098352, -0.007503127514281985981 ) ) ;
#14945=VECTOR ( 'NONE', #16472, 1000.000000000000114 ) ;
#14946=CARTESIAN_POINT ( 'NONE',  ( -8.786685647604890903, -9.545808661480235102, 52.67761315067295413 ) ) ;
#14948=CARTESIAN_POINT ( 'NONE',  ( -1.323830074806773283, -46.01435746200692023, -2.318057800980537930 ) ) ;
#14950=ORIENTED_EDGE ( 'NONE', *, *, #581, .T. ) ;
#14951=VERTEX_POINT ( 'NONE', #3768 ) ;
#14959=CARTESIAN_POINT ( 'NONE',  ( -20.57838717382308147, -1.611677988432568709, -29.92853265176830746 ) ) ;
#14962=CARTESIAN_POINT ( 'NONE',  ( -20.20612091757422846, -18.30568244821359869, 23.26073043121652262 ) ) ;
#14963=CARTESIAN_POINT ( 'NONE',  ( -1.050231094221220296, -37.20185272688478051, -26.71409683968603588 ) ) ;
#14965=ORIENTED_EDGE ( 'NONE', *, *, #28413, .T. ) ;
#14969=ORIENTED_EDGE ( 'NONE', *, *, #25536, .F. ) ;
#14986=CARTESIAN_POINT ( 'NONE',  ( -55.24728320129491266, -0.009072670231977940022, 0.01137345571547076703 ) ) ;
#14988=CARTESIAN_POINT ( 'NONE',  ( -2.911734481061404090, 40.13920818157116344, 25.69892591260225245 ) ) ;
#14991=CARTESIAN_POINT ( 'NONE',  ( -25.21435515916043002, 31.17620025257588523, -15.02493970636157705 ) ) ;
#15004=ADVANCED_FACE ( 'NONE', ( #4598 ), #16470, .F. ) ;
#15005=CARTESIAN_POINT ( 'NONE',  ( -20.57838717382308502, 27.96569011373086866, -10.78122205917010135 ) ) ;
#15010=CARTESIAN_POINT ( 'NONE',  ( -1.045287976400386842, 37.92705037016744285, -25.66401692420027203 ) ) ;
#15013=EDGE_LOOP ( 'NONE', ( #8600, #7319, #311, #13837 ) ) ;
#15015=FACE_BOUND ( 'NONE', #6377, .T. ) ;
#15023=DIRECTION ( 'NONE',  ( 1.000000000000000000, -6.938893903907226837E-18, 1.734723475976806709E-18 ) ) ;
#15024=ORIENTED_EDGE ( 'NONE', *, *, #21460, .T. ) ;
#15047=CARTESIAN_POINT ( 'NONE',  ( -1.259920593601967287, 25.19630221849107343, 38.49623866863322519 ) ) ;
#15048=CARTESIAN_POINT ( 'NONE',  ( -8.786685647604890903, 47.14957014837354876, -25.35688121747519119 ) ) ;
#15051=CARTESIAN_POINT ( 'NONE',  ( -21.41427618760457818, -25.94789270595494202, 16.60878262545447726 ) ) ;
#15057=CARTESIAN_POINT ( 'NONE',  ( -55.24300891470648622, 0.007734635432133147095, 0.006048736206180498759 ) ) ;
#15062=ORIENTED_EDGE ( 'NONE', *, *, #4965, .F. ) ;
#15063=CARTESIAN_POINT ( 'NONE',  ( -1.155001620486265645, 38.31519699443499150, -25.28075036143234300 ) ) ;
#15064=ADVANCED_FACE ( 'NONE', ( #10820 ), #21158, .T. ) ;
#15065=LINE ( 'NONE', #1978, #23950 ) ;
#15069=CARTESIAN_POINT ( 'NONE',  ( -25.21435515916025594, 34.29329011225976842, -4.655591116594504086 ) ) ;
#15075=CARTESIAN_POINT ( 'NONE',  ( -1.048994561756789734, -0.7655149579820232919, 45.79144455904142319 ) ) ;
#15076=DIRECTION ( 'NONE',  ( 1.000000000000000000, -6.938893903907226837E-18, 1.734723475976806709E-18 ) ) ;
#15077=CARTESIAN_POINT ( 'NONE',  ( -20.57838717382308147, -1.611677988432151709, 29.92853265176832878 ) ) ;
#15079=CARTESIAN_POINT ( 'NONE',  ( -25.21435515916043713, -6.169479169075696490, -34.05351380035330777 ) ) ;
#15085=CARTESIAN_POINT ( 'NONE',  ( -8.259864102781673267, 38.68084189741949785, -36.24929574824924572 ) ) ;
#15086=CARTESIAN_POINT ( 'NONE',  ( -10.86508079875786414, -50.32133009257452727, 9.118642906269784021 ) ) ;
#15087=B_SPLINE_CURVE_WITH_KNOTS ( 'NONE', 3,
 ( #14028, #22547, #16047, #508, #655, #9443, #20647 ),
 .UNSPECIFIED., .F., .F.,
 ( 4, 3, 4 ),
 ( 0.000000000000000000, 0.006568092053401791003, 0.02506242213020846987 ),
 .UNSPECIFIED. ) ;
#15088=CARTESIAN_POINT ( 'NONE',  ( -55.24271866751342941, 0.008488649505343330570, 0.004256484107795472684 ) ) ;
#15098=ORIENTED_EDGE ( 'NONE', *, *, #28078, .F. ) ;
#15108=( BOUNDED_SURFACE ( )  B_SPLINE_SURFACE ( 3, 1, ( 
 ( #21126, #7779 ),
 ( #16533, #23452 ),
 ( #5449, #27320 ),
 ( #1411, #14363 ) ),
 .UNSPECIFIED., .F., .F., .F. ) 
 B_SPLINE_SURFACE_WITH_KNOTS ( ( 4, 4 ),
 ( 2, 2 ),
 ( 0.000000000000000000, 1.000000000000000000 ),
 ( 0.000000000000000000, 1.000000000000000000 ),
 .UNSPECIFIED. ) 
 GEOMETRIC_REPRESENTATION_ITEM ( )  RATIONAL_B_SPLINE_SURFACE ( (
 ( 1.000000000000000000, 1.000000000000000000),
 ( 0.7789835883360578528, 0.9689951854195403280),
 ( 0.7789835883360578528, 0.9689951854195403280),
 ( 1.000000000000000000, 1.000000000000000000) ) ) 
 REPRESENTATION_ITEM ( '' )  SURFACE ( )  );
#15111=VERTEX_POINT ( 'NONE', #18123 ) ;
#15114=CARTESIAN_POINT ( 'NONE',  ( -20.57838717382308502, 28.96176188950218844, -7.715628353033780584 ) ) ;
#15127=ORIENTED_EDGE ( 'NONE', *, *, #11768, .T. ) ;
#15137=CARTESIAN_POINT ( 'NONE',  ( -8.786685647604898008, 38.68584556812353981, 37.00619870957891777 ) ) ;
#15141=ORIENTED_EDGE ( 'NONE', *, *, #20827, .T. ) ;
#15146=B_SPLINE_CURVE_WITH_KNOTS ( 'NONE', 3,
 ( #17243, #21714, #15212, #26441, #250, #8613 ),
 .UNSPECIFIED., .F., .F.,
 ( 4, 2, 4 ),
 ( 0.000000000000000000, 0.0004335184443140220763, 0.0008670368886280441527 ),
 .UNSPECIFIED. ) ;
#15148=CARTESIAN_POINT ( 'NONE',  ( -25.21435515916043357, -16.39063784838764093, -30.48034229288631991 ) ) ;
#15149=CARTESIAN_POINT ( 'NONE',  ( -1.056502255334265339, -37.35734037467615565, 26.51074901220544433 ) ) ;
#15157=ORIENTED_EDGE ( 'NONE', *, *, #17473, .T. ) ;
#15159=DIRECTION ( 'NONE',  ( -1.000000000000000000, 6.938893903907226837E-18, -1.734723475976806709E-18 ) ) ;
#15165=ORIENTED_EDGE ( 'NONE', *, *, #5092, .T. ) ;
#15175=PRODUCT ( 'pinion', 'pinion', '', ( #27292 ) ) ;
#15182=FACE_OUTER_BOUND ( 'NONE', #854, .T. ) ;
#15183=CARTESIAN_POINT ( 'NONE',  ( -1.113548883309539272, 25.34012683631610940, 38.22628252420783213 ) ) ;
#15185=CARTESIAN_POINT ( 'NONE',  ( -1.031422197589711764, -37.93675465142452907, 25.67058493451483514 ) ) ;
#15191=CARTESIAN_POINT ( 'NONE',  ( -4.162674018437144241, 25.90909455705170217, 41.48630000627025538 ) ) ;
#15192=EDGE_CURVE ( 'NONE', #2685, #21851, #9157, .T. ) ;
#15206=CARTESIAN_POINT ( 'NONE',  ( -1.155031165708881202, -12.20332162035433576, 44.25214473648924951 ) ) ;
#15208=DIRECTION ( 'NONE',  ( 0.7563875759206387661, 0.5490129373055256945, -0.3556158456312918936 ) ) ;
#15212=CARTESIAN_POINT ( 'NONE',  ( -20.24419206586953379, 28.55732805495827265, 7.929973069813099684 ) ) ;
#15214=CARTESIAN_POINT ( 'NONE',  ( -25.21435515916043002, -4.655591116594591128, -34.29329011225954105 ) ) ;
#15222=ORIENTED_EDGE ( 'NONE', *, *, #9408, .T. ) ;
#15225=EDGE_CURVE ( 'NONE', #27772, #25254, #6051, .T. ) ;
#15231=ORIENTED_EDGE ( 'NONE', *, *, #18152, .T. ) ;
#15232=CARTESIAN_POINT ( 'NONE',  ( -5.986830583229486358, 50.53158596890444443, -4.559539818181313819 ) ) ;
#15233=CARTESIAN_POINT ( 'NONE',  ( -4.178947244162637631, -11.88256963646706410, 47.46809051147732816 ) ) ;
#15240=CARTESIAN_POINT ( 'NONE',  ( -4.162674018437131807, -37.46098494546610880, -31.44946543094281921 ) ) ;
#15241=CARTESIAN_POINT ( 'NONE',  ( -20.20997486282892552, -0.3303743256173646836, 29.60348406988233450 ) ) ;
#15243=EDGE_LOOP ( 'NONE', ( #20978, #24457, #12589, #19698 ) ) ;
#15246=CARTESIAN_POINT ( 'NONE',  ( -20.20700224038492721, 28.44216453106536946, -8.199606986804427677 ) ) ;
#15247=CARTESIAN_POINT ( 'NONE',  ( -8.786685647604885574, 6.096987947571466530E-17, -1.524246986892866633E-17 ) ) ;
#15260=LINE ( 'NONE', #13386, #11433 ) ;
#15261=CARTESIAN_POINT ( 'NONE',  ( -20.47566338032515887, -7.708089572830225222, 28.85746366088577375 ) ) ;
#15267=DIRECTION ( 'NONE',  ( 1.000000000000000000, -6.938893903907226837E-18, 1.734723475976806709E-18 ) ) ;
#15271=ORIENTED_EDGE ( 'NONE', *, *, #20228, .F. ) ;
#15280=LINE ( 'NONE', #23821, #11636 ) ;
#15284=CARTESIAN_POINT ( 'NONE',  ( -4.162674018437137136, 37.46098494546635038, 31.44946543094254920 ) ) ;
#15286=CARTESIAN_POINT ( 'NONE',  ( -7.078251931573400491, 51.82710018979476274, 5.101176922830847893 ) ) ;
#15297=CIRCLE ( 'NONE', #21306, 28.92774122539760384 ) ;
#15303=VERTEX_POINT ( 'NONE', #10498 ) ;
#15305=VERTEX_POINT ( 'NONE', #19266 ) ;
#15308=B_SPLINE_CURVE_WITH_KNOTS ( 'NONE', 3,
 ( #20200, #9283, #2794, #9134, #11573, #26679, #20353 ),
 .UNSPECIFIED., .F., .F.,
 ( 4, 3, 4 ),
 ( 0.000000000000000000, 0.006568092053401769319, 0.02506242213020846987 ),
 .UNSPECIFIED. ) ;
#15310=CARTESIAN_POINT ( 'NONE',  ( -1.239374126674604337, 42.99367564261279995, -16.50008610789313934 ) ) ;
#15319=B_SPLINE_CURVE_WITH_KNOTS ( 'NONE', 3,
 ( #9526, #5343, #15696, #27062, #22489, #24507 ),
 .UNSPECIFIED., .F., .F.,
 ( 4, 2, 4 ),
 ( 0.000000000000000000, 0.003570751334075635258, 0.007141502668151270515 ),
 .UNSPECIFIED. ) ;
#15320=CARTESIAN_POINT ( 'NONE',  ( -1.045287976400383290, 12.68782741917383738, 44.00138577190627842 ) ) ;
#15329=CARTESIAN_POINT ( 'NONE',  ( -1.239374126674604337, -38.61989855450920572, 25.08410696974284448 ) ) ;
#15334=B_SPLINE_CURVE_WITH_KNOTS ( 'NONE', 3,
 ( #3151, #2867, #15955, #8808, #993, #16097 ),
 .UNSPECIFIED., .F., .F.,
 ( 4, 2, 4 ),
 ( 0.000000000000000000, 0.0004335184443140221305, 0.0008670368886280442611 ),
 .UNSPECIFIED. ) ;
#15343=CARTESIAN_POINT ( 'NONE',  ( -1.239374126674604337, -11.92219841463861130, -44.48112152129341013 ) ) ;
#15350=DIRECTION ( 'NONE',  ( 0.000000000000000000, 5.223019709707975211E-21, -1.000000000000000000 ) ) ;
#15365=VERTEX_POINT ( 'NONE', #15069 ) ;
#15369=CARTESIAN_POINT ( 'NONE',  ( -2.911734481061421853, 36.84482841982651280, -30.23325065583374638 ) ) ;
#15370=B_SPLINE_CURVE_WITH_KNOTS ( 'NONE', 3,
 ( #3433, #20849, #7627, #3146, #20977, #7919, #22593 ),
 .UNSPECIFIED., .F., .F.,
 ( 4, 3, 4 ),
 ( 0.000000000000000000, 0.006568092053401790135, 0.02506242213020846640 ),
 .UNSPECIFIED. ) ;
#15373=CARTESIAN_POINT ( 'NONE',  ( -25.21435515916043713, 23.92354251275973809, 25.00736669480994934 ) ) ;
#15376=CARTESIAN_POINT ( 'NONE',  ( -55.25297051322618813, -0.001818774723748856851, 0.01483298743815036902 ) ) ;
#15378=CARTESIAN_POINT ( 'NONE',  ( -20.20700224038492721, -27.82980252387826781, -10.08426345511578504 ) ) ;
#15388=B_SPLINE_CURVE_WITH_KNOTS ( 'NONE', 3,
 ( #12620, #17226, #25607, #26013, #15051, #23874 ),
 .UNSPECIFIED., .F., .F.,
 ( 4, 2, 4 ),
 ( 3.681866292528241208E-16, 0.003576372551511175675, 0.007152745103021982721 ),
 .UNSPECIFIED. ) ;
#15394=CARTESIAN_POINT ( 'NONE',  ( -1.583189561560252701, -36.01941156322808268, -29.24830400313153334 ) ) ;
#15403=CARTESIAN_POINT ( 'NONE',  ( -1.583189561560255143, 29.24830400313165413, -36.01941156322797610 ) ) ;
#15409=ORIENTED_EDGE ( 'NONE', *, *, #9554, .F. ) ;
#15412=ORIENTED_EDGE ( 'NONE', *, *, #18312, .T. ) ;
#15423=ADVANCED_FACE ( 'NONE', ( #18189 ), #7862, .T. ) ;
#15427=CARTESIAN_POINT ( 'NONE',  ( -1.046936909428696438, 36.28616897897453697, -27.93981068760634656 ) ) ;
#15438=ADVANCED_FACE ( 'NONE', ( #20783 ), #3613, .F. ) ;
#15443=DIRECTION ( 'NONE',  ( 0.7563875759206389882, -0.03500244528122105347, 0.6531865459554679898 ) ) ;
#15456=CARTESIAN_POINT ( 'NONE',  ( -55.24300891470648622, -0.009439835024157194193, 0.002702093572889528381 ) ) ;
#15457=CARTESIAN_POINT ( 'NONE',  ( -1.045287976400351981, -15.59869763335126436, -43.05558670614231431 ) ) ;
#15471=ORIENTED_EDGE ( 'NONE', *, *, #9030, .T. ) ;
#15477=EDGE_CURVE ( 'NONE', #27145, #243, #535, .T. ) ;
#15484=VERTEX_POINT ( 'NONE', #12571 ) ;
#15490=CARTESIAN_POINT ( 'NONE',  ( -55.25297051322618813, -0.002853887643043501524, -0.01466904165775538733 ) ) ;
#15494=CARTESIAN_POINT ( 'NONE',  ( -12.82751273423878047, -8.715310691359913875, 48.09651489336692975 ) ) ;
#15500=ORIENTED_EDGE ( 'NONE', *, *, #12642, .F. ) ;
#15501=CARTESIAN_POINT ( 'NONE',  ( -1.048994561756799060, -26.29622118251707619, -37.49601524795400564 ) ) ;
#15503=CARTESIAN_POINT ( 'NONE',  ( -1.619063947482197729, 2.489035965910801895, 46.30105812165545842 ) ) ;
#15513=ADVANCED_FACE ( 'NONE', ( #23255 ), #5538, .T. ) ;
#15520=ORIENTED_EDGE ( 'NONE', *, *, #25554, .F. ) ;
#15521=EDGE_CURVE ( 'NONE', #864, #12683, #26279, .T. ) ;
#15526=CARTESIAN_POINT ( 'NONE',  ( -55.24390624410018802, -0.007503127514277506058, -0.007245494385991484328 ) ) ;
#15541=CARTESIAN_POINT ( 'NONE',  ( -1.619063947482197729, -25.20140673341401438, -38.92136151114898723 ) ) ;
#15546=VERTEX_POINT ( 'NONE', #10152 ) ;
#15550=EDGE_CURVE ( 'NONE', #24539, #5490, #18298, .T. ) ;
#15555=CARTESIAN_POINT ( 'NONE',  ( -20.57838717382308147, -1.611677988432568709, -29.92853265176830746 ) ) ;
#15556=B_SPLINE_CURVE_WITH_KNOTS ( 'NONE', 3,
 ( #25534, #18464, #27232, #5813, #3627, #7546 ),
 .UNSPECIFIED., .F., .F.,
 ( 4, 2, 4 ),
 ( 4.296969928001729735E-16, 0.003576372551511233788, 0.007152745103022037365 ),
 .UNSPECIFIED. ) ;
#15560=CARTESIAN_POINT ( 'NONE',  ( -1.583189561560255143, -44.83405390829663872, 11.94859433442949381 ) ) ;
#15571=CARTESIAN_POINT ( 'NONE',  ( -55.24271866751342941, -0.004256484107795216812, 0.008488649505342837909 ) ) ;
#15574=CARTESIAN_POINT ( 'NONE',  ( -55.24198130335446422, 0.006527480770976314475, -0.006617369590168970667 ) ) ;
#15577=CARTESIAN_POINT ( 'NONE',  ( -1.239374126674604337, -16.50008610789329921, -42.99367564261275021 ) ) ;
#15582=ORIENTED_EDGE ( 'NONE', *, *, #16054, .T. ) ;
#15586=ORIENTED_EDGE ( 'NONE', *, *, #26601, .T. ) ;
#15590=EDGE_CURVE ( 'NONE', #7066, #18960, #14127, .T. ) ;
#15592=( BOUNDED_SURFACE ( )  B_SPLINE_SURFACE ( 3, 1, ( 
 ( #11729, #12015 ),
 ( #20787, #1079 ),
 ( #9866, #27407 ),
 ( #27700, #1215 ) ),
 .UNSPECIFIED., .F., .F., .F. ) 
 B_SPLINE_SURFACE_WITH_KNOTS ( ( 4, 4 ),
 ( 2, 2 ),
 ( 0.000000000000000000, 1.000000000000000000 ),
 ( 0.000000000000000000, 1.000000000000000000 ),
 .UNSPECIFIED. ) 
 GEOMETRIC_REPRESENTATION_ITEM ( )  RATIONAL_B_SPLINE_SURFACE ( (
 ( 1.000000000000000000, 1.000000000000000000),
 ( 0.9593753223639863714, 0.9995975284513187731),
 ( 0.9593753223639863714, 0.9995975284513187731),
 ( 1.000000000000000000, 1.000000000000000000) ) ) 
 REPRESENTATION_ITEM ( '' )  SURFACE ( )  );
#15598=CARTESIAN_POINT ( 'NONE',  ( -55.24340739397742794, -0.002421372372456151618, 0.009842732675348802793 ) ) ;
#15602=CARTESIAN_POINT ( 'NONE',  ( -20.20700224038492721, -29.58392382092672790, 0.9908225410481621420 ) ) ;
#15605=CARTESIAN_POINT ( 'NONE',  ( -4.162674018437141576, 18.33413805792438112, -45.34593312138888876 ) ) ;
#15608=CARTESIAN_POINT ( 'NONE',  ( -1.539763995773694827, 16.63252574783043869, -43.19716353142335663 ) ) ;
#15612=VERTEX_POINT ( 'NONE', #26807 ) ;
#15616=CARTESIAN_POINT ( 'NONE',  ( -1.259972190295308714, -35.85909728507027694, 28.82609802125297449 ) ) ;
#15623=DIRECTION ( 'NONE',  ( 1.000000000000000000, 0.000000000000000000, 0.000000000000000000 ) ) ;
#15632=CARTESIAN_POINT ( 'NONE',  ( -1.583189561560253589, -38.94740041318312507, -25.21827308671218049 ) ) ;
#15634=CARTESIAN_POINT ( 'NONE',  ( -5.986830583229478364, 19.95149887249920440, 46.64941882410778362 ) ) ;
#15637=AXIS2_PLACEMENT_3D ( 'NONE', #20194, #15736, #24698 ) ;
#15640=CARTESIAN_POINT ( 'NONE',  ( -1.050231094221204753, -43.47885872350344982, 14.39477892760344879 ) ) ;
#15643=CIRCLE ( 'NONE', #27606, 34.60786435723138510 ) ;
#15648=CARTESIAN_POINT ( 'NONE',  ( -4.780792508754331038, -49.38761389561005188, -3.764354093953405922 ) ) ;
#15651=CARTESIAN_POINT ( 'NONE',  ( -1.619063947482197729, 46.30105812165548684, -2.489035965910316506 ) ) ;
#15667=VECTOR ( 'NONE', #11094, 1000.000000000000000 ) ;
#15668=CIRCLE ( 'NONE', #5560, 34.60786435723138510 ) ;
#15674=EDGE_CURVE ( 'NONE', #15769, #1484, #3604, .T. ) ;
#15681=VERTEX_POINT ( 'NONE', #5272 ) ;
#15690=CARTESIAN_POINT ( 'NONE',  ( -20.57838717382308147, -7.715628353033481268, 28.96176188950225949 ) ) ;
#15696=CARTESIAN_POINT ( 'NONE',  ( -22.23226125620929139, 2.179935373562892131, 31.55376588768475798 ) ) ;
#15703=VERTEX_POINT ( 'NONE', #9459 ) ;
#15710=CARTESIAN_POINT ( 'NONE',  ( -1.031422197589711764, -44.01264471863837713, 12.69107518035547777 ) ) ;
#15712=CONICAL_SURFACE ( 'NONE', #7493, 34.60786435723138510, 0.8559913436420825139 ) ;
#15713=CARTESIAN_POINT ( 'NONE',  ( -1.046935749539993799, 43.14401153755488849, 15.35946454248350435 ) ) ;
#15723=FACE_OUTER_BOUND ( 'NONE', #11011, .T. ) ;
#15726=FACE_OUTER_BOUND ( 'NONE', #2008, .T. ) ;
#15727=CARTESIAN_POINT ( 'NONE',  ( -2.911734481061388990, -46.11606034418772282, -12.03743348210763031 ) ) ;
#15729=CARTESIAN_POINT ( 'NONE',  ( -1.050230346682677007, -37.05264119692671443, 26.91946103437146931 ) ) ;
#15731=CARTESIAN_POINT ( 'NONE',  ( -20.24399999263414784, 29.60996018918694617, 1.282322917263571282 ) ) ;
#15736=DIRECTION ( 'NONE',  ( 1.000000000000000000, -6.938893903907226837E-18, 1.734723475976806709E-18 ) ) ;
#15740=DIRECTION ( 'NONE',  ( 1.000000000000000000, -6.938893903907226837E-18, 1.734723475976806709E-18 ) ) ;
#15746=EDGE_LOOP ( 'NONE', ( #26945, #11517, #11648, #3082 ) ) ;
#15755=EDGE_CURVE ( 'NONE', #27931, #6993, #2201, .T. ) ;
#15761=CARTESIAN_POINT ( 'NONE',  ( -1.058473599757821404, -1.755404039369745650, -45.77379534793243465 ) ) ;
#15763=ORIENTED_EDGE ( 'NONE', *, *, #13155, .T. ) ;
#15769=VERTEX_POINT ( 'NONE', #24436 ) ;
#15772=ORIENTED_EDGE ( 'NONE', *, *, #25538, .F. ) ;
#15785=EDGE_CURVE ( 'NONE', #17500, #2726, #2535, .T. ) ;
#15790=CARTESIAN_POINT ( 'NONE',  ( -25.21435515916043713, -23.92354251275918031, 25.00736669481048224 ) ) ;
#15791=EDGE_CURVE ( 'NONE', #22965, #16076, #4704, .T. ) ;
#15794=DIRECTION ( 'NONE',  ( 0.000000000000000000, 5.223019709707975211E-21, -1.000000000000000000 ) ) ;
#15795=CARTESIAN_POINT ( 'NONE',  ( -23.79248802219722947, -3.207402715357382306, -33.03370827286730105 ) ) ;
#15796=EDGE_CURVE ( 'NONE', #20894, #23418, #25941, .T. ) ;
#15800=CARTESIAN_POINT ( 'NONE',  ( -55.25719721206881729, -0.01041086141212477223, 0.004044147484878232723 ) ) ;
#15802=CARTESIAN_POINT ( 'NONE',  ( -7.711401346138398338, 21.83927363365101115, 47.70038152767067885 ) ) ;
#15803=ORIENTED_EDGE ( 'NONE', *, *, #3377, .F. ) ;
#15805=ORIENTED_EDGE ( 'NONE', *, *, #28350, .F. ) ;
#15807=B_SPLINE_CURVE_WITH_KNOTS ( 'NONE', 3,
 ( #13685, #24510, #5053, #11530 ),
 .UNSPECIFIED., .F., .F.,
 ( 4, 4 ),
 ( 1.909141801897607538E-16, 0.001982023823822941146 ),
 .UNSPECIFIED. ) ;
#15815=DIRECTION ( 'NONE',  ( 0.000000000000000000, 5.223019709708233256E-21, -1.000000000000000000 ) ) ;
#15820=B_SPLINE_CURVE_WITH_KNOTS ( 'NONE', 3,
 ( #5951, #16745, #5504, #14426 ),
 .UNSPECIFIED., .F., .F.,
 ( 4, 4 ),
 ( 1.977889076651310254E-16, 0.001982023823822932906 ),
 .UNSPECIFIED. ) ;
#15824=ORIENTED_EDGE ( 'NONE', *, *, #12188, .F. ) ;
#15826=EDGE_CURVE ( 'NONE', #25218, #8356, #849, .T. ) ;
#15827=ORIENTED_EDGE ( 'NONE', *, *, #23880, .T. ) ;
#15831=EDGE_CURVE ( 'NONE', #15929, #24730, #16296, .T. ) ;
#15835=VERTEX_POINT ( 'NONE', #14121 ) ;
#15836=CARTESIAN_POINT ( 'NONE',  ( -1.031422197589716205, -37.93675465142491277, -25.67058493451430934 ) ) ;
#15841=CARTESIAN_POINT ( 'NONE',  ( -23.79223135445719706, 33.03345552685145492, 3.207301057648455966 ) ) ;
#15845=CARTESIAN_POINT ( 'NONE',  ( -10.86508079875782151, 46.07061504567116828, 22.20099862734772245 ) ) ;
#15857=ORIENTED_EDGE ( 'NONE', *, *, #5204, .F. ) ;
#15863=ORIENTED_EDGE ( 'NONE', *, *, #7366, .F. ) ;
#15864=CARTESIAN_POINT ( 'NONE',  ( -1.463510566862821882, -2.430838777909866355, 46.14841196428346848 ) ) ;
#15867=CARTESIAN_POINT ( 'NONE',  ( -55.24390624410018802, -0.007245494385991098352, -0.007503127514281985981 ) ) ;
#15887=ORIENTED_EDGE ( 'NONE', *, *, #17510, .T. ) ;
#15888=CARTESIAN_POINT ( 'NONE',  ( -1.619063947482201282, -16.67502769180592992, -43.26576862488428077 ) ) ;
#15889=CARTESIAN_POINT ( 'NONE',  ( -1.239374126674604337, 35.79060836339854745, 28.97829083655398819 ) ) ;
#15898=B_SPLINE_CURVE_WITH_KNOTS ( 'NONE', 3,
 ( #487, #638, #9426, #21025, #25521, #7817, #26825, #9281, #7676, #341 ),
 .UNSPECIFIED., .F., .F.,
 ( 4, 2, 2, 2, 4 ),
 ( 5.898697549827394244E-18, 0.0003346267210630972291, 0.0006692534421261884950, 0.001003880163189279761, 0.001338506884252371135 ),
 .UNSPECIFIED. ) ;
#15903=CARTESIAN_POINT ( 'NONE',  ( -1.019300379054419725, 25.26451264419644716, -38.21680004809172004 ) ) ;
#15910=CARTESIAN_POINT ( 'NONE',  ( -55.24340739397742794, -0.006539691034608149933, -0.007744344507854676943 ) ) ;
#15911=CARTESIAN_POINT ( 'NONE',  ( -22.23342874802668589, 11.82490389046315116, -29.33662284748865900 ) ) ;
#15914=CARTESIAN_POINT ( 'NONE',  ( -20.90916690077964191, -39.20864005633521998, 5.322316104228396405 ) ) ;
#15927=CARTESIAN_POINT ( 'NONE',  ( -20.57838717382308147, -16.28767523336102130, 25.16001208503123365 ) ) ;
#15929=VERTEX_POINT ( 'NONE', #19548 ) ;
#15931=CARTESIAN_POINT ( 'NONE',  ( -20.20612091757424977, 28.48192249925588371, -8.058516044219283359 ) ) ;
#15933=CARTESIAN_POINT ( 'NONE',  ( -55.24390624410018802, 0.01032895241567037548, -0.001451500391950801341 ) ) ;
#15942=ORIENTED_EDGE ( 'NONE', *, *, #3036, .T. ) ;
#15943=CARTESIAN_POINT ( 'NONE',  ( -1.048172774974294175, 37.64158596421250991, 26.08722459372745206 ) ) ;
#15945=FACE_OUTER_BOUND ( 'NONE', #11857, .T. ) ;
#15949=CARTESIAN_POINT ( 'NONE',  ( -28.13707043255157103, 0.7675454997506996335, -22.88591869784691113 ) ) ;
#15955=CARTESIAN_POINT ( 'NONE',  ( -20.24419206586952313, -27.76448493191437095, 10.37009329716794248 ) ) ;
#15967=ORIENTED_EDGE ( 'NONE', *, *, #28101, .F. ) ;
#15975=CARTESIAN_POINT ( 'NONE',  ( -20.20700224038492010, -0.9908225410476447781, 29.58392382092673500 ) ) ;
#15978=CARTESIAN_POINT ( 'NONE',  ( -1.045287976400362417, -15.59869763335038506, 43.05558670614261985 ) ) ;
#15986=CARTESIAN_POINT ( 'NONE',  ( -1.539763995773683503, 44.72359274866481371, -11.93465967526309868 ) ) ;
#15991=DIRECTION ( 'NONE',  ( 0.000000000000000000, 5.223019709707975211E-21, -1.000000000000000000 ) ) ;
#15993=ORIENTED_EDGE ( 'NONE', *, *, #20174, .T. ) ;
#16004=CARTESIAN_POINT ( 'NONE',  ( -1.539763995773680172, -16.63252574783015092, 43.19716353142347742 ) ) ;
#16006=VECTOR ( 'NONE', #1224, 1000.000000000000114 ) ;
#16023=DIRECTION ( 'NONE',  ( 1.000000000000000000, -6.938893903907226837E-18, 1.734723475976806709E-18 ) ) ;
#16030=B_SPLINE_CURVE_WITH_KNOTS ( 'NONE', 3,
 ( #2027, #10415, #6364, #28225, #8527, #10830, #19179 ),
 .UNSPECIFIED., .F., .F.,
 ( 4, 3, 4 ),
 ( 0.000000000000000000, 0.006568092053401815289, 0.02506242213020845253 ),
 .UNSPECIFIED. ) ;
#16037=CARTESIAN_POINT ( 'NONE',  ( -4.178947244162631414, 11.88256963646738740, -47.46809051147726422 ) ) ;
#16039=ADVANCED_FACE ( 'NONE', ( #251 ), #23309, .F. ) ;
#16043=CARTESIAN_POINT ( 'NONE',  ( -1.045287976400365970, 1.530335034934747318, 45.76855895860941814 ) ) ;
#16044=ADVANCED_FACE ( 'NONE', ( #22868 ), #11514, .T. ) ;
#16045=ORIENTED_EDGE ( 'NONE', *, *, #19949, .T. ) ;
#16047=CARTESIAN_POINT ( 'NONE',  ( -22.34422965417126150, -17.95715691811022552, 33.39267070835840912 ) ) ;
#16049=CARTESIAN_POINT ( 'NONE',  ( -22.23226125620930560, 7.677408153694024406, -30.68305173820428067 ) ) ;
#16054=EDGE_CURVE ( 'NONE', #10527, #18593, #15643, .T. ) ;
#16059=VERTEX_POINT ( 'NONE', #24447 ) ;
#16073=CARTESIAN_POINT ( 'NONE',  ( -25.21435515916025594, 1.749597353048488237E-16, -4.373993382621220594E-17 ) ) ;
#16076=VERTEX_POINT ( 'NONE', #9174 ) ;
#16077=CARTESIAN_POINT ( 'NONE',  ( -24.53237795827028123, -6.738475012719871593, 33.25734978085275628 ) ) ;
#16087=CARTESIAN_POINT ( 'NONE',  ( -55.24271866751342941, -0.009388511352197387999, -0.001425019990782294558 ) ) ;
#16091=CARTESIAN_POINT ( 'NONE',  ( -8.786685647604890903, -52.67761315067279781, 9.545808661481174795 ) ) ;
#16096=PLANE ( 'NONE',  #1368 ) ;
#16097=CARTESIAN_POINT ( 'NONE',  ( -20.57838717382308147, -27.96569011373078339, 10.78122205917029675 ) ) ;
#16105=ORIENTED_EDGE ( 'NONE', *, *, #28134, .T. ) ;
#16110=CARTESIAN_POINT ( 'NONE',  ( -28.13707043255157103, -21.52861750560933984, 7.802116958609231823 ) ) ;
#16112=DIRECTION ( 'NONE',  ( -0.7563875759206388771, 0.4122509917856786443, 0.5078650950445640078 ) ) ;
#16124=CARTESIAN_POINT ( 'NONE',  ( -1.056502255334265339, 43.40574022158794065, 14.64009593116057317 ) ) ;
#16132=CARTESIAN_POINT ( 'NONE',  ( -1.045287976400362417, -1.530335034934427574, -45.76855895860943235 ) ) ;
#16136=CARTESIAN_POINT ( 'NONE',  ( -2.265401668238145483, -39.53028715828216377, 25.45016726748356817 ) ) ;
#16145=CARTESIAN_POINT ( 'NONE',  ( -55.24300891470650754, 0.009812809446893281523, -0.0003472257464216086005 ) ) ;
#16146=CARTESIAN_POINT ( 'NONE',  ( -55.24271866751342941, 0.009369360294294836952, -0.001545935011626992572 ) ) ;
#16150=CARTESIAN_POINT ( 'NONE',  ( -8.786685647604890903, 7.199674155858966529, -53.04920435127184675 ) ) ;
#16161=CARTESIAN_POINT ( 'NONE',  ( -25.21435515916043713, 6.169479169075932745, 34.05351380035326514 ) ) ;
#16164=FACE_OUTER_BOUND ( 'NONE', #2820, .T. ) ;
#16165=CARTESIAN_POINT ( 'NONE',  ( -55.24728320129491266, -0.01453410071985621575, -0.0006547948648749734972 ) ) ;
#16171=CARTESIAN_POINT ( 'NONE',  ( -20.57838717382308147, -23.26537097894090778, 18.89542499756525729 ) ) ;
#16178=AXIS2_PLACEMENT_3D ( 'NONE', #6327, #15076, #20642 ) ;
#16185=CARTESIAN_POINT ( 'NONE',  ( -1.031422197589711764, 15.60268798220637798, -43.06660437151313658 ) ) ;
#16192=FACE_OUTER_BOUND ( 'NONE', #1347, .T. ) ;
#16193=CARTESIAN_POINT ( 'NONE',  ( -1.583189561560255143, -36.01941156322808979, -29.24830400313152623 ) ) ;
#16196=ORIENTED_EDGE ( 'NONE', *, *, #5462, .F. ) ;
#16201=CARTESIAN_POINT ( 'NONE',  ( -1.045287976400365970, 45.76855895860946077, 1.530335034933974381 ) ) ;
#16202=CARTESIAN_POINT ( 'NONE',  ( -1.058197053496161555, -38.06270006878834522, 25.48582931365511328 ) ) ;
#16209=CARTESIAN_POINT ( 'NONE',  ( -55.24390624410018802, -0.001811362924359030029, -0.01027195578987783083 ) ) ;
#16215=B_SPLINE_CURVE_WITH_KNOTS ( 'NONE', 3,
 ( #21264, #19239, #1543, #10349, #14916, #19111, #28012 ),
 .UNSPECIFIED., .F., .F.,
 ( 4, 3, 4 ),
 ( 0.000000000000000000, 0.009512539173626361963, 0.02506242213020844212 ),
 .UNSPECIFIED. ) ;
#16222=CARTESIAN_POINT ( 'NONE',  ( -55.24300891470650754, 0.009225237711101738972, -0.003362556190412665288 ) ) ;
#16223=CARTESIAN_POINT ( 'NONE',  ( -55.25297051322618813, 0.01466904165775564234, -0.002853887643044135131 ) ) ;
#16226=CARTESIAN_POINT ( 'NONE',  ( -20.57838717382308502, 25.16001208503106668, -16.28767523336130196 ) ) ;
#16229=EDGE_LOOP ( 'NONE', ( #22669, #3764, #26117, #4517 ) ) ;
#16236=CARTESIAN_POINT ( 'NONE',  ( -23.77929240705206837, 32.66578242509746133, -15.74261278740683778 ) ) ;
#16238=EDGE_LOOP ( 'NONE', ( #24556, #19452, #570, #19102 ) ) ;
#16240=CARTESIAN_POINT ( 'NONE',  ( -1.464342487929867209, -16.57334911911542363, -43.13914623307952922 ) ) ;
#16242=CARTESIAN_POINT ( 'NONE',  ( -28.41354790283022069, -23.16239616762929998, 1.249099604787319295 ) ) ;
#16249=CIRCLE ( 'NONE', #3837, 53.53553390275978785 ) ;
#16251=CARTESIAN_POINT ( 'NONE',  ( -20.37983603106074071, 16.25728007463443703, 24.94323704205420000 ) ) ;
#16258=B_SPLINE_CURVE_WITH_KNOTS ( 'NONE', 3,
 ( #12253, #14550, #8099, #19291, #21593, #1453 ),
 .UNSPECIFIED., .F., .F.,
 ( 4, 2, 4 ),
 ( 0.000000000000000000, 0.0004335184443140242989, 0.0008670368886280485979 ),
 .UNSPECIFIED. ) ;
#16259=CARTESIAN_POINT ( 'NONE',  ( -2.904412668506652473, -17.42365698954667863, 44.35433137608958276 ) ) ;
#16269=DIRECTION ( 'NONE',  ( 0.7637818620346802367, -0.2198041754873842346, 0.6068965246771050870 ) ) ;
#16272=CARTESIAN_POINT ( 'NONE',  ( -18.41936578851709427, -38.22933728004704790, -18.42310649277614232 ) ) ;
#16275=CARTESIAN_POINT ( 'NONE',  ( -9.156249394959713683, -38.17928057392020236, -38.89149400288393821 ) ) ;
#16276=CARTESIAN_POINT ( 'NONE',  ( -55.24390624410018802, -0.001451500391950358120, -0.01032895241567008057 ) ) ;
#16282=DIRECTION ( 'NONE',  ( 0.000000000000000000, 5.223019709707975211E-21, -1.000000000000000000 ) ) ;
#16296=LINE ( 'NONE', #7826, #12430 ) ;
#16302=CARTESIAN_POINT ( 'NONE',  ( -8.786685647604898008, 38.68584556812353981, 37.00619870957891777 ) ) ;
#16304=CARTESIAN_POINT ( 'NONE',  ( -1.259972190295307604, -25.19627397134270197, 38.49631882650675152 ) ) ;
#16306=CARTESIAN_POINT ( 'NONE',  ( -55.25297051322618813, 0.01093108995495213273, 0.01019003092403696770 ) ) ;
#16312=VERTEX_POINT ( 'NONE', #18010 ) ;
#16314=CARTESIAN_POINT ( 'NONE',  ( -19.53423201713129842, 1.355459634611817431E-16, -3.388649086529543578E-17 ) ) ;
#16318=ORIENTED_EDGE ( 'NONE', *, *, #4445, .F. ) ;
#16323=CARTESIAN_POINT ( 'NONE',  ( -23.79248802219731118, -28.61009539422396131, -16.82188324679470881 ) ) ;
#16324=CARTESIAN_POINT ( 'NONE',  ( -55.25297051322618813, -0.01093108995494780980, 0.01019003092403480623 ) ) ;
#16328=CARTESIAN_POINT ( 'NONE',  ( -1.044557008772713624, 28.22896138707370994, -36.05793264791354602 ) ) ;
#16332=CARTESIAN_POINT ( 'NONE',  ( -1.045287976400362417, 37.92705037016796155, 25.66401692419947977 ) ) ;
#16335=CARTESIAN_POINT ( 'NONE',  ( -1.019300379054419947, -35.83762006677421397, -28.53917295602885318 ) ) ;
#16336=DIRECTION ( 'NONE',  ( -0.7563875759206389882, 0.1685564395263298709, -0.6320336713238514648 ) ) ;
#16353=ORIENTED_EDGE ( 'NONE', *, *, #17831, .F. ) ;
#16356=B_SPLINE_CURVE_WITH_KNOTS ( 'NONE', 3,
 ( #9231, #24214, #17989, #26775, #7088, #13245, #24355 ),
 .UNSPECIFIED., .F., .F.,
 ( 4, 3, 4 ),
 ( 1.309687503460226953E-17, 0.009512539173626405331, 0.02506242213020846293 ),
 .UNSPECIFIED. ) ;
#16360=SHAPE_DEFINITION_REPRESENTATION ( #10845, #747 ) ;
#16362=CARTESIAN_POINT ( 'NONE',  ( -9.156249394959706578, 38.17928057391991103, -38.89149400288420111 ) ) ;
#16374=CARTESIAN_POINT ( 'NONE',  ( -20.20997486282891131, -0.3303599360441825672, -29.60348406988234871 ) ) ;
#16379=CARTESIAN_POINT ( 'NONE',  ( -25.21435515916043002, 31.17620025257588523, -15.02493970636157705 ) ) ;
#16380=CARTESIAN_POINT ( 'NONE',  ( -1.619063947482201282, -44.80407745103776307, 11.94059994246206635 ) ) ;
#16385=CARTESIAN_POINT ( 'NONE',  ( -1.050230346682680560, 14.15335421912582170, -43.55729751025868524 ) ) ;
#16389=CARTESIAN_POINT ( 'NONE',  ( -23.79248802219728987, 22.01156985585204851, 24.83956736572385893 ) ) ;
#16398=( BOUNDED_SURFACE ( )  B_SPLINE_SURFACE ( 3, 1, ( 
 ( #26207, #25945 ),
 ( #14986, #10686 ),
 ( #27048, #2896 ),
 ( #6935, #16275 ) ),
 .UNSPECIFIED., .F., .F., .F. ) 
 B_SPLINE_SURFACE_WITH_KNOTS ( ( 4, 4 ),
 ( 2, 2 ),
 ( 0.000000000000000000, 1.000000000000000000 ),
 ( 0.000000000000000000, 1.000000000000000000 ),
 .UNSPECIFIED. ) 
 GEOMETRIC_REPRESENTATION_ITEM ( )  RATIONAL_B_SPLINE_SURFACE ( (
 ( 1.000000000000000000, 1.000000000000000000),
 ( 0.7789835883360576307, 0.9689951854195403280),
 ( 0.7789835883360576307, 0.9689951854195403280),
 ( 1.000000000000000000, 1.000000000000000000) ) ) 
 REPRESENTATION_ITEM ( '' )  SURFACE ( )  );
#16401=CARTESIAN_POINT ( 'NONE',  ( -1.045287976400383290, 28.14015102489806708, -36.12803364096618708 ) ) ;
#16402=EDGE_CURVE ( 'NONE', #3497, #4240, #2891, .T. ) ;
#16407=CARTESIAN_POINT ( 'NONE',  ( -20.57838717382308147, 23.26537097894132344, 18.89542499756474569 ) ) ;
#16408=ORIENTED_EDGE ( 'NONE', *, *, #11295, .T. ) ;
#16411=B_SPLINE_CURVE_WITH_KNOTS ( 'NONE', 3,
 ( #15246, #2281, #4749, #22318 ),
 .UNSPECIFIED., .F., .F.,
 ( 4, 4 ),
 ( 1.904170172768910460E-16, 0.001982023823822945917 ),
 .UNSPECIFIED. ) ;
#16416=ORIENTED_EDGE ( 'NONE', *, *, #2844, .F. ) ;
#16418=EDGE_CURVE ( 'NONE', #24434, #21106, #24871, .T. ) ;
#16423=CARTESIAN_POINT ( 'NONE',  ( -1.259920593601971950, 2.243284667987781589, -45.95412615877140894 ) ) ;
#16426=CARTESIAN_POINT ( 'NONE',  ( -55.24198130335446422, -0.001391250620104931938, 0.009190321388308853381 ) ) ;
#16428=CARTESIAN_POINT ( 'NONE',  ( -1.045287976400362417, -1.530335034934427574, -45.76855895860943235 ) ) ;
#16431=CARTESIAN_POINT ( 'NONE',  ( -20.20700224038492721, 27.82980252387819675, -10.08426345511598932 ) ) ;
#16432=EDGE_CURVE ( 'NONE', #1301, #17827, #15065, .T. ) ;
#16435=CARTESIAN_POINT ( 'NONE',  ( -24.53239521893646824, -30.86654523348673962, -14.09666242510777145 ) ) ;
#16436=ORIENTED_EDGE ( 'NONE', *, *, #4413, .F. ) ;
#16450=CARTESIAN_POINT ( 'NONE',  ( -20.21097721650787449, -28.05863614620931656, 9.464413208035370673 ) ) ;
#16461=DIRECTION ( 'NONE',  ( 1.000000000000000000, -6.938893903907226837E-18, 1.734723475976806709E-18 ) ) ;
#16464=ORIENTED_EDGE ( 'NONE', *, *, #2042, .F. ) ;
#16470=( BOUNDED_SURFACE ( )  B_SPLINE_SURFACE ( 3, 1, ( 
 ( #8383, #26200 ),
 ( #21750, #22170 ),
 ( #23795, #17415 ),
 ( #15526, #10948 ) ),
 .UNSPECIFIED., .F., .F., .F. ) 
 B_SPLINE_SURFACE_WITH_KNOTS ( ( 4, 4 ),
 ( 2, 2 ),
 ( 0.000000000000000000, 1.000000000000000000 ),
 ( 0.000000000000000000, 1.000000000000000000 ),
 .UNSPECIFIED. ) 
 GEOMETRIC_REPRESENTATION_ITEM ( )  RATIONAL_B_SPLINE_SURFACE ( (
 ( 1.000000000000000000, 1.000000000000000000),
 ( 0.7789835883360578528, 0.9689951854195403280),
 ( 0.7789835883360578528, 0.9689951854195403280),
 ( 1.000000000000000000, 1.000000000000000000) ) ) 
 REPRESENTATION_ITEM ( '' )  SURFACE ( )  );
#16472=DIRECTION ( 'NONE',  ( 0.7637818620346800147, -0.3965875333584803486, 0.5092696688508683289 ) ) ;
#16473=CARTESIAN_POINT ( 'NONE',  ( -1.583189561560255143, 16.68617981233701997, -43.29471907393748609 ) ) ;
#16478=CARTESIAN_POINT ( 'NONE',  ( -20.21097721712959583, -17.67178718142840665, 23.76068428613700334 ) ) ;
#16494=DIRECTION ( 'NONE',  ( -0.7563875759206388771, 0.6104009704506910827, -0.2351350468682930628 ) ) ;
#16495=CIRCLE ( 'NONE', #10531, 53.53553390275978785 ) ;
#16496=VERTEX_POINT ( 'NONE', #6597 ) ;
#16501=CARTESIAN_POINT ( 'NONE',  ( -1.044557008772712070, -43.01636061108997922, -15.70482370518800153 ) ) ;
#16503=ORIENTED_EDGE ( 'NONE', *, *, #5422, .T. ) ;
#16505=EDGE_CURVE ( 'NONE', #7217, #13496, #11518, .T. ) ;
#16516=CARTESIAN_POINT ( 'NONE',  ( -20.24419206586951603, 23.20105925399726132, -18.44224248888881590 ) ) ;
#16520=CARTESIAN_POINT ( 'NONE',  ( -1.019300379054419725, -2.023851374322995778, -45.76814864815089123 ) ) ;
#16531=CARTESIAN_POINT ( 'NONE',  ( -1.050229599974477734, 14.39582765040461254, -43.47850826583058392 ) ) ;
#16533=CARTESIAN_POINT ( 'NONE',  ( -55.25297051322618813, -0.007247191603128547155, 0.01306918787467270006 ) ) ;
#16534=CARTESIAN_POINT ( 'NONE',  ( -20.20700224038492010, 24.51628800869071867, 16.58740185276683832 ) ) ;
#16543=CARTESIAN_POINT ( 'NONE',  ( -1.031422197589716205, 28.14735071801744581, -36.13727897780137965 ) ) ;
#16550=FACE_OUTER_BOUND ( 'NONE', #6268, .T. ) ;
#16552=CARTESIAN_POINT ( 'NONE',  ( -9.156249394959713683, 53.90509764945130655, -8.027840202794127578 ) ) ;
#16555=EDGE_LOOP ( 'NONE', ( #17793, #4590, #19577, #6537 ) ) ;
#16568=CARTESIAN_POINT ( 'NONE',  ( -20.47566262905010248, -23.19796652405687709, -18.81547655725238499 ) ) ;
#16570=CARTESIAN_POINT ( 'NONE',  ( -20.24399999263414429, -16.36687688782875938, -24.70869149526196651 ) ) ;
#16578=EDGE_CURVE ( 'NONE', #21771, #5523, #13840, .T. ) ;
#16582=CARTESIAN_POINT ( 'NONE',  ( -55.25719721206881729, -0.01079965405819445674, 0.002847566758684036761 ) ) ;
#16589=ORIENTED_EDGE ( 'NONE', *, *, #5871, .T. ) ;
#16600=CARTESIAN_POINT ( 'NONE',  ( -1.583189561560253589, -25.21827308671203127, 38.94740041318322454 ) ) ;
#16602=CARTESIAN_POINT ( 'NONE',  ( -9.156249394959713683, 9.022661520477768704, -53.74753343182706544 ) ) ;
#16603=CARTESIAN_POINT ( 'NONE',  ( -2.911734481061402757, -25.69892591260238746, 40.13920818157105685 ) ) ;
#16612=B_SPLINE_CURVE_WITH_KNOTS ( 'NONE', 3,
 ( #15048, #26008, #23870, #1956, #10761, #9149, #24006 ),
 .UNSPECIFIED., .F., .F.,
 ( 4, 3, 4 ),
 ( 3.469446951953614189E-18, 0.009512539173626381045, 0.02506242213020843518 ),
 .UNSPECIFIED. ) ;
#16613=ORIENTED_EDGE ( 'NONE', *, *, #14722, .F. ) ;
#16620=CARTESIAN_POINT ( 'NONE',  ( -16.86833981943424376, -30.57013526701942041, -31.95666732167553548 ) ) ;
#16625=CARTESIAN_POINT ( 'NONE',  ( -1.045287976400383290, 28.14015102489806708, -36.12803364096618708 ) ) ;
#16634=CARTESIAN_POINT ( 'NONE',  ( -25.21435515916043002, 30.48034229288640162, -16.39063784838753790 ) ) ;
#16642=DIRECTION ( 'NONE',  ( 1.000000000000000000, -6.938893903907226837E-18, 1.734723475976806709E-18 ) ) ;
#16643=CARTESIAN_POINT ( 'NONE',  ( -20.57838717382308147, -29.92853265176832878, -1.611677988432255848 ) ) ;
#16654=CARTESIAN_POINT ( 'NONE',  ( -25.21435515916043713, 30.48034229288662544, 16.39063784838709736 ) ) ;
#16656=CARTESIAN_POINT ( 'NONE',  ( -7.078251931573400491, 34.59014398252916322, -38.93060825814240644 ) ) ;
#16663=AXIS2_PLACEMENT_3D ( 'NONE', #23405, #10443, #16785 ) ;
#16667=CARTESIAN_POINT ( 'NONE',  ( -20.20700224038492721, 23.35150625415659320, -18.19058640100232438 ) ) ;
#16671=VERTEX_POINT ( 'NONE', #1762 ) ;
#16677=CARTESIAN_POINT ( 'NONE',  ( -1.259920593601969729, -12.06711544331594865, -44.39818421957811978 ) ) ;
#16682=DIRECTION ( 'NONE',  ( 1.000000000000000000, -6.938893903907226837E-18, 1.734723475976806709E-18 ) ) ;
#16693=CARTESIAN_POINT ( 'NONE',  ( -4.178947244162637631, 47.46809051147737080, 11.88256963646688824 ) ) ;
#16698=( BOUNDED_SURFACE ( )  B_SPLINE_SURFACE ( 3, 1, ( 
 ( #15571, #26523 ),
 ( #17875, #2336 ),
 ( #328, #19621 ),
 ( #28390, #8692 ) ),
 .UNSPECIFIED., .F., .F., .F. ) 
 B_SPLINE_SURFACE_WITH_KNOTS ( ( 4, 4 ),
 ( 2, 2 ),
 ( 0.000000000000000000, 1.000000000000000000 ),
 ( 0.000000000000000000, 1.000000000000000000 ),
 .UNSPECIFIED. ) 
 GEOMETRIC_REPRESENTATION_ITEM ( )  RATIONAL_B_SPLINE_SURFACE ( (
 ( 1.000000000000000000, 1.000000000000000000),
 ( 0.9593753223639863714, 0.9995975284513187731),
 ( 0.9593753223639863714, 0.9995975284513187731),
 ( 1.000000000000000000, 1.000000000000000000) ) ) 
 REPRESENTATION_ITEM ( '' )  SURFACE ( )  );
#16712=ORIENTED_EDGE ( 'NONE', *, *, #18851, .T. ) ;
#16724=CARTESIAN_POINT ( 'NONE',  ( -1.046936909428682672, -37.78538189376526901, -25.87632113675147849 ) ) ;
#16725=CARTESIAN_POINT ( 'NONE',  ( -20.57838717382308147, -28.96176188950224528, -7.715628353033566533 ) ) ;
#16729=CARTESIAN_POINT ( 'NONE',  ( -9.156249394959713683, -9.022661520477402775, 53.74753343182710807 ) ) ;
#16735=B_SPLINE_CURVE_WITH_KNOTS ( 'NONE', 3,
 ( #25762, #16971, #21144, #6054, #14809, #23618 ),
 .UNSPECIFIED., .F., .F.,
 ( 4, 2, 4 ),
 ( 0.000000000000000000, 0.0004335151646191501111, 0.0008670303292383002222 ),
 .UNSPECIFIED. ) ;
#16741=FACE_OUTER_BOUND ( 'NONE', #28257, .T. ) ;
#16745=CARTESIAN_POINT ( 'NONE',  ( -20.21097721712959583, 17.67178718142858429, -23.76068428613687189 ) ) ;
#16749=AXIS2_PLACEMENT_3D ( 'NONE', #27992, #12732, #12591 ) ;
#16759=EDGE_CURVE ( 'NONE', #16899, #5490, #18887, .T. ) ;
#16762=EDGE_CURVE ( 'NONE', #26863, #3886, #26225, .T. ) ;
#16764=CARTESIAN_POINT ( 'NONE',  ( -20.20700224038492010, 8.199606986804733211, 28.44216453106527709 ) ) ;
#16773=CARTESIAN_POINT ( 'NONE',  ( -1.619063947482197729, -25.20140673341345305, 38.92136151114934961 ) ) ;
#16779=( BOUNDED_SURFACE ( )  B_SPLINE_SURFACE ( 3, 1, ( 
 ( #4946, #11719 ),
 ( #2790, #15889 ),
 ( #26823, #24831 ),
 ( #9424, #5087 ) ),
 .UNSPECIFIED., .F., .F., .F. ) 
 B_SPLINE_SURFACE_WITH_KNOTS ( ( 4, 4 ),
 ( 2, 2 ),
 ( 0.000000000000000000, 1.000000000000000000 ),
 ( 0.000000000000000000, 1.000000000000000000 ),
 .UNSPECIFIED. ) 
 GEOMETRIC_REPRESENTATION_ITEM ( )  RATIONAL_B_SPLINE_SURFACE ( (
 ( 1.000000000000000000, 1.000000000000000000),
 ( 0.9934239774497837239, 0.8357310067453919133),
 ( 0.9934239774497837239, 0.8357310067453919133),
 ( 1.000000000000000000, 1.000000000000000000) ) ) 
 REPRESENTATION_ITEM ( '' )  SURFACE ( )  );
#16781=EDGE_LOOP ( 'NONE', ( #25790, #21948, #7852, #15967 ) ) ;
#16782=ORIENTED_EDGE ( 'NONE', *, *, #2844, .T. ) ;
#16784=ADVANCED_FACE ( 'NONE', ( #27217 ), #2859, .F. ) ;
#16785=DIRECTION ( 'NONE',  ( 0.000000000000000000, 5.223019709707975211E-21, -1.000000000000000000 ) ) ;
#16790=EDGE_LOOP ( 'NONE', ( #5758, #16942, #7374, #26260 ) ) ;
#16793=CARTESIAN_POINT ( 'NONE',  ( -1.058197053496162887, 36.00048521498994347, 28.32422455455037991 ) ) ;
#16796=B_SPLINE_CURVE_WITH_KNOTS ( 'NONE', 3,
 ( #8935, #22604, #22898, #27026, #11798, #18249 ),
 .UNSPECIFIED., .F., .F.,
 ( 4, 2, 4 ),
 ( 4.286557520396696095E-16, 0.003576372551511235957, 0.007152745103022043437 ),
 .UNSPECIFIED. ) ;
#16804=CARTESIAN_POINT ( 'NONE',  ( -1.539763995773687055, -43.19716353142342768, -16.63252574783026816 ) ) ;
#16812=CARTESIAN_POINT ( 'NONE',  ( -28.41354790283022069, 14.62505768302827036, 18.00456980371883731 ) ) ;
#16815=CARTESIAN_POINT ( 'NONE',  ( -8.786685647604890903, 23.24040270374391426, -48.22796981442777309 ) ) ;
#16818=CARTESIAN_POINT ( 'NONE',  ( -1.045287976400365970, -25.66401692419961833, 37.92705037016786918 ) ) ;
#16819=CARTESIAN_POINT ( 'NONE',  ( -25.21435515916043713, -34.05351380035328646, 6.169479169075816394 ) ) ;
#16831=CARTESIAN_POINT ( 'NONE',  ( -20.24419206586952313, 1.282847120831654530, 29.61012937815439017 ) ) ;
#16832=CARTESIAN_POINT ( 'NONE',  ( -1.048994561756806831, 14.87838255483256233, -43.31369460697981566 ) ) ;
#16843=CARTESIAN_POINT ( 'NONE',  ( -1.046936909428679119, -45.77873603877005593, 1.275306677858721649 ) ) ;
#16844=CARTESIAN_POINT ( 'NONE',  ( -24.53239521893646824, 3.868435622621471115, -33.71193723315172264 ) ) ;
#16851=CARTESIAN_POINT ( 'NONE',  ( -1.539763995773684835, -46.22267697748605997, -2.469814354917328370 ) ) ;
#16860=FACE_OUTER_BOUND ( 'NONE', #13949, .T. ) ;
#16865=CARTESIAN_POINT ( 'NONE',  ( -55.24390624410018802, 0.007245494385991800047, -0.007503127514277958821 ) ) ;
#16870=EDGE_LOOP ( 'NONE', ( #20831, #6376, #25755, #27054 ) ) ;
#16874=ORIENTED_EDGE ( 'NONE', *, *, #17304, .T. ) ;
#16875=ORIENTED_EDGE ( 'NONE', *, *, #28350, .T. ) ;
#16881=CARTESIAN_POINT ( 'NONE',  ( -12.94347594948484037, 33.69581619287875895, -35.22469990145616237 ) ) ;
#16899=VERTEX_POINT ( 'NONE', #10118 ) ;
#16900=CARTESIAN_POINT ( 'NONE',  ( -20.20612092514784308, 16.46550332780526915, -24.59769888281538996 ) ) ;
#16906=EDGE_CURVE ( 'NONE', #17251, #10554, #21180, .T. ) ;
#16910=VECTOR ( 'NONE', #25210, 1000.000000000000000 ) ;
#16911=ORIENTED_EDGE ( 'NONE', *, *, #17732, .T. ) ;
#16924=VERTEX_POINT ( 'NONE', #27513 ) ;
#16932=CARTESIAN_POINT ( 'NONE',  ( -1.619063947482197729, -44.80407745103793360, -11.94059994246142331 ) ) ;
#16933=ADVANCED_FACE ( 'NONE', ( #7822 ), #27136, .F. ) ;
#16935=DIRECTION ( 'NONE',  ( 0.000000000000000000, -1.000000000000000000, 0.000000000000000000 ) ) ;
#16941=ORIENTED_EDGE ( 'NONE', *, *, #10957, .F. ) ;
#16942=ORIENTED_EDGE ( 'NONE', *, *, #27127, .F. ) ;
#16948=CARTESIAN_POINT ( 'NONE',  ( -20.57838717382308147, 18.89542499756500149, -23.26537097894111383 ) ) ;
#16956=CARTESIAN_POINT ( 'NONE',  ( -25.21435515916043713, -31.17620025257598471, -15.02493970636134613 ) ) ;
#16962=VERTEX_POINT ( 'NONE', #4183 ) ;
#16967=CARTESIAN_POINT ( 'NONE',  ( -1.259972190295302497, -12.06706380853662530, 44.39825172539707410 ) ) ;
#16968=CARTESIAN_POINT ( 'NONE',  ( -1.050229599974480843, -43.47850826583062656, -14.39582765040444912 ) ) ;
#16971=CARTESIAN_POINT ( 'NONE',  ( -20.47566262905009538, 18.81547655725247381, -23.19796652405680248 ) ) ;
#16972=CARTESIAN_POINT ( 'NONE',  ( -55.24728320129491266, 0.005114031043466756021, 0.01362040845703047127 ) ) ;
#16974=CARTESIAN_POINT ( 'NONE',  ( -1.044557008772710516, -28.22896138707343994, 36.05793264791374497 ) ) ;
#16980=CARTESIAN_POINT ( 'NONE',  ( -1.464342487929851222, 16.57334911911573982, 43.13914623307943685 ) ) ;
#16983=( BOUNDED_SURFACE ( )  B_SPLINE_SURFACE ( 3, 1, ( 
 ( #9095, #22790 ),
 ( #5346, #23220 ),
 ( #21024, #12121 ),
 ( #22932, #16729 ) ),
 .UNSPECIFIED., .F., .F., .F. ) 
 B_SPLINE_SURFACE_WITH_KNOTS ( ( 4, 4 ),
 ( 2, 2 ),
 ( 0.000000000000000000, 1.000000000000000000 ),
 ( 0.000000000000000000, 1.000000000000000000 ),
 .UNSPECIFIED. ) 
 GEOMETRIC_REPRESENTATION_ITEM ( )  RATIONAL_B_SPLINE_SURFACE ( (
 ( 1.000000000000000000, 1.000000000000000000),
 ( 0.7789835883360576307, 0.9689951854195403280),
 ( 0.7789835883360576307, 0.9689951854195403280),
 ( 1.000000000000000000, 1.000000000000000000) ) ) 
 REPRESENTATION_ITEM ( '' )  SURFACE ( )  );
#16985=CARTESIAN_POINT ( 'NONE',  ( -1.048171036023513913, 27.73816396939564299, -36.44209502233717046 ) ) ;
#16992=CARTESIAN_POINT ( 'NONE',  ( -20.57838717382308147, 10.78122205917000365, -27.96569011373090063 ) ) ;
#16993=CARTESIAN_POINT ( 'NONE',  ( -1.048171036023513247, 1.020520027229132598, -45.78635789057864969 ) ) ;
#17004=ORIENTED_EDGE ( 'NONE', *, *, #10522, .F. ) ;
#17007=CARTESIAN_POINT ( 'NONE',  ( -21.41430102051752016, 23.81424706376365918, -19.54553566814595200 ) ) ;
#17010=CARTESIAN_POINT ( 'NONE',  ( -25.21435515916044423, -16.39063784838720395, 30.48034229288656505 ) ) ;
#17015=ORIENTED_EDGE ( 'NONE', *, *, #20068, .F. ) ;
#17023=VERTEX_POINT ( 'NONE', #21602 ) ;
#17024=VECTOR ( 'NONE', #15208, 1000.000000000000114 ) ;
#17026=B_SPLINE_CURVE_WITH_KNOTS ( 'NONE', 3,
 ( #14172, #27718, #16793, #1230, #23140, #3397, #25139, #11887, #12446, #10174 ),
 .UNSPECIFIED., .F., .F.,
 ( 4, 2, 2, 2, 4 ),
 ( 2.976713740813343128E-16, 0.0003346187017559132675, 0.0006692374035115289214, 0.001003856105267144630, 0.001338474807022760121 ),
 .UNSPECIFIED. ) ;
#17030=CARTESIAN_POINT ( 'NONE',  ( -25.21435515916025594, 1.749597353048488237E-16, -4.373993382621220594E-17 ) ) ;
#17031=CARTESIAN_POINT ( 'NONE',  ( -22.34422965417126505, 5.100074259623119666, 37.57019010019537575 ) ) ;
#17033=CIRCLE ( 'NONE', #26682, 34.60786435723138510 ) ;
#17037=CARTESIAN_POINT ( 'NONE',  ( -20.21097721650786738, -17.13687097598118925, 24.14932365326971464 ) ) ;
#17045=B_SPLINE_CURVE_WITH_KNOTS ( 'NONE', 3,
 ( #24423, #26422, #24578, #4692, #2522, #11311 ),
 .UNSPECIFIED., .F., .F.,
 ( 4, 2, 4 ),
 ( 1.491862189340054101E-16, 0.003570751334075637860, 0.007141502668151126533 ),
 .UNSPECIFIED. ) ;
#17048=CARTESIAN_POINT ( 'NONE',  ( -7.711401346138400115, 25.75361633141491424, -45.70592430511727144 ) ) ;
#17049=CARTESIAN_POINT ( 'NONE',  ( -1.019300379054419725, -28.53917295602924042, -35.83762006677390133 ) ) ;
#17056=EDGE_CURVE ( 'NONE', #10267, #15546, #8358, .T. ) ;
#17057=B_SPLINE_CURVE_WITH_KNOTS ( 'NONE', 3,
 ( #10588, #8437, #17202, #25990, #27572, #6279, #4103, #5721 ),
 .UNSPECIFIED., .F., .F.,
 ( 4, 2, 2, 4 ),
 ( 0.000000000000000000, 0.002761524886576655416, 0.005523049773153310832, 0.01104609954630661646 ),
 .UNSPECIFIED. ) ;
#17064=ORIENTED_EDGE ( 'NONE', *, *, #13583, .T. ) ;
#17065=CARTESIAN_POINT ( 'NONE',  ( -55.24271866751342941, 0.001545935011631005204, -0.009369360294295841357 ) ) ;
#17072=CARTESIAN_POINT ( 'NONE',  ( -1.619063947482197729, -2.489035965909835557, 46.30105812165550816 ) ) ;
#17074=CARTESIAN_POINT ( 'NONE',  ( -1.058473599757816297, 45.77379534793244886, -1.755404039369589997 ) ) ;
#17079=CARTESIAN_POINT ( 'NONE',  ( -1.044557008772710294, 25.56990300677035677, 37.98985164565299755 ) ) ;
#17083=ORIENTED_EDGE ( 'NONE', *, *, #7829, .F. ) ;
#17084=CARTESIAN_POINT ( 'NONE',  ( -20.90916690077964546, -17.17795951644681907, -35.64494649500676360 ) ) ;
#17086=ORIENTED_EDGE ( 'NONE', *, *, #9161, .T. ) ;
#17101=CARTESIAN_POINT ( 'NONE',  ( -20.20700224038492365, -8.199606986804534259, -28.44216453106533748 ) ) ;
#17105=CARTESIAN_POINT ( 'NONE',  ( -20.57838717382308147, 23.26537097894132344, 18.89542499756474569 ) ) ;
#17107=DIRECTION ( 'NONE',  ( 0.000000000000000000, 5.223019709707975211E-21, -1.000000000000000000 ) ) ;
#17109=CARTESIAN_POINT ( 'NONE',  ( -55.24390624410018802, -0.009209468562452135382, -0.004896917417131697002 ) ) ;
#17110=FACE_OUTER_BOUND ( 'NONE', #3109, .T. ) ;
#17111=CARTESIAN_POINT ( 'NONE',  ( -22.34422965417123663, -6.759368364654068095, 37.30738373203626423 ) ) ;
#17115=EDGE_LOOP ( 'NONE', ( #13575, #26342, #2204, #6740 ) ) ;
#17117=CARTESIAN_POINT ( 'NONE',  ( -25.21435515916043713, 34.05351380035342146, 6.169479169075106739 ) ) ;
#17120=B_SPLINE_CURVE_WITH_KNOTS ( 'NONE', 3,
 ( #15378, #25680, #26189, #17542 ),
 .UNSPECIFIED., .F., .F.,
 ( 4, 4 ),
 ( 1.892757412642747523E-16, 0.001982023823822947652 ),
 .UNSPECIFIED. ) ;
#17127=CARTESIAN_POINT ( 'NONE',  ( -55.24271866751342941, -0.001425019990778742711, -0.009388511352200234680 ) ) ;
#17135=CARTESIAN_POINT ( 'NONE',  ( -6.588769196390753535, -38.42957692275866322, -34.04709086065298607 ) ) ;
#17138=ORIENTED_EDGE ( 'NONE', *, *, #15674, .F. ) ;
#17139=ADVANCED_FACE ( 'NONE', ( #18257 ), #8568, .F. ) ;
#17147=VECTOR ( 'NONE', #3874, 1000.000000000000000 ) ;
#17151=ORIENTED_EDGE ( 'NONE', *, *, #13237, .F. ) ;
#17153=CARTESIAN_POINT ( 'NONE',  ( -8.786685647604894456, -23.24040270374358030, 48.22796981442792230 ) ) ;
#17156=CARTESIAN_POINT ( 'NONE',  ( -5.986830583229505898, 43.56094206392996426, 26.01297580803277754 ) ) ;
#17158=EDGE_CURVE ( 'NONE', #23320, #12154, #4204, .T. ) ;
#17164=ORIENTED_EDGE ( 'NONE', *, *, #14128, .T. ) ;
#17166=EDGE_CURVE ( 'NONE', #15111, #27426, #4551, .T. ) ;
#17172=ORIENTED_EDGE ( 'NONE', *, *, #20174, .F. ) ;
#17175=CARTESIAN_POINT ( 'NONE',  ( -20.20700224038492721, 27.82980252387819675, -10.08426345511598932 ) ) ;
#17177=CARTESIAN_POINT ( 'NONE',  ( -8.786685647604887350, 53.04920435127183254, 7.199674155859139724 ) ) ;
#17179=CARTESIAN_POINT ( 'NONE',  ( -8.786685647604898008, 48.22796981442802178, 23.24040270374343464 ) ) ;
#17184=CARTESIAN_POINT ( 'NONE',  ( -1.619063947482197729, -38.92136151114925724, -25.20140673341360227 ) ) ;
#17190=ORIENTED_EDGE ( 'NONE', *, *, #24530, .T. ) ;
#17191=CARTESIAN_POINT ( 'NONE',  ( -1.583189561560256253, -16.68617981233733261, -43.29471907393735819 ) ) ;
#17194=EDGE_CURVE ( 'NONE', #19755, #20942, #2466, .T. ) ;
#17202=CARTESIAN_POINT ( 'NONE',  ( -7.711401346138401891, 35.51061203065580685, 38.61705198405327621 ) ) ;
#17212=EDGE_CURVE ( 'NONE', #26877, #22293, #21984, .T. ) ;
#17224=B_SPLINE_CURVE_WITH_KNOTS ( 'NONE', 3,
 ( #16302, #20478, #760, #11986, #9545, #11845, #3072 ),
 .UNSPECIFIED., .F., .F.,
 ( 4, 3, 4 ),
 ( 1.201851678989727385E-17, 0.009512539173626329003, 0.02506242213020845599 ),
 .UNSPECIFIED. ) ;
#17226=CARTESIAN_POINT ( 'NONE',  ( -24.53239521893647890, -29.54733954334097135, 16.68574937151005599 ) ) ;
#17239=CARTESIAN_POINT ( 'NONE',  ( -28.41354790283022069, -12.60397206714818097, 19.47297445639563307 ) ) ;
#17241=CARTESIAN_POINT ( 'NONE',  ( -1.323439229708149867, 35.86372896917474407, -28.92147054731853828 ) ) ;
#17243=CARTESIAN_POINT ( 'NONE',  ( -20.20700224038492721, 28.44216453106548315, 8.199606986804035103 ) ) ;
#17247=ADVANCED_FACE ( 'NONE', ( #6601 ), #11052, .T. ) ;
#17251=VERTEX_POINT ( 'NONE', #25900 ) ;
#17252=EDGE_CURVE ( 'NONE', #12494, #18677, #1836, .T. ) ;
#17255=CARTESIAN_POINT ( 'NONE',  ( -1.048994561756789512, -43.78680886990931498, 13.42228657661168789 ) ) ;
#17256=CARTESIAN_POINT ( 'NONE',  ( -1.323439229708132547, 16.42345129173398632, 43.04565903621268319 ) ) ;
#17257=CARTESIAN_POINT ( 'NONE',  ( -4.162674018437125589, -31.44946543094270197, 37.46098494546626512 ) ) ;
#17259=CARTESIAN_POINT ( 'NONE',  ( -1.058473599757830730, 42.99101666105228503, -15.81436910992533029 ) ) ;
#17262=CARTESIAN_POINT ( 'NONE',  ( -7.711401346138401891, 52.11446537925913702, -6.030154970217080468 ) ) ;
#17263=CARTESIAN_POINT ( 'NONE',  ( -20.47566262905009538, -18.81547655725230328, 23.19796652405694459 ) ) ;
#17264=CARTESIAN_POINT ( 'NONE',  ( -25.21435515916043713, -30.48034229288650820, -16.39063784838731053 ) ) ;
#17268=B_SPLINE_CURVE_WITH_KNOTS ( 'NONE', 3,
 ( #2908, #16136, #12118, #597, #22929, #9666, #1031, #26921 ),
 .UNSPECIFIED., .F., .F.,
 ( 4, 2, 2, 4 ),
 ( 2.214340075454938295E-16, 0.002761568181852865067, 0.005523136363705506355, 0.01104627272741079066 ),
 .UNSPECIFIED. ) ;
#17270=VERTEX_POINT ( 'NONE', #17105 ) ;
#17276=EDGE_CURVE ( 'NONE', #12851, #15929, #18636, .T. ) ;
#17285=FACE_OUTER_BOUND ( 'NONE', #16781, .T. ) ;
#17288=CARTESIAN_POINT ( 'NONE',  ( -8.786685647604890903, -48.22796981442785835, -23.24040270374372952 ) ) ;
#17291=CARTESIAN_POINT ( 'NONE',  ( -1.539763995773690164, -44.72359274866473555, 11.93465967526341842 ) ) ;
#17295=EDGE_LOOP ( 'NONE', ( #122, #21317, #20703, #2022, #17164, #14871, #22734, #26314, #9199, #14064, #2314, #9375, #333, #480, #21462, #24197, #48, #14883, #20449, #22792, #19620, #17190, #27277, #26501, #19057, #26997, #5731, #15231, #16408, #18349, #15993, #18073, #11623, #25847, #8338, #26043, #20290, #13207, #15887, #19605, #8027, #23160, #23192, #6826, #14447, #16503, #19994, #14473, #4064, #10384, #9429, #9324, #9097, #2872, #3807, #27298, #25512, #16911, #12155, #9708, #27204, #25821, #5737, #16712 ) ) ;
#17304=EDGE_CURVE ( 'NONE', #17315, #24758, #26521, .T. ) ;
#17310=CARTESIAN_POINT ( 'NONE',  ( -15.02187109954785171, 45.93032478317463330, 6.234056423739666286 ) ) ;
#17311=DIRECTION ( 'NONE',  ( 0.000000000000000000, 1.000000000000000000, 0.000000000000000000 ) ) ;
#17312=CARTESIAN_POINT ( 'NONE',  ( -23.79223135445719350, 30.42557260166829636, 13.25822371132262845 ) ) ;
#17314=EDGE_LOOP ( 'NONE', ( #25306, #23341, #2150, #1787 ) ) ;
#17315=VERTEX_POINT ( 'NONE', #15790 ) ;
#17321=CARTESIAN_POINT ( 'NONE',  ( -1.619063947482201282, 38.92136151114908671, -25.20140673341387227 ) ) ;
#17328=ORIENTED_EDGE ( 'NONE', *, *, #20953, .F. ) ;
#17330=CARTESIAN_POINT ( 'NONE',  ( -25.21435515916043713, -4.655591116594118617, 34.29329011225960500 ) ) ;
#17337=EDGE_CURVE ( 'NONE', #5699, #23320, #9373, .T. ) ;
#17347=CARTESIAN_POINT ( 'NONE',  ( -55.24390624410018802, -0.001451500391952595045, 0.01032895241566660592 ) ) ;
#17349=B_SPLINE_CURVE_WITH_KNOTS ( 'NONE', 3,
 ( #22740, #13782, #5297, #20411, #7190, #22441, #17809, #9619 ),
 .UNSPECIFIED., .F., .F.,
 ( 4, 2, 2, 4 ),
 ( 0.000000000000000000, 0.002761524886576596435, 0.005523049773153192871, 0.01104609954630638054 ),
 .UNSPECIFIED. ) ;
#17350=ORIENTED_EDGE ( 'NONE', *, *, #11776, .T. ) ;
#17362=CARTESIAN_POINT ( 'NONE',  ( -4.473127245936431073, 12.17046501147583548, 47.80062405537787384 ) ) ;
#17364=ORIENTED_EDGE ( 'NONE', *, *, #9336, .T. ) ;
#17365=CARTESIAN_POINT ( 'NONE',  ( -8.786685647604890903, -25.35688121747466184, 47.14957014837381166 ) ) ;
#17373=EDGE_CURVE ( 'NONE', #22045, #3326, #7335, .T. ) ;
#17386=CARTESIAN_POINT ( 'NONE',  ( -1.619063947482194177, 25.20140673341374438, -38.92136151114915066 ) ) ;
#17389=ORIENTED_EDGE ( 'NONE', *, *, #1018, .F. ) ;
#17393=CARTESIAN_POINT ( 'NONE',  ( -28.41354790283022069, 23.16239616762931064, -1.249099604787157425 ) ) ;
#17396=CARTESIAN_POINT ( 'NONE',  ( -1.050230346682680560, 26.92058491724867153, -37.05182464821992028 ) ) ;
#17399=CARTESIAN_POINT ( 'NONE',  ( -2.911734481061402757, -12.03743348210748998, 46.11606034418773703 ) ) ;
#17400=CARTESIAN_POINT ( 'NONE',  ( -28.13707043255157103, -22.88591869784690402, 0.7675454997509406629 ) ) ;
#17401=CARTESIAN_POINT ( 'NONE',  ( -1.113427685306989767, -42.96952363574823863, 16.03057832159198171 ) ) ;
#17415=CARTESIAN_POINT ( 'NONE',  ( -4.473127245936431073, -3.196405119333463496, 49.22197550883370809 ) ) ;
#17421=CARTESIAN_POINT ( 'NONE',  ( -25.21435515916025594, 1.749597353048488237E-16, -4.373993382621220594E-17 ) ) ;
#17422=CARTESIAN_POINT ( 'NONE',  ( -18.41936578851709783, -18.42310649277602508, 38.22933728004711185 ) ) ;
#17426=CARTESIAN_POINT ( 'NONE',  ( -1.619063947482201282, -11.94059994246191359, -44.80407745103779860 ) ) ;
#17438=EDGE_CURVE ( 'NONE', #17941, #6242, #9248, .T. ) ;
#17446=CARTESIAN_POINT ( 'NONE',  ( -1.031422197589711764, 44.01264471863847660, -12.69107518035516691 ) ) ;
#17447=CARTESIAN_POINT ( 'NONE',  ( -1.048994561756786625, 37.49601524795411223, -26.29622118251694829 ) ) ;
#17448=FACE_OUTER_BOUND ( 'NONE', #17618, .T. ) ;
#17452=CARTESIAN_POINT ( 'NONE',  ( -55.24390624410018802, 0.007503127514278223366, 0.007245494385991344682 ) ) ;
#17470=VERTEX_POINT ( 'NONE', #1531 ) ;
#17472=EDGE_LOOP ( 'NONE', ( #2200, #19833, #22176, #4738 ) ) ;
#17473=EDGE_CURVE ( 'NONE', #26453, #11824, #20958, .T. ) ;
#17474=B_SPLINE_CURVE_WITH_KNOTS ( 'NONE', 3,
 ( #9634, #22756, #848, #20706, #5456, #13797, #9789 ),
 .UNSPECIFIED., .F., .F.,
 ( 4, 3, 4 ),
 ( 8.845388854693243284E-18, 0.009512539173626379310, 0.02506242213020843518 ),
 .UNSPECIFIED. ) ;
#17483=AXIS2_PLACEMENT_3D ( 'NONE', #26092, #5355, #13843 ) ;
#17484=CARTESIAN_POINT ( 'NONE',  ( -1.046935749540006011, 12.93334586714240331, 43.93230528057167561 ) ) ;
#17485=DIRECTION ( 'NONE',  ( -1.000000000000000000, 6.938893903907226837E-18, -1.734723475976806709E-18 ) ) ;
#17500=VERTEX_POINT ( 'NONE', #23427 ) ;
#17503=CARTESIAN_POINT ( 'NONE',  ( -1.031422197589711987, -45.78027046666441890, 1.530725436377941673 ) ) ;
#17510=EDGE_CURVE ( 'NONE', #8086, #2685, #11392, .T. ) ;
#17515=DIRECTION ( 'NONE',  ( 1.000000000000000000, -6.938893903907226837E-18, 1.734723475976806709E-18 ) ) ;
#17516=EDGE_LOOP ( 'NONE', ( #25785, #4091, #20402, #15772 ) ) ;
#17535=CARTESIAN_POINT ( 'NONE',  ( -18.41936578851712980, -41.75701384111727776, 7.566034416291218534 ) ) ;
#17540=CARTESIAN_POINT ( 'NONE',  ( -22.23226125620944771, 26.80886670319662102, 16.78323347921887887 ) ) ;
#17542=CARTESIAN_POINT ( 'NONE',  ( -20.20700224038492721, -28.44216453106542986, -8.199606986804219844 ) ) ;
#17544=CARTESIAN_POINT ( 'NONE',  ( -1.619063947482197729, -43.26576862488421682, 16.67502769180607203 ) ) ;
#17553=CARTESIAN_POINT ( 'NONE',  ( -1.239374126674604337, -42.99367564261289942, -16.50008610789281605 ) ) ;
#17558=FACE_OUTER_BOUND ( 'NONE', #4709, .T. ) ;
#17562=CARTESIAN_POINT ( 'NONE',  ( -55.24198130335446422, 0.008252882783650522525, -0.004276389980776339715 ) ) ;
#17565=EDGE_CURVE ( 'NONE', #12449, #21771, #25858, .T. ) ;
#17566=CARTESIAN_POINT ( 'NONE',  ( -55.24728320129491266, 0.01402509393918583563, -0.003868537197317189515 ) ) ;
#17572=CARTESIAN_POINT ( 'NONE',  ( -1.056502255334265339, -26.51074901220530222, -37.35734037467625512 ) ) ;
#17577=LINE ( 'NONE', #13257, #1872 ) ;
#17579=VERTEX_POINT ( 'NONE', #6155 ) ;
#17594=CARTESIAN_POINT ( 'NONE',  ( -22.34422965417124374, 17.95715691811047776, -33.39267070835825990 ) ) ;
#17597=CARTESIAN_POINT ( 'NONE',  ( -1.045287976400365970, 28.14015102489882736, 36.12803364096558312 ) ) ;
#17598=CARTESIAN_POINT ( 'NONE',  ( -55.24300891470648622, -0.009225237711097735230, -0.003362556190414862749 ) ) ;
#17606=CARTESIAN_POINT ( 'NONE',  ( -55.24198130335446422, 0.008310594958153458625, -0.004163123460802744397 ) ) ;
#17614=CARTESIAN_POINT ( 'NONE',  ( -55.24300891470650754, 0.0003472257464218577502, 0.009812809446892801005 ) ) ;
#17618=EDGE_LOOP ( 'NONE', ( #345, #22017, #1039, #179 ) ) ;
#17633=CARTESIAN_POINT ( 'NONE',  ( -1.045287976400362417, -43.05558670614257721, -15.59869763335051651 ) ) ;
#17634=CARTESIAN_POINT ( 'NONE',  ( -1.019300379054419947, 38.21680004809164899, -25.26451264419658571 ) ) ;
#17637=CARTESIAN_POINT ( 'NONE',  ( -28.13707043255157103, -22.00298671236735615, 6.342158660427235972 ) ) ;
#17641=CARTESIAN_POINT ( 'NONE',  ( -9.156249394959706578, 48.78605533024773422, 24.29252099376439489 ) ) ;
#17652=CARTESIAN_POINT ( 'NONE',  ( -22.23226125620929139, -31.55376588768476509, 2.179935373562780221 ) ) ;
#17661=CARTESIAN_POINT ( 'NONE',  ( -1.155031165708882979, 35.88345263711048716, -28.62780465193323920 ) ) ;
#17666=EDGE_CURVE ( 'NONE', #28126, #3264, #500, .T. ) ;
#17683=CARTESIAN_POINT ( 'NONE',  ( -8.259864102781671491, -9.986657004933254811, 52.06232470801721490 ) ) ;
#17690=CARTESIAN_POINT ( 'NONE',  ( -20.57838717382308147, 18.89542499756533545, 23.26537097894084383 ) ) ;
#17693=ORIENTED_EDGE ( 'NONE', *, *, #7105, .F. ) ;
#17694=VERTEX_POINT ( 'NONE', #9140 ) ;
#17700=ORIENTED_EDGE ( 'NONE', *, *, #6671, .T. ) ;
#17701=CARTESIAN_POINT ( 'NONE',  ( -55.24728320129491266, 0.01137345571546872526, -0.009072670231975240793 ) ) ;
#17705=EDGE_CURVE ( 'NONE', #17579, #7068, #4527, .T. ) ;
#17712=CARTESIAN_POINT ( 'NONE',  ( -55.25719721206881729, 0.009391134844733637840, 0.006045473558784292267 ) ) ;
#17718=AXIS2_PLACEMENT_3D ( 'NONE', #11809, #14091, #4895 ) ;
#17724=( BOUNDED_SURFACE ( )  B_SPLINE_SURFACE ( 3, 1, ( 
 ( #25796, #19168 ),
 ( #21327, #8108 ),
 ( #12397, #3478 ),
 ( #18742, #6094 ) ),
 .UNSPECIFIED., .F., .F., .F. ) 
 B_SPLINE_SURFACE_WITH_KNOTS ( ( 4, 4 ),
 ( 2, 2 ),
 ( 0.000000000000000000, 1.000000000000000000 ),
 ( 0.000000000000000000, 1.000000000000000000 ),
 .UNSPECIFIED. ) 
 GEOMETRIC_REPRESENTATION_ITEM ( )  RATIONAL_B_SPLINE_SURFACE ( (
 ( 1.000000000000000000, 1.000000000000000000),
 ( 0.7789835883360578528, 0.9689951854195403280),
 ( 0.7789835883360578528, 0.9689951854195403280),
 ( 1.000000000000000000, 1.000000000000000000) ) ) 
 REPRESENTATION_ITEM ( '' )  SURFACE ( )  );
#17725=ADVANCED_FACE ( 'NONE', ( #20497 ), #19247, .F. ) ;
#17730=VERTEX_POINT ( 'NONE', #11162 ) ;
#17732=EDGE_CURVE ( 'NONE', #4432, #7492, #9296, .T. ) ;
#17733=B_SPLINE_CURVE_WITH_KNOTS ( 'NONE', 3,
 ( #15927, #5135, #27144, #18521, #5276, #9600 ),
 .UNSPECIFIED., .F., .F.,
 ( 4, 2, 4 ),
 ( 1.607967956875964627E-16, 0.003570751334075640028, 0.007141502668151118727 ),
 .UNSPECIFIED. ) ;
#17747=CARTESIAN_POINT ( 'NONE',  ( -1.031422197589716205, -1.530725436377772031, -45.78027046666443312 ) ) ;
#17754=DIRECTION ( 'NONE',  ( 0.000000000000000000, 5.223019709707975211E-21, -1.000000000000000000 ) ) ;
#17761=( BOUNDED_SURFACE ( )  B_SPLINE_SURFACE ( 3, 1, ( 
 ( #23834, #1921 ),
 ( #21078, #25841 ),
 ( #1364, #28121 ),
 ( #10726, #6136 ) ),
 .UNSPECIFIED., .F., .F., .F. ) 
 B_SPLINE_SURFACE_WITH_KNOTS ( ( 4, 4 ),
 ( 2, 2 ),
 ( 0.000000000000000000, 1.000000000000000000 ),
 ( 0.000000000000000000, 1.000000000000000000 ),
 .UNSPECIFIED. ) 
 GEOMETRIC_REPRESENTATION_ITEM ( )  RATIONAL_B_SPLINE_SURFACE ( (
 ( 1.000000000000000000, 1.000000000000000000),
 ( 0.7789835883360576307, 0.9689951854195403280),
 ( 0.7789835883360576307, 0.9689951854195403280),
 ( 1.000000000000000000, 1.000000000000000000) ) ) 
 REPRESENTATION_ITEM ( '' )  SURFACE ( )  );
#17776=ORIENTED_EDGE ( 'NONE', *, *, #23236, .F. ) ;
#17785=FACE_OUTER_BOUND ( 'NONE', #1590, .T. ) ;
#17793=ORIENTED_EDGE ( 'NONE', *, *, #1976, .T. ) ;
#17797=CARTESIAN_POINT ( 'NONE',  ( -20.20997486282892552, 3.551351076220724598E-15, -29.60348406988233450 ) ) ;
#17801=CARTESIAN_POINT ( 'NONE',  ( -23.79248802219722592, -7.157555990716680583, 32.40806545715339126 ) ) ;
#17806=CARTESIAN_POINT ( 'NONE',  ( -1.046935749539997573, -25.87617179820943036, -37.78548154587986119 ) ) ;
#17809=CARTESIAN_POINT ( 'NONE',  ( -2.911734481061372115, -36.84482841982624990, 30.23325065583398441 ) ) ;
#17811=CARTESIAN_POINT ( 'NONE',  ( -8.786685647604894456, 37.00619870957989832, 38.68584556812258768 ) ) ;
#17816=CARTESIAN_POINT ( 'NONE',  ( -25.21435515916042647, 15.02493970636146692, -31.17620025257592786 ) ) ;
#17818=DIRECTION ( 'NONE',  ( 0.000000000000000000, 5.223019709707975211E-21, -1.000000000000000000 ) ) ;
#17824=ORIENTED_EDGE ( 'NONE', *, *, #11776, .F. ) ;
#17825=EDGE_CURVE ( 'NONE', #26529, #1301, #11381, .T. ) ;
#17827=VERTEX_POINT ( 'NONE', #19174 ) ;
#17831=EDGE_CURVE ( 'NONE', #9533, #864, #15820, .T. ) ;
#17843=CARTESIAN_POINT ( 'NONE',  ( -1.031422197589716205, 43.06660437151330711, 15.60268798220593389 ) ) ;
#17851=CARTESIAN_POINT ( 'NONE',  ( -1.155031165708877872, 38.31525684316177660, 25.28071330859845389 ) ) ;
#17855=CARTESIAN_POINT ( 'NONE',  ( -1.239374126674604337, -28.97829083655411964, 35.79060836339844087 ) ) ;
#17866=B_SPLINE_CURVE_WITH_KNOTS ( 'NONE', 3,
 ( #5011, #20980, #16831, #3566, #18980, #10483 ),
 .UNSPECIFIED., .F., .F.,
 ( 4, 2, 4 ),
 ( 0.000000000000000000, 0.0004335184443140195285, 0.0008670368886280390569 ),
 .UNSPECIFIED. ) ;
#17867=CARTESIAN_POINT ( 'NONE',  ( -20.57838717382308147, 7.715628353033680220, -28.96176188950220975 ) ) ;
#17870=CARTESIAN_POINT ( 'NONE',  ( -1.583189561560252701, 46.33203782964461936, 2.490696082060036343 ) ) ;
#17871=CARTESIAN_POINT ( 'NONE',  ( -18.41936578851713335, 20.09935324538248480, 37.37524689996173777 ) ) ;
#17873=ORIENTED_EDGE ( 'NONE', *, *, #5403, .F. ) ;
#17874=CARTESIAN_POINT ( 'NONE',  ( -1.239374126674604337, 2.406737988131122830, -45.98822239537607004 ) ) ;
#17875=CARTESIAN_POINT ( 'NONE',  ( -55.24198130335446422, -0.006527480770975599769, 0.006617369590168732142 ) ) ;
#17877=CYLINDRICAL_SURFACE ( 'NONE', #19018, 37.50000000000001421 ) ;
#17881=EDGE_LOOP ( 'NONE', ( #7556, #26531, #15805, #3796 ) ) ;
#17882=EDGE_LOOP ( 'NONE', ( #23389, #5420, #23077, #1651 ) ) ;
#17888=DIRECTION ( 'NONE',  ( 0.7563875759206388771, -0.4122509917856713724, 0.5078650950445698919 ) ) ;
#17895=CARTESIAN_POINT ( 'NONE',  ( -1.583189561560256253, 25.21827308671232615, -38.94740041318302559 ) ) ;
#17901=FACE_OUTER_BOUND ( 'NONE', #20459, .T. ) ;
#17907=CARTESIAN_POINT ( 'NONE',  ( -1.048996300304503082, -26.29666317565274980, 37.49570739463913327 ) ) ;
#17919=AXIS2_PLACEMENT_3D ( 'NONE', #21589, #6482, #19430 ) ;
#17920=DIRECTION ( 'NONE',  ( 1.000000000000000000, -6.938893903907226837E-18, 1.734723475976806709E-18 ) ) ;
#17921=CARTESIAN_POINT ( 'NONE',  ( -1.044556982611269058, -36.05793013899078403, 28.22896456560707534 ) ) ;
#17922=VECTOR ( 'NONE', #27077, 1000.000000000000000 ) ;
#17923=ORIENTED_EDGE ( 'NONE', *, *, #17666, .F. ) ;
#17928=CARTESIAN_POINT ( 'NONE',  ( -24.53237795827028478, -30.86653739599989521, 14.09663893005617119 ) ) ;
#17929=ORIENTED_EDGE ( 'NONE', *, *, #18959, .T. ) ;
#17930=B_SPLINE_CURVE_WITH_KNOTS ( 'NONE', 3,
 ( #4121, #17079, #6432, #15183, #12891, #15047, #24005, #13043, #1810, #23736 ),
 .UNSPECIFIED., .F., .F.,
 ( 4, 2, 2, 2, 4 ),
 ( 2.799181570144685938E-16, 0.0003346187017559026423, 0.0006692374035115253436, 0.001003856105267148099, 0.001338474807022770746 ),
 .UNSPECIFIED. ) ;
#17932=CARTESIAN_POINT ( 'NONE',  ( -23.79223135445719706, -22.01133905265668034, 24.83942264280426926 ) ) ;
#17937=EDGE_LOOP ( 'NONE', ( #1721, #14217, #16613, #13687 ) ) ;
#17941=VERTEX_POINT ( 'NONE', #18956 ) ;
#17946=CARTESIAN_POINT ( 'NONE',  ( -7.078251931573400491, -44.92740138729146082, 26.33626633876272649 ) ) ;
#17947=CARTESIAN_POINT ( 'NONE',  ( -1.583189561560253589, -16.68617981233733616, -43.29471907393735819 ) ) ;
#17956=DIRECTION ( 'NONE',  ( 1.000000000000000000, -6.938893903907226837E-18, 1.734723475976806709E-18 ) ) ;
#17969=MECHANICAL_DESIGN_GEOMETRIC_PRESENTATION_REPRESENTATION('',(#12904),#7888);
#17972=VECTOR ( 'NONE', #5254, 999.9999999999998863 ) ;
#17976=CARTESIAN_POINT ( 'NONE',  ( -21.41430102051752016, 11.22990201072317262, 28.68859753627381792 ) ) ;
#17981=ORIENTED_EDGE ( 'NONE', *, *, #153, .F. ) ;
#17983=EDGE_CURVE ( 'NONE', #15703, #27510, #21672, .T. ) ;
#17985=DIRECTION ( 'NONE',  ( 0.7637818620346800147, 0.5092696688508698832, 0.3965875333584785167 ) ) ;
#17987=CARTESIAN_POINT ( 'NONE',  ( -7.078251931573400491, -51.82710018979479116, -5.101176922830485516 ) ) ;
#17989=CARTESIAN_POINT ( 'NONE',  ( -12.94347594948484037, -35.22469990145630447, -33.69581619287863106 ) ) ;
#17990=CARTESIAN_POINT ( 'NONE',  ( -2.265401668238146815, -25.45016726748341540, -39.53028715828224904 ) ) ;
#17994=CARTESIAN_POINT ( 'NONE',  ( -55.24198130335446422, 0.004163123460802997666, 0.008310594958152995454 ) ) ;
#17996=ADVANCED_FACE ( 'NONE', ( #2215 ), #13371, .F. ) ;
#17998=AXIS2_PLACEMENT_3D ( 'NONE', #159, #6, #11238 ) ;
#18001=CARTESIAN_POINT ( 'NONE',  ( -55.24271866751342941, 0.001425019990782615698, -0.009388511352197861579 ) ) ;
#18004=VERTEX_POINT ( 'NONE', #22393 ) ;
#18009=CARTESIAN_POINT ( 'NONE',  ( -1.019300379054419725, 45.76814864815091255, -2.023851374322835017 ) ) ;
#18010=CARTESIAN_POINT ( 'NONE',  ( -8.786685647604892679, -53.04920435127177569, 7.199674155859498548 ) ) ;
#18012=AXIS2_PLACEMENT_3D ( 'NONE', #3289, #5745, #27456 ) ;
#18026=B_SPLINE_CURVE_WITH_KNOTS ( 'NONE', 3,
 ( #20979, #26246, #21274, #8694, #1265, #14508 ),
 .UNSPECIFIED., .F., .F.,
 ( 4, 2, 4 ),
 ( 6.505213034913026604E-19, 0.0004335151646191478343, 0.0008670303292382950180 ),
 .UNSPECIFIED. ) ;
#18032=EDGE_LOOP ( 'NONE', ( #28408, #26787, #19947, #9701 ) ) ;
#18035=CARTESIAN_POINT ( 'NONE',  ( -8.259864102781671491, -22.52209142944967368, -47.98931516265586339 ) ) ;
#18040=EDGE_CURVE ( 'NONE', #9315, #1788, #24410, .T. ) ;
#18046=ORIENTED_EDGE ( 'NONE', *, *, #27328, .T. ) ;
#18051=CARTESIAN_POINT ( 'NONE',  ( -1.046935749540007343, -12.93334586714209777, -43.93230528057176798 ) ) ;
#18056=( BOUNDED_SURFACE ( )  B_SPLINE_SURFACE ( 3, 1, ( 
 ( #17065, #1661 ),
 ( #27574, #7893 ),
 ( #13027, #28273 ),
 ( #11018, #2357 ) ),
 .UNSPECIFIED., .F., .F., .F. ) 
 B_SPLINE_SURFACE_WITH_KNOTS ( ( 4, 4 ),
 ( 2, 2 ),
 ( 0.000000000000000000, 1.000000000000000000 ),
 ( 0.000000000000000000, 1.000000000000000000 ),
 .UNSPECIFIED. ) 
 GEOMETRIC_REPRESENTATION_ITEM ( )  RATIONAL_B_SPLINE_SURFACE ( (
 ( 1.000000000000000000, 1.000000000000000000),
 ( 0.9934239774497838349, 0.8357310067453913582),
 ( 0.9934239774497838349, 0.8357310067453913582),
 ( 1.000000000000000000, 1.000000000000000000) ) ) 
 REPRESENTATION_ITEM ( '' )  SURFACE ( )  );
#18068=ORIENTED_EDGE ( 'NONE', *, *, #5609, .F. ) ;
#18069=CARTESIAN_POINT ( 'NONE',  ( -25.21435515916043713, -34.05351380035328646, 6.169479169075816394 ) ) ;
#18073=ORIENTED_EDGE ( 'NONE', *, *, #18379, .T. ) ;
#18075=ORIENTED_EDGE ( 'NONE', *, *, #18040, .F. ) ;
#18079=CARTESIAN_POINT ( 'NONE',  ( -20.57838717382308147, -29.92853265176832878, -1.611677988432255848 ) ) ;
#18090=DIRECTION ( 'NONE',  ( 0.000000000000000000, -5.223019709708116647E-21, 1.000000000000000000 ) ) ;
#18093=B_SPLINE_CURVE_WITH_KNOTS ( 'NONE', 3,
 ( #4197, #21767, #25681, #2030, #14576, #8662, #23805, #14859, #17291, #3785 ),
 .UNSPECIFIED., .F., .F.,
 ( 4, 2, 2, 2, 4 ),
 ( 2.847672227753435151E-16, 0.0003346187017559057865, 0.0006692374035115268615, 0.001003856105267147665, 0.001338474807022768795 ),
 .UNSPECIFIED. ) ;
#18103=CARTESIAN_POINT ( 'NONE',  ( -55.24340739397742084, 0.008612749836246956503, -0.005344433640973183380 ) ) ;
#18106=ORIENTED_EDGE ( 'NONE', *, *, #28134, .F. ) ;
#18108=CARTESIAN_POINT ( 'NONE',  ( -1.045287976400383290, 36.12803364096649972, 28.14015102489766917 ) ) ;
#18110=DIRECTION ( 'NONE',  ( -5.541455922705464902E-20, 5.223019709708320524E-21, -1.000000000000000000 ) ) ;
#18113=ORIENTED_EDGE ( 'NONE', *, *, #20410, .F. ) ;
#18123=CARTESIAN_POINT ( 'NONE',  ( -25.21435515916043002, 4.655591116594353984, -34.29329011225956947 ) ) ;
#18124=EDGE_CURVE ( 'NONE', #21826, #27931, #20231, .T. ) ;
#18126=EDGE_CURVE ( 'NONE', #22671, #24458, #23036, .T. ) ;
#18127=CARTESIAN_POINT ( 'NONE',  ( -22.34422965417122597, 16.46028608106157876, 34.15536449444073241 ) ) ;
#18128=CARTESIAN_POINT ( 'NONE',  ( -20.20700224038492365, 23.35150625415685255, 18.19058640100197977 ) ) ;
#18131=CARTESIAN_POINT ( 'NONE',  ( -23.79248802219728276, 13.25839849636400203, 30.42578156345371454 ) ) ;
#18137=CARTESIAN_POINT ( 'NONE',  ( -2.911734481061404534, -2.802366807346520439, -47.57875121082949477 ) ) ;
#18141=CARTESIAN_POINT ( 'NONE',  ( -1.155001620486259206, 44.25209926692307505, -12.20337535396694051 ) ) ;
#18143=CARTESIAN_POINT ( 'NONE',  ( -1.019300379054419947, -16.06793277091962935, 42.90269154183443590 ) ) ;
#18152=EDGE_CURVE ( 'NONE', #27648, #18231, #23692, .T. ) ;
#18161=CARTESIAN_POINT ( 'NONE',  ( -1.058197053496165108, -15.81317659443655721, 42.99116279335168400 ) ) ;
#18165=CARTESIAN_POINT ( 'NONE',  ( -22.23342874802668234, -16.78332232459660389, -26.81018246605532340 ) ) ;
#18166=CARTESIAN_POINT ( 'NONE',  ( -1.045287976400365970, -45.76855895860947498, -1.530335034933654859 ) ) ;
#18168=CARTESIAN_POINT ( 'NONE',  ( -20.21097721650786738, -24.14932365326965069, -17.13687097598128517 ) ) ;
#18176=CARTESIAN_POINT ( 'NONE',  ( -7.711401346138392121, -21.83927363365067364, -47.70038152767084227 ) ) ;
#18180=CARTESIAN_POINT ( 'NONE',  ( -22.23342874802667879, -29.33662284748868387, -11.82490389046302859 ) ) ;
#18185=ADVANCED_FACE ( 'NONE', ( #24612 ), #12594, .F. ) ;
#18189=FACE_OUTER_BOUND ( 'NONE', #11816, .T. ) ;
#18199=CARTESIAN_POINT ( 'NONE',  ( -55.24271866751342941, -0.004365563123935077734, -0.008433070970613952902 ) ) ;
#18204=DIRECTION ( 'NONE',  ( 0.7637818620346801257, 0.5345501402766276167, -0.3617919495470772184 ) ) ;
#18209=ORIENTED_EDGE ( 'NONE', *, *, #12803, .T. ) ;
#18211=ORIENTED_EDGE ( 'NONE', *, *, #18851, .F. ) ;
#18212=CARTESIAN_POINT ( 'NONE',  ( -1.323439229708125886, 2.317790194800380288, 46.01398008004440499 ) ) ;
#18214=EDGE_CURVE ( 'NONE', #7707, #19215, #19223, .T. ) ;
#18216=VERTEX_POINT ( 'NONE', #9479 ) ;
#18229=CARTESIAN_POINT ( 'NONE',  ( -55.24728320129491266, -0.005114031043468280843, 0.01362040845703383143 ) ) ;
#18231=VERTEX_POINT ( 'NONE', #12065 ) ;
#18232=ORIENTED_EDGE ( 'NONE', *, *, #16418, .T. ) ;
#18234=CARTESIAN_POINT ( 'NONE',  ( -55.25719721206881729, -0.01041086141212241994, -0.004044147484874939351 ) ) ;
#18236=CARTESIAN_POINT ( 'NONE',  ( -7.733045908741323693, -35.49239760110648945, 38.67583825854190138 ) ) ;
#18241=ORIENTED_EDGE ( 'NONE', *, *, #22568, .T. ) ;
#18249=CARTESIAN_POINT ( 'NONE',  ( -20.57838717382308147, 7.715628353034087894, 28.96176188950209962 ) ) ;
#18257=FACE_OUTER_BOUND ( 'NONE', #3336, .T. ) ;
#18259=CARTESIAN_POINT ( 'NONE',  ( -12.82751273423880001, 21.21958768041857724, 44.03362901246980243 ) ) ;
#18267=B_SPLINE_CURVE_WITH_KNOTS ( 'NONE', 3,
 ( #842, #8061, #27463, #1408, #9926, #3438, #16385, #16531, #25321, #16832, #12489, #23314, #14208 ),
 .UNSPECIFIED., .F., .F.,
 ( 4, 3, 3, 3, 4 ),
 ( 8.673617379884035472E-18, 0.0007657099931970526470, 0.001531419946797914385, 0.002296279302920149496, 0.003061450627205760701 ),
 .UNSPECIFIED. ) ;
#18276=DIRECTION ( 'NONE',  ( 1.000000000000000000, -6.938893903907226837E-18, 1.734723475976806709E-18 ) ) ;
#18279=EDGE_CURVE ( 'NONE', #27772, #14162, #5470, .T. ) ;
#18289=CARTESIAN_POINT ( 'NONE',  ( -18.41936578851705519, -42.05131332928132082, -5.707900577128024011 ) ) ;
#18298=LINE ( 'NONE', #5505, #17922 ) ;
#18303=ADVANCED_FACE ( 'NONE', ( #548 ), #3789, .F. ) ;
#18306=CARTESIAN_POINT ( 'NONE',  ( -1.048994561756784405, -37.49601524795390617, 26.29622118251720764 ) ) ;
#18312=EDGE_CURVE ( 'NONE', #8086, #10267, #23169, .T. ) ;
#18314=CARTESIAN_POINT ( 'NONE',  ( -8.786685647604885574, 6.096987947571466530E-17, -1.524246986892866633E-17 ) ) ;
#18316=VERTEX_POINT ( 'NONE', #16818 ) ;
#18318=ORIENTED_EDGE ( 'NONE', *, *, #15785, .F. ) ;
#18323=DIRECTION ( 'NONE',  ( 0.000000000000000000, 5.223019709707975211E-21, -1.000000000000000000 ) ) ;
#18326=CARTESIAN_POINT ( 'NONE',  ( -8.786685647604887350, -25.35688121747534751, -47.14957014837345639 ) ) ;
#18328=CARTESIAN_POINT ( 'NONE',  ( -1.019300379054419947, 16.06793277091992067, -42.90269154183433642 ) ) ;
#18330=CARTESIAN_POINT ( 'NONE',  ( -55.25719721206881729, -0.002847566758683717138, -0.01079965405819494247 ) ) ;
#18340=CARTESIAN_POINT ( 'NONE',  ( -8.786685647604890903, -9.545808661480982948, -52.67761315067281913 ) ) ;
#18343=CARTESIAN_POINT ( 'NONE',  ( -1.463510566862834983, -35.90603835816524025, -29.09194585123821497 ) ) ;
#18344=ORIENTED_EDGE ( 'NONE', *, *, #8857, .T. ) ;
#18349=ORIENTED_EDGE ( 'NONE', *, *, #24418, .T. ) ;
#18350=CARTESIAN_POINT ( 'NONE',  ( -20.20700224038492010, 16.58740185276710832, -24.51628800869052682 ) ) ;
#18352=B_SPLINE_CURVE_WITH_KNOTS ( 'NONE', 3,
 ( #18826, #5883, #1129, #7917, #18684, #16677, #10214, #25471, #18974, #23595 ),
 .UNSPECIFIED., .F., .F.,
 ( 4, 2, 2, 2, 4 ),
 ( 2.863532086325413454E-16, 0.0003346187017559052986, 0.0006692374035115242594, 0.001003856105267143329, 0.001338474807022762289 ),
 .UNSPECIFIED. ) ;
#18358=CARTESIAN_POINT ( 'NONE',  ( -9.156249394959706578, -38.17928057391962682, 38.89149400288449243 ) ) ;
#18359=ORIENTED_EDGE ( 'NONE', *, *, #1846, .T. ) ;
#18368=CARTESIAN_POINT ( 'NONE',  ( -55.24390624410018802, 0.004896917417131886954, -0.009209468562452662738 ) ) ;
#18379=EDGE_CURVE ( 'NONE', #16312, #4790, #5164, .T. ) ;
#18383=CARTESIAN_POINT ( 'NONE',  ( -1.583189561560256253, -11.94859433442871399, 44.83405390829683057 ) ) ;
#18391=ADVANCED_FACE ( 'NONE', ( #7762 ), #9672, .F. ) ;
#18393=B_SPLINE_CURVE_WITH_KNOTS ( 'NONE', 3,
 ( #2834, #5271, #20385, #669, #22417, #18079 ),
 .UNSPECIFIED., .F., .F.,
 ( 4, 2, 4 ),
 ( 3.607901639910057446E-16, 0.003576372551511165700, 0.007152745103021970578 ),
 .UNSPECIFIED. ) ;
#18397=ORIENTED_EDGE ( 'NONE', *, *, #8741, .T. ) ;
#18415=ORIENTED_EDGE ( 'NONE', *, *, #11971, .F. ) ;
#18439=VECTOR ( 'NONE', #21375, 1000.000000000000114 ) ;
#18449=DIRECTION ( 'NONE',  ( 0.000000000000000000, 5.223019709708233256E-21, -1.000000000000000000 ) ) ;
#18450=CARTESIAN_POINT ( 'NONE',  ( -15.02187109954776290, -45.93032478317472567, -6.234056423739352759 ) ) ;
#18452=EDGE_CURVE ( 'NONE', #14622, #18231, #28287, .T. ) ;
#18464=CARTESIAN_POINT ( 'NONE',  ( -24.53239521893651442, -14.09666242510773948, 30.86654523348680002 ) ) ;
#18466=CIRCLE ( 'NONE', #23538, 53.53553390275978785 ) ;
#18468=CARTESIAN_POINT ( 'NONE',  ( -55.24728320129491266, 0.01362040845703433277, 0.005114031043468512429 ) ) ;
#18471=CARTESIAN_POINT ( 'NONE',  ( -2.265401668238153032, -11.98901689611074062, -45.46007138824035820 ) ) ;
#18475=CARTESIAN_POINT ( 'NONE',  ( -1.049817751779881680, 43.71287583013727129, -13.66628317065001674 ) ) ;
#18476=FACE_OUTER_BOUND ( 'NONE', #7096, .T. ) ;
#18485=( BOUNDED_SURFACE ( )  B_SPLINE_SURFACE ( 3, 1, ( 
 ( #611, #13842 ),
 ( #16145, #2920 ),
 ( #11399, #890 ),
 ( #4926, #22649 ) ),
 .UNSPECIFIED., .F., .F., .F. ) 
 B_SPLINE_SURFACE_WITH_KNOTS ( ( 4, 4 ),
 ( 2, 2 ),
 ( 0.000000000000000000, 1.000000000000000000 ),
 ( 0.000000000000000000, 1.000000000000000000 ),
 .UNSPECIFIED. ) 
 GEOMETRIC_REPRESENTATION_ITEM ( )  RATIONAL_B_SPLINE_SURFACE ( (
 ( 1.000000000000000000, 1.000000000000000000),
 ( 0.9934239774497838349, 0.8357310067453913582),
 ( 0.9934239774497838349, 0.8357310067453913582),
 ( 1.000000000000000000, 1.000000000000000000) ) ) 
 REPRESENTATION_ITEM ( '' )  SURFACE ( )  );
#18495=ORIENTED_EDGE ( 'NONE', *, *, #8553, .F. ) ;
#18497=CARTESIAN_POINT ( 'NONE',  ( -1.019300379054419947, -2.023851374322355845, 45.76814864815092676 ) ) ;
#18513=B_SPLINE_CURVE_WITH_KNOTS ( 'NONE', 3,
 ( #1718, #21583, #12660, #21444, #3892, #27921, #6210, #17259, #1999, #26048 ),
 .UNSPECIFIED., .F., .F.,
 ( 4, 2, 2, 2, 4 ),
 ( 4.210279659405072890E-18, 0.0003346267210630959280, 0.0006692534421261876277, 0.001003880163189279110, 0.001338506884252370919 ),
 .UNSPECIFIED. ) ;
#18516=CARTESIAN_POINT ( 'NONE',  ( -1.583189561560256253, 36.01941156322789794, -29.24830400313178203 ) ) ;
#18520=CARTESIAN_POINT ( 'NONE',  ( -1.323830074806768398, -43.04593525292981582, -16.42382241777520946 ) ) ;
#18521=CARTESIAN_POINT ( 'NONE',  ( -23.79248802219731473, -16.82188324679459868, 28.61009539422402881 ) ) ;
#18522=ADVANCED_FACE ( 'NONE', ( #15182 ), #14284, .T. ) ;
#18529=FACE_OUTER_BOUND ( 'NONE', #28248, .T. ) ;
#18533=CARTESIAN_POINT ( 'NONE',  ( -55.25719721206881729, 0.008651607285660455754, 0.007063345920777159767 ) ) ;
#18538=ORIENTED_EDGE ( 'NONE', *, *, #1536, .T. ) ;
#18543=CARTESIAN_POINT ( 'NONE',  ( -20.20700224038492010, -0.9908225410480588913, -29.58392382092672435 ) ) ;
#18557=DIRECTION ( 'NONE',  ( 0.7637818620346801257, -0.5092696688508668856, -0.3965875333584823470 ) ) ;
#18558=AXIS2_PLACEMENT_3D ( 'NONE', #18565, #1281, #22762 ) ;
#18560=CARTESIAN_POINT ( 'NONE',  ( -20.57838717382308147, 16.28767523336121315, -25.16001208503110931 ) ) ;
#18565=CARTESIAN_POINT ( 'NONE',  ( -8.786685647604885574, 6.096987947571466530E-17, -1.524246986892866633E-17 ) ) ;
#18566=CARTESIAN_POINT ( 'NONE',  ( -1.050230346682684113, -43.55729751025872787, -14.15335421912565828 ) ) ;
#18568=EDGE_CURVE ( 'NONE', #2788, #4272, #15087, .T. ) ;
#18569=CARTESIAN_POINT ( 'NONE',  ( -20.20700224038492721, 23.35150625415659320, -18.19058640100232438 ) ) ;
#18579=CARTESIAN_POINT ( 'NONE',  ( -7.078251931573400491, -26.33626633876254886, -44.92740138729156030 ) ) ;
#18581=LINE ( 'NONE', #17393, #23945 ) ;
#18593=VERTEX_POINT ( 'NONE', #13599 ) ;
#18598=ADVANCED_FACE ( 'NONE', ( #361 ), #18620, .F. ) ;
#18601=ADVANCED_FACE ( 'NONE', ( #16192 ), #10718, .F. ) ;
#18604=EDGE_CURVE ( 'NONE', #457, #16924, #2815, .T. ) ;
#18615=LINE ( 'NONE', #5513, #1085 ) ;
#18616=CARTESIAN_POINT ( 'NONE',  ( -1.619063947482194177, 35.99532424477422410, 29.22875152547716482 ) ) ;
#18618=ORIENTED_EDGE ( 'NONE', *, *, #7453, .T. ) ;
#18620=( BOUNDED_SURFACE ( )  B_SPLINE_SURFACE ( 3, 1, ( 
 ( #9728, #24849 ),
 ( #27120, #4967 ),
 ( #27271, #5111 ),
 ( #13740, #22402 ) ),
 .UNSPECIFIED., .F., .F., .F. ) 
 B_SPLINE_SURFACE_WITH_KNOTS ( ( 4, 4 ),
 ( 2, 2 ),
 ( 0.000000000000000000, 1.000000000000000000 ),
 ( 0.000000000000000000, 1.000000000000000000 ),
 .UNSPECIFIED. ) 
 GEOMETRIC_REPRESENTATION_ITEM ( )  RATIONAL_B_SPLINE_SURFACE ( (
 ( 1.000000000000000000, 1.000000000000000000),
 ( 0.9593753223639863714, 0.9995975284513187731),
 ( 0.9593753223639863714, 0.9995975284513187731),
 ( 1.000000000000000000, 1.000000000000000000) ) ) 
 REPRESENTATION_ITEM ( '' )  SURFACE ( )  );
#18621=ORIENTED_EDGE ( 'NONE', *, *, #3667, .T. ) ;
#18636=B_SPLINE_CURVE_WITH_KNOTS ( 'NONE', 3,
 ( #19819, #19545, #109, #17241, #4288, #17661, #8479, #13069, #1703, #10499 ),
 .UNSPECIFIED., .F., .F.,
 ( 4, 2, 2, 2, 4 ),
 ( 0.000000000000000000, 0.0003346267210630939765, 0.0006692534421261879529, 0.001003880163189281929, 0.001338506884252375906 ),
 .UNSPECIFIED. ) ;
#18647=CARTESIAN_POINT ( 'NONE',  ( -1.539763995773692828, -35.94321074656915016, -29.16712963492449973 ) ) ;
#18650=CARTESIAN_POINT ( 'NONE',  ( -1.031422197589711987, 1.530725436378101989, 45.78027046666441180 ) ) ;
#18654=EDGE_CURVE ( 'NONE', #18677, #11017, #1692, .T. ) ;
#18656=ORIENTED_EDGE ( 'NONE', *, *, #10514, .F. ) ;
#18664=ORIENTED_EDGE ( 'NONE', *, *, #4579, .F. ) ;
#18667=CARTESIAN_POINT ( 'NONE',  ( -55.25297051322618813, 0.01306918787467309905, 0.007247191603128975632 ) ) ;
#18677=VERTEX_POINT ( 'NONE', #21766 ) ;
#18682=CARTESIAN_POINT ( 'NONE',  ( -1.031422197589716205, 37.93675465142509751, 25.67058493451402157 ) ) ;
#18684=CARTESIAN_POINT ( 'NONE',  ( -1.155001620486249214, -12.20337535396710749, -44.25209926692303952 ) ) ;
#18686=CARTESIAN_POINT ( 'NONE',  ( -20.90916690077966322, 35.64494649500682755, -17.17795951644668762 ) ) ;
#18688=ORIENTED_EDGE ( 'NONE', *, *, #22365, .T. ) ;
#18707=VERTEX_POINT ( 'NONE', #17426 ) ;
#18711=CARTESIAN_POINT ( 'NONE',  ( -4.780792508754330150, 48.13366140756558309, -11.68149851467477340 ) ) ;
#18717=CARTESIAN_POINT ( 'NONE',  ( -10.86508079875782329, -46.07061504567103327, -22.20099862734805996 ) ) ;
#18719=CARTESIAN_POINT ( 'NONE',  ( -21.81686047589425925, 34.70276904128910189, 16.72402253294277230 ) ) ;
#18720=CARTESIAN_POINT ( 'NONE',  ( -1.619063947482201282, 11.94059994246159384, -44.80407745103787676 ) ) ;
#18737=EDGE_CURVE ( 'NONE', #8126, #7229, #6518, .T. ) ;
#18742=CARTESIAN_POINT ( 'NONE',  ( -55.24390624410018802, 0.004896917417128144288, 0.009209468562451129242 ) ) ;
#18743=CARTESIAN_POINT ( 'NONE',  ( -23.79248802219729697, -24.83956736572394064, 22.01156985585195258 ) ) ;
#18745=FACE_OUTER_BOUND ( 'NONE', #24739, .T. ) ;
#18749=CARTESIAN_POINT ( 'NONE',  ( -20.20612091757426043, 24.59769958242388910, -16.46550228026404028 ) ) ;
#18750=CARTESIAN_POINT ( 'NONE',  ( -20.57838717382308147, -28.96176188950213870, 7.715628353033985753 ) ) ;
#18752=CARTESIAN_POINT ( 'NONE',  ( -1.323439229708146536, -25.17120723334064891, 38.58845475799796532 ) ) ;
#18759=CARTESIAN_POINT ( 'NONE',  ( -1.058473599757816963, 25.48501014712399737, -38.06357893967437889 ) ) ;
#18766=ADVANCED_FACE ( 'NONE', ( #20302 ), #4826, .F. ) ;
#18770=AXIS2_PLACEMENT_3D ( 'NONE', #376, #17920, #28303 ) ;
#18771=VECTOR ( 'NONE', #18204, 999.9999999999998863 ) ;
#18776=CARTESIAN_POINT ( 'NONE',  ( -25.21435515916043357, -16.39063784838764093, -30.48034229288631991 ) ) ;
#18778=CARTESIAN_POINT ( 'NONE',  ( -7.733045908741329022, -47.75066202881810540, -21.80378472388470001 ) ) ;
#18785=EDGE_CURVE ( 'NONE', #13365, #26863, #10376, .T. ) ;
#18793=EDGE_CURVE ( 'NONE', #10995, #16671, #25459, .T. ) ;
#18796=ADVANCED_FACE ( 'NONE', ( #9232 ), #14737, .F. ) ;
#18801=ORIENTED_EDGE ( 'NONE', *, *, #9862, .T. ) ;
#18815=DIRECTION ( 'NONE',  ( 1.000000000000000000, -6.938893903907226837E-18, 1.734723475976806709E-18 ) ) ;
#18818=ORIENTED_EDGE ( 'NONE', *, *, #6536, .T. ) ;
#18819=CARTESIAN_POINT ( 'NONE',  ( -55.24300891470650754, -0.006048736206179085827, -0.007734635432136639961 ) ) ;
#18826=CARTESIAN_POINT ( 'NONE',  ( -1.045287976400383290, -12.68782741917353185, -44.00138577190637079 ) ) ;
#18834=CARTESIAN_POINT ( 'NONE',  ( -1.044556982611280604, 44.03203163107544071, 12.57890920527730394 ) ) ;
#18844=VERTEX_POINT ( 'NONE', #23213 ) ;
#18845=CARTESIAN_POINT ( 'NONE',  ( -1.113548883309551485, -1.968251867498553409, 45.82026503946953255 ) ) ;
#18848=CARTESIAN_POINT ( 'NONE',  ( -1.048996300304514850, -45.79145529752467070, 0.7649764263856586588 ) ) ;
#18850=CARTESIAN_POINT ( 'NONE',  ( -25.21435515916043713, -15.02493970636168896, -31.17620025257581062 ) ) ;
#18851=EDGE_CURVE ( 'NONE', #5379, #15303, #22387, .T. ) ;
#18863=DIRECTION ( 'NONE',  ( 0.000000000000000000, 5.223019709708233256E-21, -1.000000000000000000 ) ) ;
#18869=VERTEX_POINT ( 'NONE', #7231 ) ;
#18871=FACE_OUTER_BOUND ( 'NONE', #19711, .T. ) ;
#18873=CARTESIAN_POINT ( 'NONE',  ( -8.786685647604890903, 52.67761315067286176, -9.545808661480789326 ) ) ;
#18875=ORIENTED_EDGE ( 'NONE', *, *, #25823, .T. ) ;
#18887=CIRCLE ( 'NONE', #17483, 12.50000000000000000 ) ;
#18892=ORIENTED_EDGE ( 'NONE', *, *, #8265, .T. ) ;
#18906=CARTESIAN_POINT ( 'NONE',  ( -25.21435515916043713, 6.169479169075932745, 34.05351380035326514 ) ) ;
#18911=CARTESIAN_POINT ( 'NONE',  ( -1.046935749540010674, 43.93230528057182482, -12.93334586714193790 ) ) ;
#18917=B_SPLINE_CURVE_WITH_KNOTS ( 'NONE', 3,
 ( #25097, #5363, #21039, #14129, #18749, #1328 ),
 .UNSPECIFIED., .F., .F.,
 ( 4, 2, 4 ),
 ( 0.000000000000000000, 0.0004335151646191511953, 0.0008670303292383023906 ),
 .UNSPECIFIED. ) ;
#18939=FACE_OUTER_BOUND ( 'NONE', #3255, .T. ) ;
#18944=CARTESIAN_POINT ( 'NONE',  ( -1.155031165708884755, -38.31525684316158475, -25.28071330859873100 ) ) ;
#18955=CARTESIAN_POINT ( 'NONE',  ( -55.24728320129491266, 0.009072670231975488858, 0.01137345571546827770 ) ) ;
#18956=CARTESIAN_POINT ( 'NONE',  ( -8.786685647604898008, 48.22796981442802178, 23.24040270374343464 ) ) ;
#18959=EDGE_CURVE ( 'NONE', #24758, #7039, #13447, .T. ) ;
#18960=VERTEX_POINT ( 'NONE', #14684 ) ;
#18969=CARTESIAN_POINT ( 'NONE',  ( -55.24271866751342941, -0.004365563123939053720, 0.008433070970613821063 ) ) ;
#18974=CARTESIAN_POINT ( 'NONE',  ( -1.539763995773685057, -11.93465967526326921, -44.72359274866478529 ) ) ;
#18976=CARTESIAN_POINT ( 'NONE',  ( -1.058197053496158890, 12.47644286888577270, 44.07533330186774378 ) ) ;
#18980=CARTESIAN_POINT ( 'NONE',  ( -20.47566338032508426, 1.586617869344308041, 29.82700953060495408 ) ) ;
#18984=CARTESIAN_POINT ( 'NONE',  ( -21.81686047589426281, -18.24499610240063419, -33.92779429964196680 ) ) ;
#18992=CARTESIAN_POINT ( 'NONE',  ( -55.24728320129491266, 0.01453410071985307417, -0.0006547948648738343260 ) ) ;
#18995=ADVANCED_FACE ( 'NONE', ( #18871 ), #27433, .F. ) ;
#18996=CARTESIAN_POINT ( 'NONE',  ( -1.619063947482197729, -16.67502769180532596, 43.26576862488450104 ) ) ;
#18999=CARTESIAN_POINT ( 'NONE',  ( -23.79248802219730052, -13.25839849636379597, -30.42578156345381046 ) ) ;
#19001=CARTESIAN_POINT ( 'NONE',  ( -55.25297051322618813, 0.01019003092403517226, 0.01093108995494820879 ) ) ;
#19018=AXIS2_PLACEMENT_3D ( 'NONE', #2487, #4658, #13571 ) ;
#19022=ORIENTED_EDGE ( 'NONE', *, *, #1982, .T. ) ;
#19023=CARTESIAN_POINT ( 'NONE',  ( -1.619063947482201282, 16.67502769180561728, -43.26576862488438735 ) ) ;
#19028=ADVANCED_FACE ( 'NONE', ( #3753 ), #21558, .F. ) ;
#19030=ADVANCED_FACE ( 'NONE', ( #27644 ), #20795, .F. ) ;
#19038=CARTESIAN_POINT ( 'NONE',  ( -1.619063947482197729, 2.489035965910801895, 46.30105812165545842 ) ) ;
#19039=CARTESIAN_POINT ( 'NONE',  ( -22.23226125620944416, 24.24619897613477093, -20.31044300692182603 ) ) ;
#19051=ORIENTED_EDGE ( 'NONE', *, *, #16402, .F. ) ;
#19057=ORIENTED_EDGE ( 'NONE', *, *, #16906, .T. ) ;
#19058=ADVANCED_FACE ( 'NONE', ( #27798 ), #25621, .F. ) ;
#19061=ADVANCED_FACE ( 'NONE', ( #8927 ), #4985, .F. ) ;
#19071=CARTESIAN_POINT ( 'NONE',  ( -4.780792508754321268, -45.80716263181250980, -18.84172549606854119 ) ) ;
#19077=DIRECTION ( 'NONE',  ( 0.7563875759206388771, 0.3556158456312978888, 0.5490129373055215867 ) ) ;
#19079=VERTEX_POINT ( 'NONE', #13507 ) ;
#19080=CARTESIAN_POINT ( 'NONE',  ( -28.13707043255157103, -18.06394523322443035, 14.07296284901352479 ) ) ;
#19082=CARTESIAN_POINT ( 'NONE',  ( -28.41354790283022069, 22.41474081378008876, 5.969609727607788408 ) ) ;
#19086=EDGE_CURVE ( 'NONE', #7528, #7658, #18466, .T. ) ;
#19087=CARTESIAN_POINT ( 'NONE',  ( -1.044556982611274387, -37.98985389331830476, -25.56989963842190150 ) ) ;
#19090=EDGE_CURVE ( 'NONE', #7787, #15835, #6583, .T. ) ;
#19097=CARTESIAN_POINT ( 'NONE',  ( -1.155031165708891860, -44.25214473648919977, -12.20332162035446366 ) ) ;
#19102=ORIENTED_EDGE ( 'NONE', *, *, #20311, .T. ) ;
#19106=CARTESIAN_POINT ( 'NONE',  ( -20.20700224038492721, 24.51628800869048419, -16.58740185276719359 ) ) ;
#19107=ORIENTED_EDGE ( 'NONE', *, *, #26088, .F. ) ;
#19111=CARTESIAN_POINT ( 'NONE',  ( -21.81686047589428057, -26.62923599424948407, 27.83628745321478704 ) ) ;
#19131=EDGE_CURVE ( 'NONE', #654, #16962, #24426, .T. ) ;
#19137=CARTESIAN_POINT ( 'NONE',  ( -1.056502255334265339, -0.5104472526216820016, 45.80535052436398047 ) ) ;
#19146=CARTESIAN_POINT ( 'NONE',  ( -22.34422965417122953, 37.30738373203627845, 6.759368364653937533 ) ) ;
#19147=FACE_OUTER_BOUND ( 'NONE', #13102, .T. ) ;
#19155=CARTESIAN_POINT ( 'NONE',  ( -1.019300379054419725, 28.53917295602949977, 35.83762006677368106 ) ) ;
#19156=CARTESIAN_POINT ( 'NONE',  ( -1.058197053496162887, -25.48582931365496762, -38.06270006878843759 ) ) ;
#19168=CARTESIAN_POINT ( 'NONE',  ( -9.156249394959706578, 24.29252099376491358, -48.78605533024748553 ) ) ;
#19170=CARTESIAN_POINT ( 'NONE',  ( -21.81686047589429123, 26.62923599424970433, -27.83628745321458453 ) ) ;
#19174=CARTESIAN_POINT ( 'NONE',  ( -20.57838717382308147, 1.611677988432778319, 29.92853265176829325 ) ) ;
#19177=EDGE_CURVE ( 'NONE', #25165, #4432, #5200, .T. ) ;
#19179=CARTESIAN_POINT ( 'NONE',  ( -8.786685647604889127, 9.545808661480615243, -52.67761315067287597 ) ) ;
#19186=CARTESIAN_POINT ( 'NONE',  ( -6.574463467970654840, -25.96726214983158698, 44.27173031830760408 ) ) ;
#19188=ORIENTED_EDGE ( 'NONE', *, *, #3510, .F. ) ;
#19193=ORIENTED_EDGE ( 'NONE', *, *, #27460, .T. ) ;
#19198=DIRECTION ( 'NONE',  ( -0.7563875759206388771, -0.1685564395263341175, 0.6320336713238504656 ) ) ;
#19199=ADVANCED_FACE ( 'NONE', ( #14207 ), #5943, .F. ) ;
#19207=CARTESIAN_POINT ( 'NONE',  ( -5.986830583229317604, -43.56094206392958768, -26.01297580803309728 ) ) ;
#19210=CARTESIAN_POINT ( 'NONE',  ( -20.20700224038492721, -16.58740185276692358, 24.51628800869065827 ) ) ;
#19215=VERTEX_POINT ( 'NONE', #18108 ) ;
#19217=DIRECTION ( 'NONE',  ( 0.7637818620346800147, 0.6068965246771059752, 0.2198041754873819864 ) ) ;
#19223=B_SPLINE_CURVE_WITH_KNOTS ( 'NONE', 3,
 ( #22584, #11917, #15943, #22736, #14198, #20548, #13778, #5293, #22880, #9615, #3001, #20685, #7469 ),
 .UNSPECIFIED., .F., .F.,
 ( 4, 3, 3, 3, 4 ),
 ( 1.250926888277100303E-17, 0.0007657099931970619711, 0.001531419946797935418, 0.002296279302920161639, 0.003061450627205739884 ),
 .UNSPECIFIED. ) ;
#19227=CARTESIAN_POINT ( 'NONE',  ( -28.13707043255157103, 12.83104814250481596, 18.96624908365832596 ) ) ;
#19230=EDGE_CURVE ( 'NONE', #14713, #17827, #17866, .T. ) ;
#19234=CARTESIAN_POINT ( 'NONE',  ( -20.21097721712959583, 24.14932359587290023, -17.13687106192352161 ) ) ;
#19238=CARTESIAN_POINT ( 'NONE',  ( -28.41354790283022069, -22.41474081378005323, -5.969609727607934957 ) ) ;
#19239=CARTESIAN_POINT ( 'NONE',  ( -10.86508079875780730, -35.35100740321749413, 36.95527278096565027 ) ) ;
#19245=CARTESIAN_POINT ( 'NONE',  ( -23.79223135445720771, 22.01133905265687929, -24.83942264280410228 ) ) ;
#19247=( BOUNDED_SURFACE ( )  B_SPLINE_SURFACE ( 3, 1, ( 
 ( #24710, #6849 ),
 ( #351, #15903 ),
 ( #2507, #2358 ),
 ( #6998, #17895 ) ),
 .UNSPECIFIED., .F., .F., .F. ) 
 B_SPLINE_SURFACE_WITH_KNOTS ( ( 4, 4 ),
 ( 2, 2 ),
 ( 0.000000000000000000, 1.000000000000000000 ),
 ( 0.000000000000000000, 1.000000000000000000 ),
 .UNSPECIFIED. ) 
 GEOMETRIC_REPRESENTATION_ITEM ( )  RATIONAL_B_SPLINE_SURFACE ( (
 ( 1.000000000000000000, 1.000000000000000000),
 ( 0.9934239774497838349, 0.8357310067453913582),
 ( 0.9934239774497838349, 0.8357310067453913582),
 ( 1.000000000000000000, 1.000000000000000000) ) ) 
 REPRESENTATION_ITEM ( '' )  SURFACE ( )  );
#19248=CARTESIAN_POINT ( 'NONE',  ( -1.045287976400379737, -25.66401692420040703, -37.92705037016734337 ) ) ;
#19262=CARTESIAN_POINT ( 'NONE',  ( -28.13707043255157103, -6.342158660427161365, -22.00298671236737391 ) ) ;
#19266=CARTESIAN_POINT ( 'NONE',  ( -1.619063947482197729, -38.92136151114888776, 25.20140673341416360 ) ) ;
#19289=CARTESIAN_POINT ( 'NONE',  ( -55.24271866751342941, -0.001545935011626541761, -0.009369360294294543784 ) ) ;
#19291=CARTESIAN_POINT ( 'NONE',  ( -20.38016308990358638, -24.94368798801364662, -16.25718651464972098 ) ) ;
#19296=ORIENTED_EDGE ( 'NONE', *, *, #15477, .T. ) ;
#19298=ORIENTED_EDGE ( 'NONE', *, *, #23499, .T. ) ;
#19317=( BOUNDED_SURFACE ( )  B_SPLINE_SURFACE ( 3, 1, ( 
 ( #12362, #16543 ),
 ( #12093, #20714 ),
 ( #5460, #12231 ),
 ( #5616, #27333 ) ),
 .UNSPECIFIED., .F., .F., .F. ) 
 B_SPLINE_SURFACE_WITH_KNOTS ( ( 4, 4 ),
 ( 2, 2 ),
 ( 0.000000000000000000, 1.000000000000000000 ),
 ( 0.000000000000000000, 1.000000000000000000 ),
 .UNSPECIFIED. ) 
 GEOMETRIC_REPRESENTATION_ITEM ( )  RATIONAL_B_SPLINE_SURFACE ( (
 ( 1.000000000000000000, 1.000000000000000000),
 ( 0.9593753223639863714, 0.9995975284513187731),
 ( 0.9593753223639863714, 0.9995975284513187731),
 ( 1.000000000000000000, 1.000000000000000000) ) ) 
 REPRESENTATION_ITEM ( '' )  SURFACE ( )  );
#19320=VECTOR ( 'NONE', #25515, 1000.000000000000114 ) ;
#19333=VECTOR ( 'NONE', #25709, 999.9999999999998863 ) ;
#19336=CARTESIAN_POINT ( 'NONE',  ( -55.24300891470648622, -0.006048736206180239418, 0.007734635432132643158 ) ) ;
#19341=EDGE_LOOP ( 'NONE', ( #4896, #16318, #21377, #3458 ) ) ;
#19346=DIRECTION ( 'NONE',  ( -0.7637818620346800147, 0.6201872550346668733, 0.1788995134688804445 ) ) ;
#19351=LINE ( 'NONE', #4095, #22207 ) ;
#19358=CIRCLE ( 'NONE', #24912, 53.53553390275978785 ) ;
#19367=CARTESIAN_POINT ( 'NONE',  ( -1.050229599974486616, 13.90955673306187990, 43.63650726458048013 ) ) ;
#19383=CARTESIAN_POINT ( 'NONE',  ( -2.265401668238148591, 2.645701981445804929, -46.93990709177545995 ) ) ;
#19384=EDGE_CURVE ( 'NONE', #13723, #12509, #4469, .T. ) ;
#19385=CARTESIAN_POINT ( 'NONE',  ( -1.019300379054419725, -42.90269154183418010, 16.06793277092037187 ) ) ;
#19390=CARTESIAN_POINT ( 'NONE',  ( -20.47566262905010248, -1.586617686065349808, 29.82700878811085232 ) ) ;
#19399=CARTESIAN_POINT ( 'NONE',  ( -25.21435515916025594, 1.749597353048488237E-16, -4.373993382621220594E-17 ) ) ;
#19402=B_SPLINE_CURVE_WITH_KNOTS ( 'NONE', 3,
 ( #249, #25027, #2692, #3128 ),
 .UNSPECIFIED., .F., .F.,
 ( 4, 4 ),
 ( 1.847623020647441449E-16, 0.001982023823822945483 ),
 .UNSPECIFIED. ) ;
#19404=VECTOR ( 'NONE', #1114, 1000.000000000000114 ) ;
#19406=EDGE_CURVE ( 'NONE', #23707, #25959, #5501, .T. ) ;
#19425=CARTESIAN_POINT ( 'NONE',  ( -9.156249394959713683, 48.32878616081047340, 25.18996226954561735 ) ) ;
#19426=CARTESIAN_POINT ( 'NONE',  ( -1.049819825607587465, 26.50610175068268859, -37.34982882986852815 ) ) ;
#19427=ORIENTED_EDGE ( 'NONE', *, *, #26088, .T. ) ;
#19430=DIRECTION ( 'NONE',  ( 0.000000000000000000, 5.223019709707975211E-21, -1.000000000000000000 ) ) ;
#19432=AXIS2_PLACEMENT_3D ( 'NONE', #2189, #19757, #50 ) ;
#19435=CARTESIAN_POINT ( 'NONE',  ( -20.57838717382308147, 7.715628353034087894, 28.96176188950209962 ) ) ;
#19439=EDGE_LOOP ( 'NONE', ( #5739, #3466, #4945, #20529 ) ) ;
#19443=AXIS2_PLACEMENT_3D ( 'NONE', #14727, #24098, #26230 ) ;
#19448=CARTESIAN_POINT ( 'NONE',  ( -55.24198130335446422, 0.008310594958151115014, 0.004163123460805739397 ) ) ;
#19450=( BOUNDED_SURFACE ( )  B_SPLINE_SURFACE ( 3, 1, ( 
 ( #22220, #9263 ),
 ( #24538, #26811 ),
 ( #17598, #4801 ),
 ( #13565, #7120 ) ),
 .UNSPECIFIED., .F., .F., .F. ) 
 B_SPLINE_SURFACE_WITH_KNOTS ( ( 4, 4 ),
 ( 2, 2 ),
 ( 0.000000000000000000, 1.000000000000000000 ),
 ( 0.000000000000000000, 1.000000000000000000 ),
 .UNSPECIFIED. ) 
 GEOMETRIC_REPRESENTATION_ITEM ( )  RATIONAL_B_SPLINE_SURFACE ( (
 ( 1.000000000000000000, 1.000000000000000000),
 ( 0.9934239774497837239, 0.8357310067453919133),
 ( 0.9934239774497837239, 0.8357310067453919133),
 ( 1.000000000000000000, 1.000000000000000000) ) ) 
 REPRESENTATION_ITEM ( '' )  SURFACE ( )  );
#19452=ORIENTED_EDGE ( 'NONE', *, *, #6891, .T. ) ;
#19454=CARTESIAN_POINT ( 'NONE',  ( -1.031422197589716205, -12.69107518035533211, -44.01264471863842687 ) ) ;
#19477=VECTOR ( 'NONE', #17888, 1000.000000000000000 ) ;
#19478=CARTESIAN_POINT ( 'NONE',  ( -1.048172774974290622, 43.86067135048637766, 13.17853518375252442 ) ) ;
#19482=FACE_OUTER_BOUND ( 'NONE', #17516, .T. ) ;
#19483=CARTESIAN_POINT ( 'NONE',  ( -1.050229599974492833, 37.20249516760172526, -26.71319688967646755 ) ) ;
#19485=ORIENTED_EDGE ( 'NONE', *, *, #26191, .F. ) ;
#19491=CARTESIAN_POINT ( 'NONE',  ( -2.265401668238157473, 39.53028715828234851, -25.45016726748328040 ) ) ;
#19495=CARTESIAN_POINT ( 'NONE',  ( -8.786685647604890903, 25.35688121747502066, -47.14957014837363403 ) ) ;
#19501=( BOUNDED_SURFACE ( )  B_SPLINE_SURFACE ( 3, 1, ( 
 ( #26619, #155 ),
 ( #22175, #8796 ),
 ( #8650, #9220 ),
 ( #8946, #20147 ) ),
 .UNSPECIFIED., .F., .F., .F. ) 
 B_SPLINE_SURFACE_WITH_KNOTS ( ( 4, 4 ),
 ( 2, 2 ),
 ( 0.000000000000000000, 1.000000000000000000 ),
 ( 0.000000000000000000, 1.000000000000000000 ),
 .UNSPECIFIED. ) 
 GEOMETRIC_REPRESENTATION_ITEM ( )  RATIONAL_B_SPLINE_SURFACE ( (
 ( 1.000000000000000000, 1.000000000000000000),
 ( 0.7789835883360576307, 0.9689951854195403280),
 ( 0.7789835883360576307, 0.9689951854195403280),
 ( 1.000000000000000000, 1.000000000000000000) ) ) 
 REPRESENTATION_ITEM ( '' )  SURFACE ( )  );
#19502=CARTESIAN_POINT ( 'NONE',  ( -23.79223135445719350, -3.207301057648115350, 33.03345552685149755 ) ) ;
#19506=FACE_OUTER_BOUND ( 'NONE', #13948, .T. ) ;
#19509=CARTESIAN_POINT ( 'NONE',  ( -8.786685647604890903, -53.04920435127188938, -7.199674155858766689 ) ) ;
#19524=FACE_OUTER_BOUND ( 'NONE', #21846, .T. ) ;
#19527=ADVANCED_FACE ( 'NONE', ( #18939 ), #961, .F. ) ;
#19540=CARTESIAN_POINT ( 'NONE',  ( -4.473127245936431073, -12.17046501147550153, -47.80062405537796622 ) ) ;
#19541=CARTESIAN_POINT ( 'NONE',  ( -15.02187109954783750, -6.234056423739195552, 45.93032478317469725 ) ) ;
#19545=CARTESIAN_POINT ( 'NONE',  ( -1.539760825549691958, 35.94320866319490193, -29.16712717142773315 ) ) ;
#19547=CARTESIAN_POINT ( 'NONE',  ( -8.786685647604931759, 47.14957014837394667, 25.35688121747446999 ) ) ;
#19548=CARTESIAN_POINT ( 'NONE',  ( -1.045287976400351981, 36.12803364096590997, -28.14015102489844011 ) ) ;
#19553=CARTESIAN_POINT ( 'NONE',  ( -8.259864102781676820, 22.52209142945002895, 47.98931516265572128 ) ) ;
#19566=CARTESIAN_POINT ( 'NONE',  ( -5.986830583229484581, -11.27873876172107437, 49.46736940480268174 ) ) ;
#19567=DIRECTION ( 'NONE',  ( 0.000000000000000000, 5.223019709707975211E-21, -1.000000000000000000 ) ) ;
#19572=EDGE_CURVE ( 'NONE', #23418, #9221, #10449, .T. ) ;
#19577=ORIENTED_EDGE ( 'NONE', *, *, #21460, .F. ) ;
#19584=CARTESIAN_POINT ( 'NONE',  ( -10.86508079875781618, 35.35100740321776414, -36.95527278096538737 ) ) ;
#19586=EDGE_CURVE ( 'NONE', #12242, #5301, #1367, .T. ) ;
#19605=ORIENTED_EDGE ( 'NONE', *, *, #15192, .T. ) ;
#19610=CARTESIAN_POINT ( 'NONE',  ( -8.786685647604890903, -53.04920435127188938, -7.199674155858766689 ) ) ;
#19614=CARTESIAN_POINT ( 'NONE',  ( -12.94347594948484037, 48.30328466416762723, 6.555928820869474372 ) ) ;
#19620=ORIENTED_EDGE ( 'NONE', *, *, #15796, .T. ) ;
#19621=CARTESIAN_POINT ( 'NONE',  ( -1.056502255334264895, 36.75727364034733569, -27.33667001641181926 ) ) ;
#19635=ORIENTED_EDGE ( 'NONE', *, *, #25233, .T. ) ;
#19654=CARTESIAN_POINT ( 'NONE',  ( -1.048172774974295285, -26.08722459372758706, 37.64158596421241043 ) ) ;
#19658=CARTESIAN_POINT ( 'NONE',  ( -7.733045908741340568, 21.80378472388487054, -47.75066202881800592 ) ) ;
#19661=CARTESIAN_POINT ( 'NONE',  ( -1.045287976400365970, 15.59869763335068171, -43.05558670614252037 ) ) ;
#19662=CARTESIAN_POINT ( 'NONE',  ( -1.619063947482197729, 25.20140673341430571, 38.92136151114879539 ) ) ;
#19663=CARTESIAN_POINT ( 'NONE',  ( -8.786685647604885574, 6.096987947571466530E-17, -1.524246986892866633E-17 ) ) ;
#19664=CARTESIAN_POINT ( 'NONE',  ( -55.24300891470650754, 0.008142823778062566187, 0.005486913146700293786 ) ) ;
#19669=ORIENTED_EDGE ( 'NONE', *, *, #23124, .F. ) ;
#19675=DIRECTION ( 'NONE',  ( 1.000000000000000000, -6.938893903907226837E-18, 1.734723475976806709E-18 ) ) ;
#19685=AXIS2_PLACEMENT_3D ( 'NONE', #5266, #16642, #26986 ) ;
#19689=ORIENTED_EDGE ( 'NONE', *, *, #4641, .T. ) ;
#19695=CARTESIAN_POINT ( 'NONE',  ( -1.539763995773681282, 43.19716353142356269, 16.63252574782999460 ) ) ;
#19697=CARTESIAN_POINT ( 'NONE',  ( -1.050229599974477734, 27.12684363859256109, -36.90196321294305193 ) ) ;
#19698=ORIENTED_EDGE ( 'NONE', *, *, #25949, .F. ) ;
#19700=CARTESIAN_POINT ( 'NONE',  ( -7.078251931573400491, -50.86685171665403260, 11.16394717458729957 ) ) ;
#19711=EDGE_LOOP ( 'NONE', ( #12378, #20682, #19193, #12700 ) ) ;
#19713=CARTESIAN_POINT ( 'NONE',  ( -55.24198130335446422, -0.009170435128244796077, 0.001516807524704069481 ) ) ;
#19715=ADVANCED_FACE ( 'NONE', ( #22074 ), #2984, .F. ) ;
#19722=CARTESIAN_POINT ( 'NONE',  ( -20.47566262905010603, 10.72601569609896366, -27.87687924095551750 ) ) ;
#19749=CARTESIAN_POINT ( 'NONE',  ( -1.619063947482197729, 25.20140673341430571, 38.92136151114879539 ) ) ;
#19753=CARTESIAN_POINT ( 'NONE',  ( -1.048996300304507523, 36.59642367107745997, -27.53442103413706477 ) ) ;
#19755=VERTEX_POINT ( 'NONE', #26668 ) ;
#19757=DIRECTION ( 'NONE',  ( 1.000000000000000000, -6.938893903907226837E-18, 1.734723475976806709E-18 ) ) ;
#19767=CARTESIAN_POINT ( 'NONE',  ( -5.986830583229481029, 26.01297580803325360, -43.56094206392965873 ) ) ;
#19775=EDGE_CURVE ( 'NONE', #6247, #8074, #20625, .T. ) ;
#19780=VECTOR ( 'NONE', #6593, 1000.000000000000114 ) ;
#19781=DIRECTION ( 'NONE',  ( 0.000000000000000000, 5.223019709707975211E-21, -1.000000000000000000 ) ) ;
#19789=CARTESIAN_POINT ( 'NONE',  ( -1.259972190295296057, 45.95417440459617353, -2.243354636025928439 ) ) ;
#19793=CARTESIAN_POINT ( 'NONE',  ( -22.23226125620930205, 31.55376588768478285, -2.179935373562563061 ) ) ;
#19797=CARTESIAN_POINT ( 'NONE',  ( -1.323830074806763957, 12.01461446423264690, 44.47857376182257383 ) ) ;
#19799=AXIS2_PLACEMENT_3D ( 'NONE', #18314, #16023, #2343 ) ;
#19807=AXIS2_PLACEMENT_3D ( 'NONE', #4530, #17485, #24569 ) ;
#19815=LINE ( 'NONE', #6598, #23987 ) ;
#19816=ORIENTED_EDGE ( 'NONE', *, *, #12468, .F. ) ;
#19819=CARTESIAN_POINT ( 'NONE',  ( -1.619063947482201282, 35.99532424477380488, -29.22875152547769062 ) ) ;
#19820=VECTOR ( 'NONE', #27739, 1000.000000000000000 ) ;
#19825=AXIS2_PLACEMENT_3D ( 'NONE', #5986, #12582, #1363 ) ;
#19830=CARTESIAN_POINT ( 'NONE',  ( -1.619063947482197729, 16.67502769180622835, 43.26576862488415287 ) ) ;
#19833=ORIENTED_EDGE ( 'NONE', *, *, #12675, .T. ) ;
#19836=CARTESIAN_POINT ( 'NONE',  ( -1.046936909428679785, -43.14407378092982981, 15.35929614323710801 ) ) ;
#19838=CARTESIAN_POINT ( 'NONE',  ( -6.588769196390751759, -34.04709086065287238, 38.42957692275880532 ) ) ;
#19839=CARTESIAN_POINT ( 'NONE',  ( -21.81686047589429833, -37.90526371014251339, 6.867757412721077870 ) ) ;
#19845=CARTESIAN_POINT ( 'NONE',  ( -1.583189561560252701, -44.83405390829663872, 11.94859433442948493 ) ) ;
#19853=ORIENTED_EDGE ( 'NONE', *, *, #10957, .T. ) ;
#19856=EDGE_CURVE ( 'NONE', #21416, #20163, #27098, .T. ) ;
#19860=CARTESIAN_POINT ( 'NONE',  ( -55.24198130335446422, -0.009170435128244797812, -0.001516807524708348827 ) ) ;
#19868=VERTEX_POINT ( 'NONE', #20916 ) ;
#19871=CARTESIAN_POINT ( 'NONE',  ( -1.056502255334264895, -43.40574022158763512, 14.64009593116146846 ) ) ;
#19873=FACE_OUTER_BOUND ( 'NONE', #13279, .T. ) ;
#19876=CARTESIAN_POINT ( 'NONE',  ( -55.24728320129491266, -0.01362040845703352439, -0.005114031043468804730 ) ) ;
#19878=B_SPLINE_CURVE_WITH_KNOTS ( 'NONE', 3,
 ( #10669, #4036, #12671, #5933, #28208, #8509, #1730, #23647 ),
 .UNSPECIFIED., .F., .F.,
 ( 4, 2, 2, 4 ),
 ( 2.193594746808674791E-16, 0.002761568181852864200, 0.005523136363705508957, 0.01104627272741079240 ),
 .UNSPECIFIED. ) ;
#19890=ORIENTED_EDGE ( 'NONE', *, *, #3434, .T. ) ;
#19894=AXIS2_PLACEMENT_3D ( 'NONE', #6059, #5774, #14813 ) ;
#19900=CARTESIAN_POINT ( 'NONE',  ( -55.24390624410018802, -0.001451500391950358120, -0.01032895241567008057 ) ) ;
#19906=CARTESIAN_POINT ( 'NONE',  ( -1.048172774974299282, 36.44231470008717366, -27.73787987941021171 ) ) ;
#19907=CARTESIAN_POINT ( 'NONE',  ( -2.904412668506672457, -2.864640348250298008, 47.56768199507434502 ) ) ;
#19917=( BOUNDED_SURFACE ( )  B_SPLINE_SURFACE ( 3, 1, ( 
 ( #2473, #15560 ),
 ( #24372, #20033 ),
 ( #24528, #34 ),
 ( #22357, #15710 ) ),
 .UNSPECIFIED., .F., .F., .F. ) 
 B_SPLINE_SURFACE_WITH_KNOTS ( ( 4, 4 ),
 ( 2, 2 ),
 ( 0.000000000000000000, 1.000000000000000000 ),
 ( 0.000000000000000000, 1.000000000000000000 ),
 .UNSPECIFIED. ) 
 GEOMETRIC_REPRESENTATION_ITEM ( )  RATIONAL_B_SPLINE_SURFACE ( (
 ( 1.000000000000000000, 1.000000000000000000),
 ( 0.9934239774497837239, 0.8357310067453919133),
 ( 0.9934239774497837239, 0.8357310067453919133),
 ( 1.000000000000000000, 1.000000000000000000) ) ) 
 REPRESENTATION_ITEM ( '' )  SURFACE ( )  );
#19919=CARTESIAN_POINT ( 'NONE',  ( -1.031422197589711987, -15.60268798220668707, -43.06660437151302290 ) ) ;
#19927=B_SPLINE_CURVE_WITH_KNOTS ( 'NONE', 3,
 ( #14523, #16843, #11803, #18848, #14222, #3026, #20994, #27777, #23046, #14380, #11942, #10081, #9942 ),
 .UNSPECIFIED., .F., .F.,
 ( 4, 3, 3, 3, 4 ),
 ( 1.105886215935214523E-17, 0.0007657099931970556828, 0.001531419946797917854, 0.002296279302920152532, 0.003061450627205755497 ),
 .UNSPECIFIED. ) ;
#19934=ORIENTED_EDGE ( 'NONE', *, *, #12738, .F. ) ;
#19936=CARTESIAN_POINT ( 'NONE',  ( -1.050231094221204087, -14.39477892760331024, -43.47885872350351377 ) ) ;
#19947=ORIENTED_EDGE ( 'NONE', *, *, #4637, .F. ) ;
#19949=EDGE_CURVE ( 'NONE', #7747, #5592, #14755, .T. ) ;
#19950=DIRECTION ( 'NONE',  ( 0.7563875759206388771, 0.5078650950445714463, 0.4122509917856694850 ) ) ;
#19956=CARTESIAN_POINT ( 'NONE',  ( -1.019300379054419725, -45.76814864815089123, 2.023851374323154761 ) ) ;
#19964=DIRECTION ( 'NONE',  ( -0.7637818620346800147, -0.1788995134688828315, 0.6201872550346662072 ) ) ;
#19967=CARTESIAN_POINT ( 'NONE',  ( -1.464342487929859660, -46.14921266389556820, 2.431462367721817230 ) ) ;
#19974=DIRECTION ( 'NONE',  ( 1.000000000000000000, -6.938893903907226837E-18, 1.734723475976806709E-18 ) ) ;
#19979=CARTESIAN_POINT ( 'NONE',  ( -1.049817751779885233, -26.50542916749595435, -37.35030165458165641 ) ) ;
#19986=ORIENTED_EDGE ( 'NONE', *, *, #4532, .T. ) ;
#19988=CARTESIAN_POINT ( 'NONE',  ( -55.25297051322618813, -0.006313402748431807057, -0.01354497706059512932 ) ) ;
#19991=EDGE_CURVE ( 'NONE', #22163, #14951, #9571, .T. ) ;
#19993=CARTESIAN_POINT ( 'NONE',  ( -1.045287976400365970, -43.05558670614224326, 15.59869763335140469 ) ) ;
#19994=ORIENTED_EDGE ( 'NONE', *, *, #31, .T. ) ;
#19995=CARTESIAN_POINT ( 'NONE',  ( -20.20612092514785019, 29.57813644637190365, -1.137292630518160097 ) ) ;
#19998=ORIENTED_EDGE ( 'NONE', *, *, #23883, .T. ) ;
#20004=CARTESIAN_POINT ( 'NONE',  ( -55.24271866751342941, 0.009388511352198142604, 0.001425019990782173561 ) ) ;
#20007=CARTESIAN_POINT ( 'NONE',  ( -8.786685647604890903, 38.68584556812300690, -37.00619870957947910 ) ) ;
#20008=ORIENTED_EDGE ( 'NONE', *, *, #8140, .T. ) ;
#20013=CARTESIAN_POINT ( 'NONE',  ( -1.619063947482197729, 46.30105812165548684, 2.489035965910320503 ) ) ;
#20014=FACE_OUTER_BOUND ( 'NONE', #15243, .T. ) ;
#20033=CARTESIAN_POINT ( 'NONE',  ( -1.239374126674604337, -44.48112152129338170, 11.92219841463876229 ) ) ;
#20036=CARTESIAN_POINT ( 'NONE',  ( -1.049817751779883457, 43.39729912094399822, 14.63752841325003295 ) ) ;
#20037=ADVANCED_FACE ( 'NONE', ( #17110 ), #3911, .F. ) ;
#20044=DIRECTION ( 'NONE',  ( 0.000000000000000000, 5.223019709707975211E-21, -1.000000000000000000 ) ) ;
#20055=DIRECTION ( 'NONE',  ( 1.000000000000000000, -6.938893903907226837E-18, 1.734723475976806709E-18 ) ) ;
#20057=ORIENTED_EDGE ( 'NONE', *, *, #28266, .F. ) ;
#20068=EDGE_CURVE ( 'NONE', #25305, #211, #22166, .T. ) ;
#20076=CARTESIAN_POINT ( 'NONE',  ( -1.045287976400365970, 44.00138577190666922, 12.68782741917247670 ) ) ;
#20080=CARTESIAN_POINT ( 'NONE',  ( -23.79248802219723302, 33.03370827286732947, -3.207402715357277057 ) ) ;
#20089=CARTESIAN_POINT ( 'NONE',  ( -8.786685647604706162, -38.68584556812290032, 37.00619870957955015 ) ) ;
#20091=CARTESIAN_POINT ( 'NONE',  ( -1.113427685307003534, -35.91272432484637278, 28.52429901637207266 ) ) ;
#20096=CARTESIAN_POINT ( 'NONE',  ( -24.53237795827027767, -29.54731592868574808, -16.68575684089485023 ) ) ;
#20113=ORIENTED_EDGE ( 'NONE', *, *, #2945, .T. ) ;
#20117=CARTESIAN_POINT ( 'NONE',  ( -20.20700224038492010, -10.08426345511570332, 27.82980252387829623 ) ) ;
#20136=ORIENTED_EDGE ( 'NONE', *, *, #25823, .F. ) ;
#20139=DIRECTION ( 'NONE',  ( -1.000000000000000000, 6.938893903907226837E-18, -1.734723475976806709E-18 ) ) ;
#20147=CARTESIAN_POINT ( 'NONE',  ( -9.156249394959713683, 38.89149400288408032, -38.17928057392006025 ) ) ;
#20149=CARTESIAN_POINT ( 'NONE',  ( -25.21435515916025594, 34.29329011225976132, 4.655591116594488099 ) ) ;
#20154=CARTESIAN_POINT ( 'NONE',  ( -28.13707043255157103, 7.802116958609309094, 21.52861750560930432 ) ) ;
#20156=CARTESIAN_POINT ( 'NONE',  ( -9.156249394959713683, 8.027840202794694235, 53.90509764945120708 ) ) ;
#20160=CARTESIAN_POINT ( 'NONE',  ( -12.82751273423880356, -6.573887447703164355, -48.43568301531138331 ) ) ;
#20163=VERTEX_POINT ( 'NONE', #8484 ) ;
#20174=EDGE_CURVE ( 'NONE', #24273, #16312, #26288, .T. ) ;
#20185=ORIENTED_EDGE ( 'NONE', *, *, #18654, .F. ) ;
#20191=ORIENTED_EDGE ( 'NONE', *, *, #2155, .T. ) ;
#20194=CARTESIAN_POINT ( 'NONE',  ( -8.786685647604885574, 6.096987947571466530E-17, -1.524246986892866633E-17 ) ) ;
#20200=CARTESIAN_POINT ( 'NONE',  ( -25.21435515916043713, -34.05351380035337883, -6.169479169075319014 ) ) ;
#20203=VERTEX_POINT ( 'NONE', #3096 ) ;
#20213=CARTESIAN_POINT ( 'NONE',  ( -1.048172774974291066, 1.020161070261757841, 45.78636862970791555 ) ) ;
#20216=CARTESIAN_POINT ( 'NONE',  ( -20.21097721712959228, -29.61001327235739566, -0.3305963429841727863 ) ) ;
#20220=CARTESIAN_POINT ( 'NONE',  ( -24.53239521893648245, -33.25736993155760501, 6.738460611583118265 ) ) ;
#20228=EDGE_CURVE ( 'NONE', #28300, #22454, #24024, .T. ) ;
#20231=B_SPLINE_CURVE_WITH_KNOTS ( 'NONE', 3,
 ( #8762, #26178, #6756, #8916, #13080, #2261 ),
 .UNSPECIFIED., .F., .F.,
 ( 4, 2, 4 ),
 ( 8.673617379884034509E-19, 0.0004335184443140208837, 0.0008670368886280409000 ),
 .UNSPECIFIED. ) ;
#20240=CARTESIAN_POINT ( 'NONE',  ( -21.41427618760457818, -19.54551635498111395, 23.81423075802604217 ) ) ;
#20247=ADVANCED_FACE ( 'NONE', ( #22979 ), #14581, .F. ) ;
#20256=CARTESIAN_POINT ( 'NONE',  ( -4.473127245936431073, -41.70021447285034810, 26.34600523034583119 ) ) ;
#20259=DIRECTION ( 'NONE',  ( 5.541455922705463698E-20, -5.223019709708320524E-21, 1.000000000000000000 ) ) ;
#20261=CARTESIAN_POINT ( 'NONE',  ( -23.77929240705206126, 25.06639637888459404, 26.20227034809527211 ) ) ;
#20264=CARTESIAN_POINT ( 'NONE',  ( -1.619063947482201282, -16.67502769180592992, -43.26576862488428077 ) ) ;
#20265=AXIS2_PLACEMENT_3D ( 'NONE', #27146, #20391, #4855 ) ;
#20279=B_SPLINE_CURVE_WITH_KNOTS ( 'NONE', 3,
 ( #8255, #7842, #10420, #19186, #6107, #14862, #16603, #23244 ),
 .UNSPECIFIED., .F., .F.,
 ( 4, 2, 2, 4 ),
 ( 0.000000000000000000, 0.002761524886576655416, 0.005523049773153310832, 0.01104609954630660432 ),
 .UNSPECIFIED. ) ;
#20290=ORIENTED_EDGE ( 'NONE', *, *, #20068, .T. ) ;
#20298=CARTESIAN_POINT ( 'NONE',  ( -18.41936578851709072, 38.22933728004715448, 18.42310649277586876 ) ) ;
#20299=DIRECTION ( 'NONE',  ( -0.7637818620346800147, -0.2198041754873968356, -0.6068965246771005351 ) ) ;
#20301=CARTESIAN_POINT ( 'NONE',  ( -1.323830074806768176, 44.47857376182273015, -12.01461446423216906 ) ) ;
#20302=FACE_OUTER_BOUND ( 'NONE', #25116, .T. ) ;
#20311=EDGE_CURVE ( 'NONE', #1484, #25606, #3059, .T. ) ;
#20313=ORIENTED_EDGE ( 'NONE', *, *, #4002, .F. ) ;
#20316=CARTESIAN_POINT ( 'NONE',  ( -55.24271866751342941, -0.006757859501005985571, -0.006671293903669251422 ) ) ;
#20319=CARTESIAN_POINT ( 'NONE',  ( -55.24271866751342941, 0.006671293903668402275, 0.006757859501010043089 ) ) ;
#20320=CARTESIAN_POINT ( 'NONE',  ( -1.239374126674604337, 45.98822239537608425, -2.406737988131283146 ) ) ;
#20325=CARTESIAN_POINT ( 'NONE',  ( -1.155001620486246550, -16.13799328198394178, 42.97366440495927975 ) ) ;
#20337=CARTESIAN_POINT ( 'NONE',  ( -55.24198130335446422, -0.001516807524707838167, 0.009170435128245089246 ) ) ;
#20340=CARTESIAN_POINT ( 'NONE',  ( -2.904412668506660911, -11.97478724945543860, -46.12477647685269488 ) ) ;
#20341=ORIENTED_EDGE ( 'NONE', *, *, #24795, .F. ) ;
#20346=B_SPLINE_CURVE_WITH_KNOTS ( 'NONE', 3,
 ( #28183, #26172, #17111, #4428, #117, #15494, #14946 ),
 .UNSPECIFIED., .F., .F.,
 ( 4, 3, 4 ),
 ( 0.000000000000000000, 0.006568092053401789268, 0.02506242213020845946 ),
 .UNSPECIFIED. ) ;
#20350=CARTESIAN_POINT ( 'NONE',  ( -23.79223135445719350, -30.42557260166821109, -13.25822371132282917 ) ) ;
#20353=CARTESIAN_POINT ( 'NONE',  ( -8.786685647604890903, -52.67761315067293282, -9.545808661480407409 ) ) ;
#20356=VERTEX_POINT ( 'NONE', #27841 ) ;
#20365=AXIS2_PLACEMENT_3D ( 'NONE', #22106, #6328, #17311 ) ;
#20369=CARTESIAN_POINT ( 'NONE',  ( -20.57838717382308147, 10.78122205917000365, -27.96569011373090063 ) ) ;
#20372=EDGE_CURVE ( 'NONE', #11759, #8126, #13727, .T. ) ;
#20385=CARTESIAN_POINT ( 'NONE',  ( -23.79223135445721837, -33.03345552685147624, -3.207301057648224596 ) ) ;
#20388=ORIENTED_EDGE ( 'NONE', *, *, #9342, .T. ) ;
#20391=DIRECTION ( 'NONE',  ( 1.000000000000000000, -6.938893903907226837E-18, 1.734723475976806709E-18 ) ) ;
#20393=CARTESIAN_POINT ( 'NONE',  ( -1.031422197589711987, -25.67058493451414591, 37.93675465142499803 ) ) ;
#20395=ORIENTED_EDGE ( 'NONE', *, *, #17438, .F. ) ;
#20398=CIRCLE ( 'NONE', #3402, 12.50000000000000000 ) ;
#20402=ORIENTED_EDGE ( 'NONE', *, *, #6154, .F. ) ;
#20407=CARTESIAN_POINT ( 'NONE',  ( -20.20612091757422135, -10.22177757278296184, 27.77903622052264865 ) ) ;
#20409=CARTESIAN_POINT ( 'NONE',  ( -1.031422197589716205, 36.13727897780168519, 28.14735071801704436 ) ) ;
#20410=EDGE_CURVE ( 'NONE', #8158, #22719, #9608, .T. ) ;
#20411=CARTESIAN_POINT ( 'NONE',  ( -6.574463467970541153, -38.37705091668347279, 34.08059230520071026 ) ) ;
#20413=CARTESIAN_POINT ( 'NONE',  ( -4.780792508754326597, -48.13366140756551914, 11.68149851467511446 ) ) ;
#20417=CARTESIAN_POINT ( 'NONE',  ( -28.41354790283022069, -8.345538364877233661, -21.64275480268745255 ) ) ;
#20435=LINE ( 'NONE', #16110, #10301 ) ;
#20440=DIRECTION ( 'NONE',  ( 0.7637818620346801257, 0.6201872550346656521, -0.1788995134688848854 ) ) ;
#20445=CARTESIAN_POINT ( 'NONE',  ( -23.79248802219722236, 32.40806545715341258, 7.157555990716568672 ) ) ;
#20449=ORIENTED_EDGE ( 'NONE', *, *, #25638, .T. ) ;
#20450=CARTESIAN_POINT ( 'NONE',  ( -1.045287976400379737, 44.00138577190644185, -12.68782741917337198 ) ) ;
#20459=EDGE_LOOP ( 'NONE', ( #27963, #17083, #27420, #11903 ) ) ;
#20462=CARTESIAN_POINT ( 'NONE',  ( -25.21435515916025594, 1.749597353048488237E-16, -4.373993382621220594E-17 ) ) ;
#20478=CARTESIAN_POINT ( 'NONE',  ( -10.86508079875779842, 36.95527278096579948, 35.35100740321738044 ) ) ;
#20497=FACE_OUTER_BOUND ( 'NONE', #115, .T. ) ;
#20498=CARTESIAN_POINT ( 'NONE',  ( -8.786685647604898008, 48.22796981442765940, -23.24040270374399952 ) ) ;
#20507=CARTESIAN_POINT ( 'NONE',  ( -1.048996300304498419, 0.7649764263858191971, 45.79145529752468491 ) ) ;
#20508=ORIENTED_EDGE ( 'NONE', *, *, #3454, .T. ) ;
#20525=B_SPLINE_CURVE_WITH_KNOTS ( 'NONE', 3,
 ( #16380, #838, #2860, #11638, #20413, #9622, #696, #16091 ),
 .UNSPECIFIED., .F., .F.,
 ( 4, 2, 2, 4 ),
 ( 2.225109362706117716E-16, 0.002761568181852862899, 0.005523136363705503753, 0.01104627272741078893 ),
 .UNSPECIFIED. ) ;
#20527=ORIENTED_EDGE ( 'NONE', *, *, #8118, .T. ) ;
#20529=ORIENTED_EDGE ( 'NONE', *, *, #13341, .F. ) ;
#20531=ORIENTED_EDGE ( 'NONE', *, *, #681, .T. ) ;
#20538=CARTESIAN_POINT ( 'NONE',  ( -19.53423201713129842, 1.355459634611817431E-16, -3.388649086529543578E-17 ) ) ;
#20548=CARTESIAN_POINT ( 'NONE',  ( -1.050231094221214079, 37.20185272688497236, 26.71409683968576942 ) ) ;
#20552=B_SPLINE_CURVE_WITH_KNOTS ( 'NONE', 3,
 ( #10480, #12757, #1680, #17084, #8185, #27888, #10614 ),
 .UNSPECIFIED., .F., .F.,
 ( 4, 3, 4 ),
 ( 0.000000000000000000, 0.006568092053401776258, 0.02506242213020846987 ),
 .UNSPECIFIED. ) ;
#20554=FACE_OUTER_BOUND ( 'NONE', #25573, .T. ) ;
#20564=VERTEX_POINT ( 'NONE', #23088 ) ;
#20574=CARTESIAN_POINT ( 'NONE',  ( -1.048994561756802169, 45.79144455904140898, 0.7655149579825029083 ) ) ;
#20578=CARTESIAN_POINT ( 'NONE',  ( -4.162674018437153123, 47.46216648493558665, -11.82104147411576989 ) ) ;
#20579=VERTEX_POINT ( 'NONE', #12136 ) ;
#20604=FACE_OUTER_BOUND ( 'NONE', #291, .T. ) ;
#20605=ADVANCED_FACE ( 'NONE', ( #18745 ), #1477, .T. ) ;
#20610=CARTESIAN_POINT ( 'NONE',  ( -21.81686047589431965, 5.181745222995449929, -38.17230180719251820 ) ) ;
#20611=CARTESIAN_POINT ( 'NONE',  ( -1.463510566862834761, -16.57250862017389892, 43.13857742234520032 ) ) ;
#20616=CARTESIAN_POINT ( 'NONE',  ( -20.21097721712959228, -28.26295595852180043, 8.835581498567762537 ) ) ;
#20625=LINE ( 'NONE', #6983, #13413 ) ;
#20640=CARTESIAN_POINT ( 'NONE',  ( -5.986830583229461489, 46.64941882410799678, -19.95149887249867859 ) ) ;
#20642=DIRECTION ( 'NONE',  ( 0.000000000000000000, 5.223019709708233256E-21, -1.000000000000000000 ) ) ;
#20647=CARTESIAN_POINT ( 'NONE',  ( -8.786685647604890903, -25.35688121747466184, 47.14957014837381166 ) ) ;
#20650=CARTESIAN_POINT ( 'NONE',  ( -18.41936578851711204, -7.566034416291083531, -41.75701384111729197 ) ) ;
#20655=CARTESIAN_POINT ( 'NONE',  ( -1.239374126674604337, 2.406737988131765871, 45.98822239537605583 ) ) ;
#20656=CARTESIAN_POINT ( 'NONE',  ( -1.619063947482197729, -38.92136151114888776, 25.20140673341416360 ) ) ;
#20666=CARTESIAN_POINT ( 'NONE',  ( -1.031422197589711987, 36.13727897780127307, -28.14735071801756661 ) ) ;
#20672=SHAPE_REPRESENTATION_RELATIONSHIP ( 'NONE' , 'NONE' ,  #747, #24076 ) ;
#20678=CARTESIAN_POINT ( 'NONE',  ( -9.156249394959706578, 53.74753343182702991, -9.022661520477960551 ) ) ;
#20681=CARTESIAN_POINT ( 'NONE',  ( -20.38016308990358638, 23.16952666206584155, -18.69911008768343663 ) ) ;
#20682=ORIENTED_EDGE ( 'NONE', *, *, #26121, .F. ) ;
#20683=EDGE_LOOP ( 'NONE', ( #17172, #6668, #22608, #4633 ) ) ;
#20685=CARTESIAN_POINT ( 'NONE',  ( -1.046935749539997129, 36.28605774377803073, 27.93995161054655085 ) ) ;
#20689=CARTESIAN_POINT ( 'NONE',  ( -8.786685647604890903, -48.22796981442753150, 23.24040270374441874 ) ) ;
#20690=CARTESIAN_POINT ( 'NONE',  ( -12.82751273423876270, 48.43568301531151121, -6.573887447703007147 ) ) ;
#20693=VERTEX_POINT ( 'NONE', #17153 ) ;
#20695=CARTESIAN_POINT ( 'NONE',  ( -55.24390624410018802, 0.001451500391951047672, 0.01032895241566990016 ) ) ;
#20703=ORIENTED_EDGE ( 'NONE', *, *, #18040, .T. ) ;
#20706=CARTESIAN_POINT ( 'NONE',  ( -15.02187109954784106, 45.60876405941888123, -8.264310930412539946 ) ) ;
#20712=ORIENTED_EDGE ( 'NONE', *, *, #9342, .F. ) ;
#20714=CARTESIAN_POINT ( 'NONE',  ( -1.056502255334265339, 27.33667001641170557, -36.75727364034741385 ) ) ;
#20716=CARTESIAN_POINT ( 'NONE',  ( -20.57838717382308147, -28.96176188950224528, -7.715628353033566533 ) ) ;
#20733=CARTESIAN_POINT ( 'NONE',  ( -20.20700224038492721, -23.35150625415645820, 18.19058640100249491 ) ) ;
#20734=ORIENTED_EDGE ( 'NONE', *, *, #8339, .T. ) ;
#20737=LINE ( 'NONE', #1173, #19320 ) ;
#20740=CARTESIAN_POINT ( 'NONE',  ( -1.464342487929850778, 38.76467504336618219, 25.15873223207648834 ) ) ;
#20742=ORIENTED_EDGE ( 'NONE', *, *, #18604, .F. ) ;
#20748=VECTOR ( 'NONE', #27716, 999.9999999999998863 ) ;
#20750=CARTESIAN_POINT ( 'NONE',  ( -1.056502255334264895, -43.72121397317232550, -13.66916755949833373 ) ) ;
#20764=CARTESIAN_POINT ( 'NONE',  ( -28.41354790283022069, 18.00456980371900784, -14.62505768302807319 ) ) ;
#20779=CIRCLE ( 'NONE', #24478, 53.53553390275978785 ) ;
#20782=AXIS2_PLACEMENT_3D ( 'NONE', #8908, #12926, #11198 ) ;
#20783=FACE_OUTER_BOUND ( 'NONE', #17115, .T. ) ;
#20787=CARTESIAN_POINT ( 'NONE',  ( -55.24198130335446422, -0.006617369590168513567, -0.006527480770976002225 ) ) ;
#20792=CARTESIAN_POINT ( 'NONE',  ( -20.20700224038492365, 10.08426345511628597, 27.82980252387807951 ) ) ;
#20795=( BOUNDED_SURFACE ( )  B_SPLINE_SURFACE ( 3, 1, ( 
 ( #19289, #6073 ),
 ( #12665, #12800 ),
 ( #28063, #1860 ),
 ( #25649, #12523 ) ),
 .UNSPECIFIED., .F., .F., .F. ) 
 B_SPLINE_SURFACE_WITH_KNOTS ( ( 4, 4 ),
 ( 2, 2 ),
 ( 0.000000000000000000, 1.000000000000000000 ),
 ( 0.000000000000000000, 1.000000000000000000 ),
 .UNSPECIFIED. ) 
 GEOMETRIC_REPRESENTATION_ITEM ( )  RATIONAL_B_SPLINE_SURFACE ( (
 ( 1.000000000000000000, 1.000000000000000000),
 ( 0.9593753223639863714, 0.9995975284513187731),
 ( 0.9593753223639863714, 0.9995975284513187731),
 ( 1.000000000000000000, 1.000000000000000000) ) ) 
 REPRESENTATION_ITEM ( '' )  SURFACE ( )  );
#20801=FACE_OUTER_BOUND ( 'NONE', #13360, .T. ) ;
#20821=CARTESIAN_POINT ( 'NONE',  ( -28.13707043255157103, 7.802116958609002673, -21.52861750560941800 ) ) ;
#20822=VERTEX_POINT ( 'NONE', #13532 ) ;
#20827=EDGE_CURVE ( 'NONE', #7710, #16962, #12044, .T. ) ;
#20831=ORIENTED_EDGE ( 'NONE', *, *, #11896, .T. ) ;
#20836=ORIENTED_EDGE ( 'NONE', *, *, #23105, .F. ) ;
#20849=CARTESIAN_POINT ( 'NONE',  ( -23.77929240705206482, -31.93650644494352875, -17.17389748746951739 ) ) ;
#20850=ADVANCED_FACE ( 'NONE', ( #24074 ), #9225, .F. ) ;
#20856=CARTESIAN_POINT ( 'NONE',  ( -24.53237795827033807, 22.94498492516385468, 24.99972053297880947 ) ) ;
#20859=ORIENTED_EDGE ( 'NONE', *, *, #19406, .F. ) ;
#20870=ORIENTED_EDGE ( 'NONE', *, *, #25538, .T. ) ;
#20889=CARTESIAN_POINT ( 'NONE',  ( -20.57838717382308147, -16.28767523336139078, -25.16001208503099917 ) ) ;
#20890=ORIENTED_EDGE ( 'NONE', *, *, #21155, .T. ) ;
#20894=VERTEX_POINT ( 'NONE', #27196 ) ;
#20905=EDGE_CURVE ( 'NONE', #28211, #744, #14033, .T. ) ;
#20906=CARTESIAN_POINT ( 'NONE',  ( -20.20700224038492721, -10.08426345511609235, -27.82980252387815767 ) ) ;
#20915=ORIENTED_EDGE ( 'NONE', *, *, #3967, .F. ) ;
#20916=CARTESIAN_POINT ( 'NONE',  ( -20.57838717382308147, -23.26537097894118133, -18.89542499756491978 ) ) ;
#20918=DIRECTION ( 'NONE',  ( 1.000000000000000000, -6.938893903907226837E-18, 1.734723475976806709E-18 ) ) ;
#20924=CARTESIAN_POINT ( 'NONE',  ( -25.21435515916025594, 1.749597353048488237E-16, -4.373993382621220594E-17 ) ) ;
#20925=ADVANCED_FACE ( 'NONE', ( #2892 ), #2806, .F. ) ;
#20938=CARTESIAN_POINT ( 'NONE',  ( -20.20700224038492721, -23.35150625415645820, 18.19058640100249491 ) ) ;
#20941=CARTESIAN_POINT ( 'NONE',  ( -20.57838717382308147, 23.26537097894132344, 18.89542499756474569 ) ) ;
#20942=VERTEX_POINT ( 'NONE', #15978 ) ;
#20947=DIRECTION ( 'NONE',  ( 1.000000000000000000, -6.938893903907226837E-18, 1.734723475976806709E-18 ) ) ;
#20948=ORIENTED_EDGE ( 'NONE', *, *, #1883, .F. ) ;
#20953=EDGE_CURVE ( 'NONE', #7229, #6633, #23709, .T. ) ;
#20956=CARTESIAN_POINT ( 'NONE',  ( -20.90916690077964191, 34.84883504600978910, 18.74041620980130674 ) ) ;
#20958=LINE ( 'NONE', #5423, #5100 ) ;
#20960=LINE ( 'NONE', #21100, #19820 ) ;
#20961=VERTEX_POINT ( 'NONE', #14818 ) ;
#20965=CARTESIAN_POINT ( 'NONE',  ( -8.786685647604890903, -37.00619870957905277, 38.68584556812340480 ) ) ;
#20968=VERTEX_POINT ( 'NONE', #10654 ) ;
#20975=EDGE_LOOP ( 'NONE', ( #1202, #14005, #24254, #15863 ) ) ;
#20977=CARTESIAN_POINT ( 'NONE',  ( -16.86833981943428640, -38.94907963570735632, -20.94590537750593739 ) ) ;
#20978=ORIENTED_EDGE ( 'NONE', *, *, #18452, .T. ) ;
#20979=CARTESIAN_POINT ( 'NONE',  ( -20.57838717382308147, -29.92853265176832878, -1.611677988432255848 ) ) ;
#20980=CARTESIAN_POINT ( 'NONE',  ( -20.20612092514784663, 1.137292630518469849, 29.57813644637188233 ) ) ;
#20981=CARTESIAN_POINT ( 'NONE',  ( -1.619063947482197729, 44.80407745103800465, 11.94059994246113021 ) ) ;
#20985=ORIENTED_EDGE ( 'NONE', *, *, #12607, .F. ) ;
#20994=CARTESIAN_POINT ( 'NONE',  ( -1.050230346682665239, -45.79907861045645490, -0.0006945978174090946524 ) ) ;
#20999=CARTESIAN_POINT ( 'NONE',  ( -21.41430102051751660, -11.22990201072297012, -28.68859753627389253 ) ) ;
#21010=CARTESIAN_POINT ( 'NONE',  ( 14.74894986621300319, -1.023413983156987147E-16, 2.558534957892467869E-17 ) ) ;
#21021=B_SPLINE_CURVE_WITH_KNOTS ( 'NONE', 3,
 ( #26650, #6964, #5502, #5065, #27376, #22657 ),
 .UNSPECIFIED., .F., .F.,
 ( 4, 2, 4 ),
 ( 4.982613841084487634E-18, 0.0004335151646191490811, 0.0008670303292382946928 ),
 .UNSPECIFIED. ) ;
#21024=CARTESIAN_POINT ( 'NONE',  ( -55.25297051322618813, 0.01354497706059944184, 0.006313402748433108967 ) ) ;
#21025=CARTESIAN_POINT ( 'NONE',  ( -1.323439229708138987, -28.92147054731866263, -35.86372896917463038 ) ) ;
#21028=VERTEX_POINT ( 'NONE', #9128 ) ;
#21030=ADVANCED_FACE ( 'NONE', ( #13432 ), #16779, .F. ) ;
#21039=CARTESIAN_POINT ( 'NONE',  ( -20.37983603106074781, 24.94323704205437409, -16.25728007463414571 ) ) ;
#21044=CARTESIAN_POINT ( 'NONE',  ( -1.031422197589716205, -45.78027046666446154, -1.530725436377304183 ) ) ;
#21045=CARTESIAN_POINT ( 'NONE',  ( -20.20700224038492721, 29.58392382092673500, 0.9908225410479544193 ) ) ;
#21049=ORIENTED_EDGE ( 'NONE', *, *, #19131, .T. ) ;
#21050=CARTESIAN_POINT ( 'NONE',  ( -1.048994561756795729, 43.78680886990941445, -13.42228657661138058 ) ) ;
#21051=CARTESIAN_POINT ( 'NONE',  ( -25.21435515916043357, 6.169479169075458458, -34.05351380035335751 ) ) ;
#21067=EDGE_CURVE ( 'NONE', #9221, #25218, #2290, .T. ) ;
#21075=B_SPLINE_CURVE_WITH_KNOTS ( 'NONE', 3,
 ( #20792, #1082, #25419, #9871, #3382, #10016 ),
 .UNSPECIFIED., .F., .F.,
 ( 4, 2, 4 ),
 ( 0.000000000000000000, 0.0004335184443140258710, 0.0008670368886280517421 ),
 .UNSPECIFIED. ) ;
#21077=LINE ( 'NONE', #27983, #22612 ) ;
#21078=CARTESIAN_POINT ( 'NONE',  ( -55.24728320129491266, 0.009072670231978626973, -0.01137345571547102377 ) ) ;
#21081=DIRECTION ( 'NONE',  ( -0.7637818620346800147, -0.6068965246771030886, 0.2198041754873903408 ) ) ;
#21082=FACE_OUTER_BOUND ( 'NONE', #9344, .T. ) ;
#21100=CARTESIAN_POINT ( 'NONE',  ( -28.13707043255157103, 0.7675454997510209321, 22.88591869784690047 ) ) ;
#21106=VERTEX_POINT ( 'NONE', #206 ) ;
#21109=CARTESIAN_POINT ( 'NONE',  ( -4.178947244162641184, -48.81675275154074001, 3.367451375481625320 ) ) ;
#21112=CARTESIAN_POINT ( 'NONE',  ( -22.23342874802667168, -7.677086057585177592, -30.68433055777678931 ) ) ;
#21113=CARTESIAN_POINT ( 'NONE',  ( -1.031422197589711987, -44.01264471863856187, -12.69107518035484361 ) ) ;
#21117=CARTESIAN_POINT ( 'NONE',  ( -1.031422197589711987, -43.06660437151296605, 15.60268798220683273 ) ) ;
#21126=CARTESIAN_POINT ( 'NONE',  ( -55.25719721206881729, -0.0006290797159201363779, 0.01115102788683008592 ) ) ;
#21133=CARTESIAN_POINT ( 'NONE',  ( -6.574463467970658392, 50.12924290857549181, 11.01561683919999091 ) ) ;
#21141=CARTESIAN_POINT ( 'NONE',  ( -1.050231094221210970, 45.79908322896420003, -0.2545420581350661404 ) ) ;
#21143=CARTESIAN_POINT ( 'NONE',  ( -24.53237795827028123, -14.09663893005605395, -30.86653739599992363 ) ) ;
#21144=CARTESIAN_POINT ( 'NONE',  ( -20.37983603106073005, 18.69865230096527142, -23.16947629293368038 ) ) ;
#21147=B_SPLINE_CURVE_WITH_KNOTS ( 'NONE', 3,
 ( #28455, #19553, #15802, #22141, #15634, #24309, #11201, #19830 ),
 .UNSPECIFIED., .F., .F.,
 ( 4, 2, 2, 4 ),
 ( 0.000000000000000000, 0.002761524886576657151, 0.005523049773153314301, 0.01104609954630661819 ),
 .UNSPECIFIED. ) ;
#21154=CARTESIAN_POINT ( 'NONE',  ( -23.77929240705206482, 35.68044874544704470, 6.464423883190010933 ) ) ;
#21155=EDGE_CURVE ( 'NONE', #414, #21724, #26304, .T. ) ;
#21158=CONICAL_SURFACE ( 'NONE', #8742, 53.53553390275978785, 0.7853981625000051592 ) ;
#21159=CARTESIAN_POINT ( 'NONE',  ( -1.045287976400351981, 12.68782741917293855, -44.00138577190654132 ) ) ;
#21165=CARTESIAN_POINT ( 'NONE',  ( -1.044557008772712514, -25.56990300677008676, -37.98985164565319650 ) ) ;
#21169=ADVANCED_FACE ( 'NONE', ( #18476 ), #4712, .T. ) ;
#21173=ORIENTED_EDGE ( 'NONE', *, *, #24530, .F. ) ;
#21180=CIRCLE ( 'NONE', #9222, 53.53553390275978785 ) ;
#21200=CARTESIAN_POINT ( 'NONE',  ( -55.25297051322618813, -0.01354497706059863693, -0.006313402748433391727 ) ) ;
#21208=ORIENTED_EDGE ( 'NONE', *, *, #3720, .F. ) ;
#21211=VERTEX_POINT ( 'NONE', #21051 ) ;
#21222=CARTESIAN_POINT ( 'NONE',  ( -55.24390624410018802, 0.009209468562451588944, -0.004896917417127890151 ) ) ;
#21232=LINE ( 'NONE', #28120, #12924 ) ;
#21240=LINE ( 'NONE', #1100, #27299 ) ;
#21246=CARTESIAN_POINT ( 'NONE',  ( -1.619063947482201282, 35.99532424477380488, -29.22875152547769062 ) ) ;
#21249=CARTESIAN_POINT ( 'NONE',  ( -1.259972190295313599, -44.39825172539703146, -12.06706380853675142 ) ) ;
#21256=CARTESIAN_POINT ( 'NONE',  ( -1.045287976400362417, 25.66401692420069125, 37.92705037016716574 ) ) ;
#21264=CARTESIAN_POINT ( 'NONE',  ( -8.786685647604890903, -37.00619870957905277, 38.68584556812340480 ) ) ;
#21268=CARTESIAN_POINT ( 'NONE',  ( -1.619063947482201282, 38.92136151114908671, -25.20140673341387227 ) ) ;
#21270=CARTESIAN_POINT ( 'NONE',  ( -21.41427618760458174, 19.54551635498129514, -23.81423075802588940 ) ) ;
#21274=CARTESIAN_POINT ( 'NONE',  ( -20.37983603106074426, -29.73529213200290400, -1.508851015062473211 ) ) ;
#21278=CARTESIAN_POINT ( 'NONE',  ( -1.583189561560252701, 11.94859433442964658, 44.83405390829658188 ) ) ;
#21285=CARTESIAN_POINT ( 'NONE',  ( -1.045287976400386842, 37.92705037016744285, -25.66401692420027203 ) ) ;
#21287=DIRECTION ( 'NONE',  ( 0.7563875759206388771, 0.6104009704506959677, 0.2351350468682803785 ) ) ;
#21289=CARTESIAN_POINT ( 'NONE',  ( -1.049819825607587909, -43.71263398674761191, -13.66706894614421408 ) ) ;
#21297=CARTESIAN_POINT ( 'NONE',  ( -1.113548883309551929, -16.03115934825500588, 42.96943836789122173 ) ) ;
#21305=CARTESIAN_POINT ( 'NONE',  ( -1.113548883309558368, 42.96943836789127147, 16.03115934825484956 ) ) ;
#21306=AXIS2_PLACEMENT_3D ( 'NONE', #21564, #19675, #26300 ) ;
#21310=CARTESIAN_POINT ( 'NONE',  ( -20.20700224038492721, -18.19058640100206503, 23.35150625415678860 ) ) ;
#21314=EDGE_LOOP ( 'NONE', ( #9817, #7139, #25960, #280 ) ) ;
#21315=CARTESIAN_POINT ( 'NONE',  ( -1.619063947482197729, -38.92136151114925724, -25.20140673341360227 ) ) ;
#21316=CARTESIAN_POINT ( 'NONE',  ( -1.045287976400365970, 1.530335034933814731, -45.76855895860946788 ) ) ;
#21317=ORIENTED_EDGE ( 'NONE', *, *, #4641, .F. ) ;
#21327=CARTESIAN_POINT ( 'NONE',  ( -55.25297051322618813, 0.01466904165775178431, 0.002853887643042449414 ) ) ;
#21335=CIRCLE ( 'NONE', #8939, 34.60786435723138510 ) ;
#21344=VERTEX_POINT ( 'NONE', #21487 ) ;
#21345=DIRECTION ( 'NONE',  ( -0.7637818620346801257, 0.1788995134688785849, -0.6201872550346672064 ) ) ;
#21346=( BOUNDED_SURFACE ( )  B_SPLINE_SURFACE ( 3, 1, ( 
 ( #25966, #23825 ),
 ( #10569, #10437 ),
 ( #19336, #6257 ),
 ( #28112, #17446 ) ),
 .UNSPECIFIED., .F., .F., .F. ) 
 B_SPLINE_SURFACE_WITH_KNOTS ( ( 4, 4 ),
 ( 2, 2 ),
 ( 0.000000000000000000, 1.000000000000000000 ),
 ( 0.000000000000000000, 1.000000000000000000 ),
 .UNSPECIFIED. ) 
 GEOMETRIC_REPRESENTATION_ITEM ( )  RATIONAL_B_SPLINE_SURFACE ( (
 ( 1.000000000000000000, 1.000000000000000000),
 ( 0.9934239774497837239, 0.8357310067453919133),
 ( 0.9934239774497837239, 0.8357310067453919133),
 ( 1.000000000000000000, 1.000000000000000000) ) ) 
 REPRESENTATION_ITEM ( '' )  SURFACE ( )  );
#21356=ADVANCED_FACE ( 'NONE', ( #176 ), #14902, .F. ) ;
#21357=CARTESIAN_POINT ( 'NONE',  ( -25.21435515916043713, -23.92354251275954979, -25.00736669481013053 ) ) ;
#21369=CARTESIAN_POINT ( 'NONE',  ( -8.786685647604896232, 9.545808661481343549, 52.67761315067276229 ) ) ;
#21373=CARTESIAN_POINT ( 'NONE',  ( -55.25297051322618813, -0.01483298743815008106, -0.001818774723749387676 ) ) ;
#21374=B_SPLINE_CURVE_WITH_KNOTS ( 'NONE', 3,
 ( #10824, #19584, #16881, #25668, #5948, #19170, #14699 ),
 .UNSPECIFIED., .F., .F.,
 ( 4, 3, 4 ),
 ( 1.734723475976807094E-18, 0.009512539173626401862, 0.02506242213020843518 ),
 .UNSPECIFIED. ) ;
#21375=DIRECTION ( 'NONE',  ( 0.7637818620346800147, -0.3617919495470791613, -0.5345501402766260624 ) ) ;
#21377=ORIENTED_EDGE ( 'NONE', *, *, #17565, .T. ) ;
#21379=CARTESIAN_POINT ( 'NONE',  ( -1.539760825549686407, -38.84664866728793697, -25.17088484262129455 ) ) ;
#21380=ORIENTED_EDGE ( 'NONE', *, *, #11295, .F. ) ;
#21384=( BOUNDED_SURFACE ( )  B_SPLINE_SURFACE ( 3, 1, ( 
 ( #18234, #22737 ),
 ( #26455, #17946 ),
 ( #6758, #20256 ),
 ( #11206, #7047 ) ),
 .UNSPECIFIED., .F., .F., .F. ) 
 B_SPLINE_SURFACE_WITH_KNOTS ( ( 4, 4 ),
 ( 2, 2 ),
 ( 0.000000000000000000, 1.000000000000000000 ),
 ( 0.000000000000000000, 1.000000000000000000 ),
 .UNSPECIFIED. ) 
 GEOMETRIC_REPRESENTATION_ITEM ( )  RATIONAL_B_SPLINE_SURFACE ( (
 ( 1.000000000000000000, 1.000000000000000000),
 ( 0.7789835883360578528, 0.9689951854195403280),
 ( 0.7789835883360578528, 0.9689951854195403280),
 ( 1.000000000000000000, 1.000000000000000000) ) ) 
 REPRESENTATION_ITEM ( '' )  SURFACE ( )  );
#21398=B_SPLINE_CURVE_WITH_KNOTS ( 'NONE', 3,
 ( #25926, #6217, #4033, #28205, #8505, #16725 ),
 .UNSPECIFIED., .F., .F.,
 ( 4, 2, 4 ),
 ( 1.734723475976807094E-18, 0.0004335184443140234316, 0.0008670368886280451284 ),
 .UNSPECIFIED. ) ;
#21401=CARTESIAN_POINT ( 'NONE',  ( -1.031422197589711987, 44.01264471863864713, 12.69107518035455762 ) ) ;
#21414=CARTESIAN_POINT ( 'NONE',  ( -8.786685647604887350, -25.35688121747534751, -47.14957014837345639 ) ) ;
#21416=VERTEX_POINT ( 'NONE', #17386 ) ;
#21424=CARTESIAN_POINT ( 'NONE',  ( -8.786685647604896232, -7.199674155858612146, 53.04920435127190359 ) ) ;
#21428=CARTESIAN_POINT ( 'NONE',  ( -28.41354790283022069, 19.47297445639550162, -12.60397206714839413 ) ) ;
#21432=CARTESIAN_POINT ( 'NONE',  ( -1.463510566862824991, -29.09194585123808707, 35.90603835816536815 ) ) ;
#21435=LINE ( 'NONE', #24037, #1492 ) ;
#21441=CARTESIAN_POINT ( 'NONE',  ( -20.20612091757423912, 1.137293889216362874, -29.57813639663777039 ) ) ;
#21442=DIRECTION ( 'NONE',  ( -0.7071067818211357325, 9.150583771627653840E-17, -0.7071067805519594129 ) ) ;
#21444=CARTESIAN_POINT ( 'NONE',  ( -1.323439229708146536, 43.04565903621286083, -16.42345129173351381 ) ) ;
#21450=CARTESIAN_POINT ( 'NONE',  ( -20.37983603106074426, -18.69865230096510444, 23.16947629293382960 ) ) ;
#21451=CARTESIAN_POINT ( 'NONE',  ( -1.050230346682690108, -37.05182464822001975, -26.92058491724852942 ) ) ;
#21460=EDGE_CURVE ( 'NONE', #17730, #21851, #21435, .T. ) ;
#21462=ORIENTED_EDGE ( 'NONE', *, *, #2654, .T. ) ;
#21468=CARTESIAN_POINT ( 'NONE',  ( -1.019300379054419947, 12.21833869579527310, 44.15350047934384747 ) ) ;
#21476=CARTESIAN_POINT ( 'NONE',  ( -1.031422197589711764, 28.14735071801743871, -36.13727897780136544 ) ) ;
#21480=CARTESIAN_POINT ( 'NONE',  ( -20.57838717382308502, 27.96569011373086866, -10.78122205917010135 ) ) ;
#21487=CARTESIAN_POINT ( 'NONE',  ( -1.619063947482197729, -35.99532424477401094, -29.22875152547743838 ) ) ;
#21488=ORIENTED_EDGE ( 'NONE', *, *, #15521, .T. ) ;
#21491=ORIENTED_EDGE ( 'NONE', *, *, #24948, .F. ) ;
#21494=DIRECTION ( 'NONE',  ( 0.000000000000000000, 5.223019709707975211E-21, -1.000000000000000000 ) ) ;
#21495=CARTESIAN_POINT ( 'NONE',  ( -1.045287976400365970, 44.00138577190666922, 12.68782741917247670 ) ) ;
#21497=CARTESIAN_POINT ( 'NONE',  ( -16.86833981943423311, 31.95666732167563850, -30.57013526701928186 ) ) ;
#21499=CARTESIAN_POINT ( 'NONE',  ( -1.049817751779873465, 37.35030165458175588, -26.50542916749582645 ) ) ;
#21509=ORIENTED_EDGE ( 'NONE', *, *, #10823, .F. ) ;
#21515=B_SPLINE_CURVE_WITH_KNOTS ( 'NONE', 3,
 ( #10546, #28086, #6237, #10691, #17156, #25947, #14988, #21613 ),
 .UNSPECIFIED., .F., .F.,
 ( 4, 2, 2, 4 ),
 ( 0.000000000000000000, 0.002761524886576667125, 0.005523049773153334251, 0.01104609954630666677 ),
 .UNSPECIFIED. ) ;
#21519=ORIENTED_EDGE ( 'NONE', *, *, #6034, .F. ) ;
#21523=B_SPLINE_CURVE_WITH_KNOTS ( 'NONE', 3,
 ( #25032, #13343, #22140, #2403 ),
 .UNSPECIFIED., .F., .F.,
 ( 4, 4 ),
 ( 1.906343156168367839E-16, 0.0009910334943227156780 ),
 .UNSPECIFIED. ) ;
#21526=CARTESIAN_POINT ( 'NONE',  ( -1.045287976400383290, 12.68782741917383738, 44.00138577190627842 ) ) ;
#21529=ORIENTED_EDGE ( 'NONE', *, *, #17252, .T. ) ;
#21537=ADVANCED_FACE ( 'NONE', ( #12786 ), #15712, .T. ) ;
#21540=CARTESIAN_POINT ( 'NONE',  ( -25.21435515916025594, 1.749597353048488237E-16, -4.373993382621220594E-17 ) ) ;
#21541=CARTESIAN_POINT ( 'NONE',  ( -20.20700224038492010, -16.58740185276728241, -24.51628800869040958 ) ) ;
#21545=ORIENTED_EDGE ( 'NONE', *, *, #9554, .T. ) ;
#21548=DIRECTION ( 'NONE',  ( 1.000000000000000000, -6.938893903907226837E-18, 1.734723475976806709E-18 ) ) ;
#21555=B_SPLINE_CURVE_WITH_KNOTS ( 'NONE', 3,
 ( #26516, #24379, #4646, #28111, #10714, #4075, #12846, #17179 ),
 .UNSPECIFIED., .F., .F.,
 ( 4, 2, 2, 4 ),
 ( 2.194186273941487696E-16, 0.002761568181852869838, 0.005523136363705520233, 0.01104627272741081495 ),
 .UNSPECIFIED. ) ;
#21558=( BOUNDED_SURFACE ( )  B_SPLINE_SURFACE ( 3, 1, ( 
 ( #16865, #6215 ),
 ( #10663, #4030 ),
 ( #23912, #1450 ),
 ( #10520, #23781 ) ),
 .UNSPECIFIED., .F., .F., .F. ) 
 B_SPLINE_SURFACE_WITH_KNOTS ( ( 4, 4 ),
 ( 2, 2 ),
 ( 0.000000000000000000, 1.000000000000000000 ),
 ( 0.000000000000000000, 1.000000000000000000 ),
 .UNSPECIFIED. ) 
 GEOMETRIC_REPRESENTATION_ITEM ( )  RATIONAL_B_SPLINE_SURFACE ( (
 ( 1.000000000000000000, 1.000000000000000000),
 ( 0.9934239774497837239, 0.8357310067453919133),
 ( 0.9934239774497837239, 0.8357310067453919133),
 ( 1.000000000000000000, 1.000000000000000000) ) ) 
 REPRESENTATION_ITEM ( '' )  SURFACE ( )  );
#21559=LINE ( 'NONE', #27769, #8869 ) ;
#21560=ORIENTED_EDGE ( 'NONE', *, *, #18124, .F. ) ;
#21561=CARTESIAN_POINT ( 'NONE',  ( -7.078251931573400491, -11.16394717458712726, -50.86685171665407523 ) ) ;
#21564=CARTESIAN_POINT ( 'NONE',  ( -19.53423201713129842, 1.355459634611817431E-16, -3.388649086529543578E-17 ) ) ;
#21566=CARTESIAN_POINT ( 'NONE',  ( 14.74894986621300319, -1.023413983156987147E-16, 2.558534957892467869E-17 ) ) ;
#21570=CARTESIAN_POINT ( 'NONE',  ( -7.078251931573406708, 47.71415099571806451, -20.86696228105241602 ) ) ;
#21583=CARTESIAN_POINT ( 'NONE',  ( -1.539760825549693068, 43.19716078875438825, -16.63252404870369006 ) ) ;
#21589=CARTESIAN_POINT ( 'NONE',  ( -25.21435515916025594, 1.749597353048488237E-16, -4.373993382621220594E-17 ) ) ;
#21593=CARTESIAN_POINT ( 'NONE',  ( -20.47566338032522992, -25.06314818626703200, -16.24827550219816885 ) ) ;
#21595=CARTESIAN_POINT ( 'NONE',  ( -1.619063947482197729, -35.99532424477401094, -29.22875152547743838 ) ) ;
#21602=CARTESIAN_POINT ( 'NONE',  ( -1.619063947482197729, 46.30105812165548684, -2.489035965910316506 ) ) ;
#21604=VECTOR ( 'NONE', #21813, 1000.000000000000114 ) ;
#21613=CARTESIAN_POINT ( 'NONE',  ( -1.619063947482197729, 38.92136151114943488, 25.20140673341330739 ) ) ;
#21618=ORIENTED_EDGE ( 'NONE', *, *, #21067, .F. ) ;
#21620=LINE ( 'NONE', #12981, #6952 ) ;
#21623=EDGE_LOOP ( 'NONE', ( #24923, #9669, #26430, #1652 ) ) ;
#21631=DIRECTION ( 'NONE',  ( 1.000000000000000000, -6.938893903907226837E-18, 1.734723475976806709E-18 ) ) ;
#21632=EDGE_CURVE ( 'NONE', #15681, #6278, #21523, .T. ) ;
#21633=CARTESIAN_POINT ( 'NONE',  ( -8.786685647604894456, 7.199674155859698388, 53.04920435127174017 ) ) ;
#21635=CARTESIAN_POINT ( 'NONE',  ( -20.20612092514784663, 8.058517256681097862, -28.48192215759668855 ) ) ;
#21636=VECTOR ( 'NONE', #14133, 1000.000000000000000 ) ;
#21637=CARTESIAN_POINT ( 'NONE',  ( -20.90916690077959927, 28.59207721780146727, -27.35210456531384082 ) ) ;
#21641=FACE_OUTER_BOUND ( 'NONE', #27331, .T. ) ;
#21642=CARTESIAN_POINT ( 'NONE',  ( -1.049819825607602342, 36.75053263699390271, -27.33096219556254169 ) ) ;
#21653=CARTESIAN_POINT ( 'NONE',  ( -8.786685647604890903, -37.00619870957961410, -38.68584556812286479 ) ) ;
#21658=CARTESIAN_POINT ( 'NONE',  ( -24.53239521893650021, -3.868435622621272163, 33.71193723315178659 ) ) ;
#21661=AXIS2_PLACEMENT_3D ( 'NONE', #1250, #18815, #10050 ) ;
#21666=CARTESIAN_POINT ( 'NONE',  ( -1.031422197589711764, 43.06660437151329290, 15.60268798220593034 ) ) ;
#21668=DIRECTION ( 'NONE',  ( -0.7563875759206388771, 0.5490129373055280260, 0.3556158456312881189 ) ) ;
#21669=CARTESIAN_POINT ( 'NONE',  ( -20.20612091757417161, 27.77903622052274102, 10.22177757278288013 ) ) ;
#21671=CARTESIAN_POINT ( 'NONE',  ( -1.056502255334264895, -26.51074901220476576, 37.35734037467662461 ) ) ;
#21672=LINE ( 'NONE', #19227, #26687 ) ;
#21681=CARTESIAN_POINT ( 'NONE',  ( -55.24300891470648622, -0.003362556190414485880, 0.009225237711097986765 ) ) ;
#21682=VERTEX_POINT ( 'NONE', #3696 ) ;
#21689=DIRECTION ( 'NONE',  ( -0.7563875759206389882, -0.3556158456312901173, 0.5490129373055266937 ) ) ;
#21695=CARTESIAN_POINT ( 'NONE',  ( -20.20612091757422490, -1.137293889216157705, 29.57813639663779171 ) ) ;
#21707=LINE ( 'NONE', #17239, #17147 ) ;
#21714=CARTESIAN_POINT ( 'NONE',  ( -20.20612092514784663, 28.48192215759677737, 8.058517256680804763 ) ) ;
#21722=ORIENTED_EDGE ( 'NONE', *, *, #14128, .F. ) ;
#21724=VERTEX_POINT ( 'NONE', #6018 ) ;
#21725=CARTESIAN_POINT ( 'NONE',  ( -1.050229599974472627, -43.63650726458052986, 13.90955673306172002 ) ) ;
#21732=ORIENTED_EDGE ( 'NONE', *, *, #7530, .T. ) ;
#21738=AXIS2_PLACEMENT_3D ( 'NONE', #11683, #7095, #15991 ) ;
#21739=B_SPLINE_CURVE_WITH_KNOTS ( 'NONE', 3,
 ( #23303, #16374, #14638, #11918 ),
 .UNSPECIFIED., .F., .F.,
 ( 4, 4 ),
 ( 0.0009910334943227156780, 0.001982023823822944616 ),
 .UNSPECIFIED. ) ;
#21750=CARTESIAN_POINT ( 'NONE',  ( -55.25297051322618813, -0.01483298743814594547, 0.001818774723749421287 ) ) ;
#21753=CARTESIAN_POINT ( 'NONE',  ( -55.24271866751342941, 0.004256484107793641683, 0.008488649505346114801 ) ) ;
#21755=CIRCLE ( 'NONE', #18558, 53.53553390275978785 ) ;
#21756=VECTOR ( 'NONE', #6621, 1000.000000000000114 ) ;
#21765=FACE_OUTER_BOUND ( 'NONE', #4062, .T. ) ;
#21766=CARTESIAN_POINT ( 'NONE',  ( -1.619063947482197729, 11.94059994246222622, 44.80407745103770623 ) ) ;
#21767=CARTESIAN_POINT ( 'NONE',  ( -1.044557008772714068, -44.03203053429562885, 12.57891310333395118 ) ) ;
#21771=VERTEX_POINT ( 'NONE', #25730 ) ;
#21776=( BOUNDED_SURFACE ( )  B_SPLINE_SURFACE ( 3, 1, ( 
 ( #14263, #23086 ),
 ( #9253, #18009 ),
 ( #26797, #20320 ),
 ( #15867, #24676 ) ),
 .UNSPECIFIED., .F., .F., .F. ) 
 B_SPLINE_SURFACE_WITH_KNOTS ( ( 4, 4 ),
 ( 2, 2 ),
 ( 0.000000000000000000, 1.000000000000000000 ),
 ( 0.000000000000000000, 1.000000000000000000 ),
 .UNSPECIFIED. ) 
 GEOMETRIC_REPRESENTATION_ITEM ( )  RATIONAL_B_SPLINE_SURFACE ( (
 ( 1.000000000000000000, 1.000000000000000000),
 ( 0.9934239774497838349, 0.8357310067453913582),
 ( 0.9934239774497838349, 0.8357310067453913582),
 ( 1.000000000000000000, 1.000000000000000000) ) ) 
 REPRESENTATION_ITEM ( '' )  SURFACE ( )  );
#21778=ORIENTED_EDGE ( 'NONE', *, *, #9103, .T. ) ;
#21785=EDGE_CURVE ( 'NONE', #17023, #26786, #22198, .T. ) ;
#21788=CARTESIAN_POINT ( 'NONE',  ( -20.90916690077965612, 5.322316104228523415, 39.20864005633514893 ) ) ;
#21798=CARTESIAN_POINT ( 'NONE',  ( -1.031422197589716205, -37.93675465142454328, 25.67058493451484225 ) ) ;
#21801=VERTEX_POINT ( 'NONE', #8582 ) ;
#21813=DIRECTION ( 'NONE',  ( 0.7637818620346800147, 0.6451161201712181104, 0.02150485345384620800 ) ) ;
#21814=EDGE_LOOP ( 'NONE', ( #24509, #4850, #18211, #22275, #23714, #5206 ) ) ;
#21815=CARTESIAN_POINT ( 'NONE',  ( -1.583189561560255143, 43.29471907393764951, 16.68617981233656877 ) ) ;
#21826=VERTEX_POINT ( 'NONE', #13039 ) ;
#21827=ORIENTED_EDGE ( 'NONE', *, *, #6565, .T. ) ;
#21828=CARTESIAN_POINT ( 'NONE',  ( -25.21435515916025594, 1.749597353048488237E-16, -4.373993382621220594E-17 ) ) ;
#21832=CARTESIAN_POINT ( 'NONE',  ( -4.473127245936431073, 45.82513704981569447, 18.25038884639822712 ) ) ;
#21835=CARTESIAN_POINT ( 'NONE',  ( -8.786685647604896232, 25.35688121747570278, 47.14957014837326454 ) ) ;
#21846=EDGE_LOOP ( 'NONE', ( #25199, #7820, #25183, #20734 ) ) ;
#21851=VERTEX_POINT ( 'NONE', #17633 ) ;
#21852=CARTESIAN_POINT ( 'NONE',  ( -1.044556982611271279, -12.57890920527746381, 44.03203163107538387 ) ) ;
#21854=CARTESIAN_POINT ( 'NONE',  ( -1.113427685307001314, -45.82016658690749722, 1.967672929087657785 ) ) ;
#21858=CARTESIAN_POINT ( 'NONE',  ( -1.048171036023500147, -1.020520027228813298, 45.78635789057867100 ) ) ;
#21868=CARTESIAN_POINT ( 'NONE',  ( -1.619063947482197729, -29.22875152547730337, 35.99532424477411041 ) ) ;
#21871=CARTESIAN_POINT ( 'NONE',  ( -55.25719721206881729, 0.01041086141212550775, -0.004044147484878501606 ) ) ;
#21872=CARTESIAN_POINT ( 'NONE',  ( -22.23342874802669655, -24.24669006619387090, -20.31166691703116811 ) ) ;
#21899=CARTESIAN_POINT ( 'NONE',  ( -1.031422197589716205, -44.01264471863839134, 12.69107518035547955 ) ) ;
#21903=CARTESIAN_POINT ( 'NONE',  ( -55.24390624410018802, -0.01032895241566962087, 0.001451500391950532459 ) ) ;
#21913=ORIENTED_EDGE ( 'NONE', *, *, #28078, .T. ) ;
#21920=CARTESIAN_POINT ( 'NONE',  ( -1.239374126674604337, 38.61989855450975995, 25.08410696974200604 ) ) ;
#21923=CARTESIAN_POINT ( 'NONE',  ( -6.588769196390765970, 38.42957692275894033, 34.04709086065274448 ) ) ;
#21926=CARTESIAN_POINT ( 'NONE',  ( -1.049819825607599455, 27.33096219556293249, 36.75053263699358297 ) ) ;
#21934=FACE_OUTER_BOUND ( 'NONE', #12728, .T. ) ;
#21936=( BOUNDED_SURFACE ( )  B_SPLINE_SURFACE ( 3, 1, ( 
 ( #22483, #26490 ),
 ( #26772, #17987 ),
 ( #13244, #2745 ),
 ( #24354, #5042 ) ),
 .UNSPECIFIED., .F., .F., .F. ) 
 B_SPLINE_SURFACE_WITH_KNOTS ( ( 4, 4 ),
 ( 2, 2 ),
 ( 0.000000000000000000, 1.000000000000000000 ),
 ( 0.000000000000000000, 1.000000000000000000 ),
 .UNSPECIFIED. ) 
 GEOMETRIC_REPRESENTATION_ITEM ( )  RATIONAL_B_SPLINE_SURFACE ( (
 ( 1.000000000000000000, 1.000000000000000000),
 ( 0.7789835883360578528, 0.9689951854195403280),
 ( 0.7789835883360578528, 0.9689951854195403280),
 ( 1.000000000000000000, 1.000000000000000000) ) ) 
 REPRESENTATION_ITEM ( '' )  SURFACE ( )  );
#21948=ORIENTED_EDGE ( 'NONE', *, *, #17732, .F. ) ;
#21953=CARTESIAN_POINT ( 'NONE',  ( -20.47566262905010603, 27.87687924095562408, 10.72601569609867944 ) ) ;
#21958=CARTESIAN_POINT ( 'NONE',  ( -55.24340739397742084, -0.008612749836246226184, 0.005344433640972935315 ) ) ;
#21959=CARTESIAN_POINT ( 'NONE',  ( -1.539760825549689072, 46.22267384399381740, -2.469813586483248447 ) ) ;
#21967=CARTESIAN_POINT ( 'NONE',  ( -55.25719721206881729, 0.002847566758684554142, 0.01079965405819473083 ) ) ;
#21971=( BOUNDED_SURFACE ( )  B_SPLINE_SURFACE ( 3, 1, ( 
 ( #12629, #28299 ),
 ( #10903, #6040 ),
 ( #14928, #17362 ),
 ( #10489, #21278 ) ),
 .UNSPECIFIED., .F., .F., .F. ) 
 B_SPLINE_SURFACE_WITH_KNOTS ( ( 4, 4 ),
 ( 2, 2 ),
 ( 0.000000000000000000, 1.000000000000000000 ),
 ( 0.000000000000000000, 1.000000000000000000 ),
 .UNSPECIFIED. ) 
 GEOMETRIC_REPRESENTATION_ITEM ( )  RATIONAL_B_SPLINE_SURFACE ( (
 ( 1.000000000000000000, 1.000000000000000000),
 ( 0.7789835883360578528, 0.9689951854195403280),
 ( 0.7789835883360578528, 0.9689951854195403280),
 ( 1.000000000000000000, 1.000000000000000000) ) ) 
 REPRESENTATION_ITEM ( '' )  SURFACE ( )  );
#21973=CARTESIAN_POINT ( 'NONE',  ( -55.24390624410018802, 0.007245494385991918876, 0.007503127514281743120 ) ) ;
#21981=DIRECTION ( 'NONE',  ( -0.7563875759206388771, -0.03500244528123461207, -0.6531865459554673237 ) ) ;
#21984=LINE ( 'NONE', #21428, #17024 ) ;
#21985=DIRECTION ( 'NONE',  ( 1.000000000000000000, -6.938893903907226837E-18, 1.734723475976806709E-18 ) ) ;
#21988=CARTESIAN_POINT ( 'NONE',  ( -1.050230347699842692, 1.897926697972695375E-16, 45.79907861674080749 ) ) ;
#21999=CARTESIAN_POINT ( 'NONE',  ( -1.049819825607588575, -27.33096219556267670, -36.75053263699379613 ) ) ;
#22001=CARTESIAN_POINT ( 'NONE',  ( -5.986830583229481917, 38.20088153919500229, -33.39046620690925238 ) ) ;
#22017=ORIENTED_EDGE ( 'NONE', *, *, #23794, .F. ) ;
#22030=ORIENTED_EDGE ( 'NONE', *, *, #3193, .T. ) ;
#22036=CARTESIAN_POINT ( 'NONE',  ( -55.25719721206881729, -0.002847566758682281655, 0.01079965405819869988 ) ) ;
#22045=VERTEX_POINT ( 'NONE', #15114 ) ;
#22056=CARTESIAN_POINT ( 'NONE',  ( -55.25719721206881729, 0.009391134844729439810, -0.006045473558784624467 ) ) ;
#22064=AXIS2_PLACEMENT_3D ( 'NONE', #26494, #13390, #24505 ) ;
#22074=FACE_OUTER_BOUND ( 'NONE', #13818, .T. ) ;
#22085=CARTESIAN_POINT ( 'NONE',  ( -55.24340739397742084, -0.009386184976286139278, -0.003826481709803953961 ) ) ;
#22086=CARTESIAN_POINT ( 'NONE',  ( -20.57838717382308147, -27.96569011373078339, 10.78122205917029675 ) ) ;
#22087=EDGE_LOOP ( 'NONE', ( #20395, #24191, #15141, #11652 ) ) ;
#22106=CARTESIAN_POINT ( 'NONE',  ( 14.74894986621300141, -1.023413983156987271E-16, 2.558534957892468177E-17 ) ) ;
#22123=DIRECTION ( 'NONE',  ( -1.000000000000000000, 6.938893903907226837E-18, -1.734723475976806709E-18 ) ) ;
#22126=CARTESIAN_POINT ( 'NONE',  ( -20.57838717382308147, -25.16001208503117326, -16.28767523336112433 ) ) ;
#22132=CARTESIAN_POINT ( 'NONE',  ( -1.155031165708893415, -45.85732438018708024, 2.068616213631418344 ) ) ;
#22140=CARTESIAN_POINT ( 'NONE',  ( -20.20997486282891131, 0.3303743256174362375, -29.60348406988234871 ) ) ;
#22141=CARTESIAN_POINT ( 'NONE',  ( -6.574463467970653063, 20.55340846381200848, 47.03022655117382556 ) ) ;
#22144=AXIS2_PLACEMENT_3D ( 'NONE', #21828, #4539, #2224 ) ;
#22162=ORIENTED_EDGE ( 'NONE', *, *, #24034, .T. ) ;
#22163=VERTEX_POINT ( 'NONE', #22591 ) ;
#22164=ADVANCED_FACE ( 'NONE', ( #20554 ), #4478, .F. ) ;
#22166=CIRCLE ( 'NONE', #20782, 53.53553390275978785 ) ;
#22167=EDGE_CURVE ( 'NONE', #15365, #8101, #9511, .T. ) ;
#22170=CARTESIAN_POINT ( 'NONE',  ( -7.078251931573400491, -5.101176922830306104, 51.82710018979479116 ) ) ;
#22172=B_SPLINE_CURVE_WITH_KNOTS ( 'NONE', 3,
 ( #3262, #11894, #22563, #18212, #13753, #5129, #7301, #955, #7447, #11608 ),
 .UNSPECIFIED., .F., .F.,
 ( 4, 2, 2, 2, 4 ),
 ( 3.104682540412587095E-18, 0.0003346267210630946812, 0.0006692534421261863266, 0.001003880163189277809, 0.001338506884252369401 ),
 .UNSPECIFIED. ) ;
#22174=CARTESIAN_POINT ( 'NONE',  ( -8.786685647604890903, -47.14957014837335691, 25.35688121747554291 ) ) ;
#22175=CARTESIAN_POINT ( 'NONE',  ( -55.24728320129491266, -0.01137345571547045305, -0.009072670231978460439 ) ) ;
#22176=ORIENTED_EDGE ( 'NONE', *, *, #5063, .T. ) ;
#22182=CARTESIAN_POINT ( 'NONE',  ( -25.21435515916043357, -15.02493970636125198, 31.17620025257602379 ) ) ;
#22195=CARTESIAN_POINT ( 'NONE',  ( -1.045287976400351981, 43.05558670614237116, -15.59869763335110449 ) ) ;
#22198=B_SPLINE_CURVE_WITH_KNOTS ( 'NONE', 3,
 ( #4256, #21959, #28283, #23864, #19789, #12885, #8307, #17074, #10755, #25865 ),
 .UNSPECIFIED., .F., .F.,
 ( 4, 2, 2, 2, 4 ),
 ( 1.371419323662773916E-18, 0.0003346267210630953859, 0.0006692534421261894708, 0.001003880163189283447, 0.001338506884252376773 ),
 .UNSPECIFIED. ) ;
#22207=VECTOR ( 'NONE', #15443, 1000.000000000000114 ) ;
#22210=CARTESIAN_POINT ( 'NONE',  ( -20.21097721650786738, 29.61001326827675939, -0.3305964462498667822 ) ) ;
#22220=CARTESIAN_POINT ( 'NONE',  ( -55.24390624410018802, -0.01032895241566633357, -0.001451500391952961289 ) ) ;
#22238=ADVANCED_FACE ( 'NONE', ( #6027 ), #1934, .T. ) ;
#22244=FACE_OUTER_BOUND ( 'NONE', #27096, .T. ) ;
#22258=CARTESIAN_POINT ( 'NONE',  ( -55.24390624410018802, -0.007503127514277506058, -0.007245494385991484328 ) ) ;
#22259=CARTESIAN_POINT ( 'NONE',  ( -21.41430102051745266, 30.75470819672112199, -1.815007301162081088 ) ) ;
#22263=FACE_OUTER_BOUND ( 'NONE', #17881, .T. ) ;
#22267=EDGE_CURVE ( 'NONE', #7492, #18707, #18352, .T. ) ;
#22270=ADVANCED_FACE ( 'NONE', ( #1678 ), #1516, .T. ) ;
#22275=ORIENTED_EDGE ( 'NONE', *, *, #26289, .T. ) ;
#22282=CARTESIAN_POINT ( 'NONE',  ( -20.20700224038492721, 28.44216453106536946, -8.199606986804427677 ) ) ;
#22291=ORIENTED_EDGE ( 'NONE', *, *, #6568, .T. ) ;
#22293=VERTEX_POINT ( 'NONE', #21268 ) ;
#22294=CARTESIAN_POINT ( 'NONE',  ( -1.048172774974284405, -27.73787987941035027, -36.44231470008705998 ) ) ;
#22299=CARTESIAN_POINT ( 'NONE',  ( -2.904412668506678674, -47.56768199507435213, -2.864640348250463653 ) ) ;
#22305=CARTESIAN_POINT ( 'NONE',  ( -18.41936578851709783, 18.42310649277627022, -38.22933728004698395 ) ) ;
#22311=CARTESIAN_POINT ( 'NONE',  ( -20.20700224038492721, -27.82980252387812570, 10.08426345511618649 ) ) ;
#22318=CARTESIAN_POINT ( 'NONE',  ( -20.20700224038492721, 27.82980252387819675, -10.08426345511598932 ) ) ;
#22323=VERTEX_POINT ( 'NONE', #21541 ) ;
#22332=CARTESIAN_POINT ( 'NONE',  ( -21.41430102051745266, 29.81033373822138799, 7.777552968935449229 ) ) ;
#22333=CARTESIAN_POINT ( 'NONE',  ( -2.265401668238148591, 46.93990709177546705, 2.645701981445969686 ) ) ;
#22343=CARTESIAN_POINT ( 'NONE',  ( -1.113427685306987991, 38.22586258295232398, 25.34053733836490707 ) ) ;
#22349=ORIENTED_EDGE ( 'NONE', *, *, #17056, .F. ) ;
#22352=CARTESIAN_POINT ( 'NONE',  ( -20.38016308990357572, -1.509191766064412299, -29.73560196176845238 ) ) ;
#22357=CARTESIAN_POINT ( 'NONE',  ( -55.24271866751342941, 0.006671293903669565407, -0.006757859501006440936 ) ) ;
#22365=EDGE_CURVE ( 'NONE', #8723, #14914, #11844, .T. ) ;
#22375=FACE_OUTER_BOUND ( 'NONE', #26192, .T. ) ;
#22387=B_SPLINE_CURVE_WITH_KNOTS ( 'NONE', 3,
 ( #16132, #9663, #1303, #2902, #11679, #25076, #3182 ),
 .UNSPECIFIED., .F., .F.,
 ( 4, 3, 4 ),
 ( 1.062518129035794345E-17, 0.0007657099931970561164, 0.001530725384384652287 ),
 .UNSPECIFIED. ) ;
#22393=CARTESIAN_POINT ( 'NONE',  ( -20.20700224038492721, 24.51628800869048419, -16.58740185276719359 ) ) ;
#22402=CARTESIAN_POINT ( 'NONE',  ( -1.031422197589716205, 43.06660437151310816, -15.60268798220652187 ) ) ;
#22407=CARTESIAN_POINT ( 'NONE',  ( -23.77929240705206482, -35.93174012244168836, 4.877832571065307654 ) ) ;
#22411=CARTESIAN_POINT ( 'NONE',  ( -1.619063947482197729, 46.30105812165548684, 2.489035965910320503 ) ) ;
#22417=CARTESIAN_POINT ( 'NONE',  ( -21.41427618760446450, -30.75468365310881325, -1.815001260755733536 ) ) ;
#22441=CARTESIAN_POINT ( 'NONE',  ( -4.178947244162567465, -37.51424432987625579, 31.41809272265961539 ) ) ;
#22446=CARTESIAN_POINT ( 'NONE',  ( -1.323439229708149867, -16.42345129173367013, -43.04565903621277556 ) ) ;
#22454=VERTEX_POINT ( 'NONE', #23671 ) ;
#22461=ORIENTED_EDGE ( 'NONE', *, *, #6087, .F. ) ;
#22465=CARTESIAN_POINT ( 'NONE',  ( -24.53237795827024570, -33.25734978085267102, -6.738475012719991497 ) ) ;
#22468=CARTESIAN_POINT ( 'NONE',  ( -20.47566262905010603, 23.19796652405701565, 18.81547655725221091 ) ) ;
#22470=CARTESIAN_POINT ( 'NONE',  ( -20.47566262905009538, -25.06314747784824348, 16.24827521404678521 ) ) ;
#22476=ORIENTED_EDGE ( 'NONE', *, *, #7257, .F. ) ;
#22477=CARTESIAN_POINT ( 'NONE',  ( -9.156249394959713683, -38.89149400288378899, 38.17928057392034447 ) ) ;
#22481=B_SPLINE_CURVE_WITH_KNOTS ( 'NONE', 3,
 ( #8147, #23269, #3519, #25566, #19207, #12301, #1777, #17184 ),
 .UNSPECIFIED., .F., .F.,
 ( 4, 2, 2, 4 ),
 ( 0.000000000000000000, 0.002761524886576556103, 0.005523049773153112206, 0.01104609954630622441 ),
 .UNSPECIFIED. ) ;
#22483=CARTESIAN_POINT ( 'NONE',  ( -55.25719721206881729, -0.006045473558784178643, -0.009391134844729129294 ) ) ;
#22484=CARTESIAN_POINT ( 'NONE',  ( -1.044557008772706297, 44.03203053429572833, -12.57891310333364210 ) ) ;
#22485=CARTESIAN_POINT ( 'NONE',  ( -20.20700224038492010, -8.199606986804138131, 28.44216453106544762 ) ) ;
#22489=CARTESIAN_POINT ( 'NONE',  ( -24.53237795827028833, 3.868415699416160258, 33.71192251888858493 ) ) ;
#22509=CARTESIAN_POINT ( 'NONE',  ( -20.57838717382308147, -16.28767523336139078, -25.16001208503099917 ) ) ;
#22513=FACE_OUTER_BOUND ( 'NONE', #6814, .T. ) ;
#22516=CARTESIAN_POINT ( 'NONE',  ( -20.20612091757419648, 29.57813639663782013, 1.137293889216468790 ) ) ;
#22518=VERTEX_POINT ( 'NONE', #25181 ) ;
#22522=CARTESIAN_POINT ( 'NONE',  ( -20.24419206586950892, -23.20105925399712987, 18.44224248888897577 ) ) ;
#22526=VECTOR ( 'NONE', #27674, 1000.000000000000000 ) ;
#22545=CARTESIAN_POINT ( 'NONE',  ( -1.050230347699841582, 0.2550051351977194458, 45.79907861674081460 ) ) ;
#22547=CARTESIAN_POINT ( 'NONE',  ( -23.77929240705207192, -17.17389748746940370, 31.93650644494359270 ) ) ;
#22548=CARTESIAN_POINT ( 'NONE',  ( -1.619063947482194177, 29.22875152547808852, 35.99532424477347092 ) ) ;
#22552=CARTESIAN_POINT ( 'NONE',  ( -23.79223135445719706, 24.83942264280432610, 22.01133905265658441 ) ) ;
#22555=DIRECTION ( 'NONE',  ( -0.7637818620346800147, -0.6201872550346679835, -0.1788995134688763367 ) ) ;
#22563=CARTESIAN_POINT ( 'NONE',  ( -1.464342487929843450, 2.431462367721978435, 46.14921266389554688 ) ) ;
#22568=EDGE_CURVE ( 'NONE', #13087, #10554, #169, .T. ) ;
#22573=CARTESIAN_POINT ( 'NONE',  ( -20.47566338032535782, -10.72601609985042792, -27.87687989047296355 ) ) ;
#22583=ORIENTED_EDGE ( 'NONE', *, *, #8404, .T. ) ;
#22584=CARTESIAN_POINT ( 'NONE',  ( -1.045287976400362417, 37.92705037016796155, 25.66401692419947977 ) ) ;
#22591=CARTESIAN_POINT ( 'NONE',  ( -1.045287976400386842, -28.14015102489780062, 36.12803364096639314 ) ) ;
#22592=CARTESIAN_POINT ( 'NONE',  ( -12.82751273423883198, -35.32125660155422509, 33.78816682541326344 ) ) ;
#22593=CARTESIAN_POINT ( 'NONE',  ( -8.786685647604720373, -47.14957014837338534, -25.35688121747513435 ) ) ;
#22600=CARTESIAN_POINT ( 'NONE',  ( -25.21435515916025594, 1.749597353048488237E-16, -4.373993382621220594E-17 ) ) ;
#22604=CARTESIAN_POINT ( 'NONE',  ( -24.53239521893651087, 6.738460611583212412, 33.25736993155762633 ) ) ;
#22605=CARTESIAN_POINT ( 'NONE',  ( 14.74894986621300319, 4.541450660883840889E-15, -37.50000000000001421 ) ) ;
#22608=ORIENTED_EDGE ( 'NONE', *, *, #23105, .T. ) ;
#22611=CIRCLE ( 'NONE', #1456, 53.53553390275978785 ) ;
#22612=VECTOR ( 'NONE', #19346, 1000.000000000000114 ) ;
#22614=EDGE_CURVE ( 'NONE', #16496, #27145, #138, .T. ) ;
#22624=EDGE_LOOP ( 'NONE', ( #22674, #23815, #12182, #9310 ) ) ;
#22632=ORIENTED_EDGE ( 'NONE', *, *, #4443, .F. ) ;
#22633=CARTESIAN_POINT ( 'NONE',  ( -1.031422197589716205, 12.69107518035502835, -44.01264471863851924 ) ) ;
#22635=CARTESIAN_POINT ( 'NONE',  ( -25.21435515916025594, 1.749597353048488237E-16, -4.373993382621220594E-17 ) ) ;
#22642=EDGE_CURVE ( 'NONE', #26863, #11014, #26614, .T. ) ;
#22644=ORIENTED_EDGE ( 'NONE', *, *, #11695, .F. ) ;
#22649=CARTESIAN_POINT ( 'NONE',  ( -1.583189561560256253, -36.01941156322767057, 29.24830400313204493 ) ) ;
#22652=UNCERTAINTY_MEASURE_WITH_UNIT (LENGTH_MEASURE( 1.000000000000000082E-05 ), #24161, 'distance_accuracy_value', 'NONE');
#22657=CARTESIAN_POINT ( 'NONE',  ( -20.20700224038492721, -28.44216453106531617, 8.199606986804630182 ) ) ;
#22663=CARTESIAN_POINT ( 'NONE',  ( -1.044556982611280382, -25.56989963842174873, 37.98985389331836870 ) ) ;
#22664=LINE ( 'NONE', #20764, #6427 ) ;
#22666=CARTESIAN_POINT ( 'NONE',  ( -1.048996300304502194, -36.59642367107725391, 27.53442103413733122 ) ) ;
#22669=ORIENTED_EDGE ( 'NONE', *, *, #6536, .F. ) ;
#22671=VERTEX_POINT ( 'NONE', #27604 ) ;
#22672=CARTESIAN_POINT ( 'NONE',  ( -5.986830583229483693, -19.95149887249887399, -46.64941882410793283 ) ) ;
#22674=ORIENTED_EDGE ( 'NONE', *, *, #9336, .F. ) ;
#22684=CARTESIAN_POINT ( 'NONE',  ( -55.25719721206881729, -0.004044147484874425005, 0.01041086141212271658 ) ) ;
#22685=VECTOR ( 'NONE', #19198, 1000.000000000000000 ) ;
#22686=CARTESIAN_POINT ( 'NONE',  ( -1.048994561756786625, -13.42228657661154401, -43.78680886990936472 ) ) ;
#22690=CARTESIAN_POINT ( 'NONE',  ( -55.24300891470648622, 0.002702093572889911754, 0.009439835024157509913 ) ) ;
#22703=CARTESIAN_POINT ( 'NONE',  ( -22.23342874802668589, 24.24669006619402367, 20.31166691703097982 ) ) ;
#22709=ORIENTED_EDGE ( 'NONE', *, *, #11863, .F. ) ;
#22719=VERTEX_POINT ( 'NONE', #16534 ) ;
#22720=CARTESIAN_POINT ( 'NONE',  ( -23.79248802219730052, -30.42578156345377849, 13.25839849636389367 ) ) ;
#22727=CARTESIAN_POINT ( 'NONE',  ( -1.019300379054419725, -25.26451264419615939, 38.21680004809191189 ) ) ;
#22733=ORIENTED_EDGE ( 'NONE', *, *, #19949, .F. ) ;
#22734=ORIENTED_EDGE ( 'NONE', *, *, #24487, .T. ) ;
#22736=CARTESIAN_POINT ( 'NONE',  ( -1.048996300304502194, 37.49570739463922564, 26.29666317565261124 ) ) ;
#22737=CARTESIAN_POINT ( 'NONE',  ( -9.156249394959706578, -48.32878616080991208, 25.18996226954667605 ) ) ;
#22740=CARTESIAN_POINT ( 'NONE',  ( -8.786685647604706162, -38.68584556812290032, 37.00619870957955015 ) ) ;
#22756=CARTESIAN_POINT ( 'NONE',  ( -10.86508079875781085, 50.32133009257468359, -9.118642906269416315 ) ) ;
#22757=CARTESIAN_POINT ( 'NONE',  ( -55.25719721206881729, 0.008651607285661618019, -0.007063345920781386421 ) ) ;
#22762=DIRECTION ( 'NONE',  ( 0.000000000000000000, 5.223019709708233256E-21, -1.000000000000000000 ) ) ;
#22765=CARTESIAN_POINT ( 'NONE',  ( -23.77929240705205416, 15.74261278740719128, 32.66578242509729790 ) ) ;
#22774=CARTESIAN_POINT ( 'NONE',  ( -55.25297051322618813, 0.007247191603132027878, 0.01306918787467585205 ) ) ;
#22776=CARTESIAN_POINT ( 'NONE',  ( -24.53237795827031320, 33.25734978085278470, 6.738475012719742807 ) ) ;
#22777=CARTESIAN_POINT ( 'NONE',  ( -8.786685647604887350, 53.04920435127183254, 7.199674155859139724 ) ) ;
#22786=FACE_OUTER_BOUND ( 'NONE', #12063, .T. ) ;
#22790=CARTESIAN_POINT ( 'NONE',  ( -1.583189561560253589, -11.94859433442870866, 44.83405390829683057 ) ) ;
#22791=ORIENTED_EDGE ( 'NONE', *, *, #5462, .T. ) ;
#22792=ORIENTED_EDGE ( 'NONE', *, *, #10522, .T. ) ;
#22797=CARTESIAN_POINT ( 'NONE',  ( -10.86508079875774158, -50.67624451685647102, -6.877801422380581009 ) ) ;
#22799=CARTESIAN_POINT ( 'NONE',  ( -18.41936578851717599, 5.707900577128148356, -42.05131332928112187 ) ) ;
#22805=CARTESIAN_POINT ( 'NONE',  ( -20.20700224038492721, -28.44216453106531617, 8.199606986804630182 ) ) ;
#22812=CARTESIAN_POINT ( 'NONE',  ( -1.049819825607596124, -36.75053263699369666, 27.33096219556280815 ) ) ;
#22821=ORIENTED_EDGE ( 'NONE', *, *, #8677, .T. ) ;
#22824=B_SPLINE_CURVE_WITH_KNOTS ( 'NONE', 3,
 ( #9516, #22332, #7356, #20445, #22776, #24651 ),
 .UNSPECIFIED., .F., .F.,
 ( 4, 2, 4 ),
 ( 0.000000000000000000, 0.003570751334075638293, 0.007141502668151268780 ),
 .UNSPECIFIED. ) ;
#22835=CARTESIAN_POINT ( 'NONE',  ( -55.25297051322618813, 0.002853887643042873987, -0.01466904165775150676 ) ) ;
#22843=CARTESIAN_POINT ( 'NONE',  ( -20.57838717382308147, 7.715628353033680220, -28.96176188950220975 ) ) ;
#22847=CARTESIAN_POINT ( 'NONE',  ( -1.323830074806774837, -35.86387698262934265, -28.92190886481852274 ) ) ;
#22850=CARTESIAN_POINT ( 'NONE',  ( -1.058197053496162665, 45.77356582045591438, 1.754224732379708662 ) ) ;
#22852=ORIENTED_EDGE ( 'NONE', *, *, #15477, .F. ) ;
#22853=FACE_OUTER_BOUND ( 'NONE', #24367, .T. ) ;
#22858=ORIENTED_EDGE ( 'NONE', *, *, #25536, .T. ) ;
#22865=ADVANCED_FACE ( 'NONE', ( #17785 ), #1712, .F. ) ;
#22868=FACE_OUTER_BOUND ( 'NONE', #20683, .T. ) ;
#22871=ORIENTED_EDGE ( 'NONE', *, *, #9161, .F. ) ;
#22874=CARTESIAN_POINT ( 'NONE',  ( -20.57838717382308147, 29.92853265176831812, 1.611677988432465014 ) ) ;
#22880=CARTESIAN_POINT ( 'NONE',  ( -1.049817751779888786, 36.75003908324330837, 27.33161971822157810 ) ) ;
#22883=CARTESIAN_POINT ( 'NONE',  ( -23.79223135445718995, -7.157574570129374258, -32.40779366744832402 ) ) ;
#22886=CARTESIAN_POINT ( 'NONE',  ( -1.031422197589711987, -12.69107518035471394, 44.01264471863858319 ) ) ;
#22889=ORIENTED_EDGE ( 'NONE', *, *, #19086, .F. ) ;
#22896=CARTESIAN_POINT ( 'NONE',  ( -28.13707043255157103, -18.06394523322463641, -14.07296284901326189 ) ) ;
#22898=CARTESIAN_POINT ( 'NONE',  ( -23.79223135445719706, 7.157574570129600744, 32.40779366744824586 ) ) ;
#22910=EDGE_LOOP ( 'NONE', ( #24312, #19986, #24467, #23201 ) ) ;
#22918=CARTESIAN_POINT ( 'NONE',  ( -9.156249394959706578, -25.18996226954649131, -48.32878616081000445 ) ) ;
#22923=EDGE_LOOP ( 'NONE', ( #1004, #22476, #20341, #22733 ) ) ;
#22924=CARTESIAN_POINT ( 'NONE',  ( -1.619063947482201282, 44.80407745103784123, -11.94059994246174838 ) ) ;
#22925=CARTESIAN_POINT ( 'NONE',  ( -1.113548883309547266, -25.34012683631582519, -38.22628252420800976 ) ) ;
#22929=CARTESIAN_POINT ( 'NONE',  ( -4.780792508754313275, -42.16805077400938728, 25.98388465890126042 ) ) ;
#22932=CARTESIAN_POINT ( 'NONE',  ( -55.25719721206881729, 0.007063345920781645762, 0.008651607285661163521 ) ) ;
#22940=UNCERTAINTY_MEASURE_WITH_UNIT (LENGTH_MEASURE( 1.000000000000000082E-05 ), #12714, 'distance_accuracy_value', 'NONE');
#22943=EDGE_CURVE ( 'NONE', #11824, #15305, #3938, .T. ) ;
#22956=CARTESIAN_POINT ( 'NONE',  ( -25.21435515916043357, -34.29329011225959079, -4.655591116594231416 ) ) ;
#22959=EDGE_LOOP ( 'NONE', ( #12072, #14385, #15942, #20136 ) ) ;
#22965=VERTEX_POINT ( 'NONE', #2529 ) ;
#22968=B_SPLINE_CURVE_WITH_KNOTS ( 'NONE', 3,
 ( #19610, #22797, #7379, #18450, #18289, #27071, #9539 ),
 .UNSPECIFIED., .F., .F.,
 ( 4, 3, 4 ),
 ( 9.269414991073849107E-17, 0.009512539173626381045, 0.02506242213020854620 ),
 .UNSPECIFIED. ) ;
#22973=CARTESIAN_POINT ( 'NONE',  ( -55.24390624410018802, -0.01032895241566633357, -0.001451500391952961289 ) ) ;
#22976=CARTESIAN_POINT ( 'NONE',  ( -19.53423201713129842, 3.678323623448370869E-15, -28.92774122539760384 ) ) ;
#22979=FACE_OUTER_BOUND ( 'NONE', #14317, .T. ) ;
#22987=CARTESIAN_POINT ( 'NONE',  ( -20.20700224038492721, -24.51628800869035274, 16.58740185276737122 ) ) ;
#23010=DIRECTION ( 'NONE',  ( 1.000000000000000000, -6.938893903907226837E-18, 1.734723475976806709E-18 ) ) ;
#23011=DIRECTION ( 'NONE',  ( 0.000000000000000000, 5.223019709708233256E-21, -1.000000000000000000 ) ) ;
#23025=ORIENTED_EDGE ( 'NONE', *, *, #5353, .T. ) ;
#23032=CARTESIAN_POINT ( 'NONE',  ( -16.86833981943424021, -39.83928801320577406, 19.19877306373892978 ) ) ;
#23036=B_SPLINE_CURVE_WITH_KNOTS ( 'NONE', 3,
 ( #24176, #11064, #22294, #123, #21999, #13346, #4433, #11205, #19979, #15501, #264, #17806, #2554 ),
 .UNSPECIFIED., .F., .F.,
 ( 4, 3, 3, 3, 4 ),
 ( 9.813077866773594792E-18, 0.0007657099931970512375, 0.001531419946797918071, 0.002296279302920157302, 0.003061450627205767206 ),
 .UNSPECIFIED. ) ;
#23039=DIRECTION ( 'NONE',  ( 0.000000000000000000, 5.223019709708233256E-21, -1.000000000000000000 ) ) ;
#23040=CARTESIAN_POINT ( 'NONE',  ( -20.57838717382308147, -18.89542499756516847, -23.26537097894098594 ) ) ;
#23042=ORIENTED_EDGE ( 'NONE', *, *, #12184, .F. ) ;
#23046=CARTESIAN_POINT ( 'NONE',  ( -1.049817751779892117, -45.79652915392414769, -0.5106138415325238711 ) ) ;
#23054=CARTESIAN_POINT ( 'NONE',  ( -20.20700224038492721, 18.19058640100257662, 23.35150625415638714 ) ) ;
#23060=CARTESIAN_POINT ( 'NONE',  ( -25.21435515916043357, 31.17620025257608418, 15.02493970636113474 ) ) ;
#23061=CARTESIAN_POINT ( 'NONE',  ( -20.57838717382308147, -28.96176188950224528, -7.715628353033566533 ) ) ;
#23063=( BOUNDED_SURFACE ( )  B_SPLINE_SURFACE ( 3, 1, ( 
 ( #6561, #21815 ),
 ( #1940, #8440 ),
 ( #15456, #10746 ),
 ( #24265, #21666 ) ),
 .UNSPECIFIED., .F., .F., .F. ) 
 B_SPLINE_SURFACE_WITH_KNOTS ( ( 4, 4 ),
 ( 2, 2 ),
 ( 0.000000000000000000, 1.000000000000000000 ),
 ( 0.000000000000000000, 1.000000000000000000 ),
 .UNSPECIFIED. ) 
 GEOMETRIC_REPRESENTATION_ITEM ( )  RATIONAL_B_SPLINE_SURFACE ( (
 ( 1.000000000000000000, 1.000000000000000000),
 ( 0.9934239774497837239, 0.8357310067453919133),
 ( 0.9934239774497837239, 0.8357310067453919133),
 ( 1.000000000000000000, 1.000000000000000000) ) ) 
 REPRESENTATION_ITEM ( '' )  SURFACE ( )  );
#23077=ORIENTED_EDGE ( 'NONE', *, *, #24199, .F. ) ;
#23079=EDGE_CURVE ( 'NONE', #26786, #4240, #27425, .T. ) ;
#23082=ORIENTED_EDGE ( 'NONE', *, *, #8339, .F. ) ;
#23086=CARTESIAN_POINT ( 'NONE',  ( -1.031422197589711987, 45.78027046666443312, -1.530725436377622151 ) ) ;
#23088=CARTESIAN_POINT ( 'NONE',  ( -8.786685647604720373, -47.14957014837338534, -25.35688121747513435 ) ) ;
#23089=CARTESIAN_POINT ( 'NONE',  ( -7.711401346138401891, 6.030154970217631138, 52.11446537925907307 ) ) ;
#23090=CARTESIAN_POINT ( 'NONE',  ( -25.21435515916043713, 25.00736669481056751, 23.92354251275909505 ) ) ;
#23091=CARTESIAN_POINT ( 'NONE',  ( -21.41427618760457463, 16.60878262545457318, 25.94789270595488517 ) ) ;
#23100=CARTESIAN_POINT ( 'NONE',  ( -55.24198130335446422, 0.009170435128245573234, 0.001516807524708093389 ) ) ;
#23104=CARTESIAN_POINT ( 'NONE',  ( -1.259972190295308936, 25.19627397134298263, -38.49631882650656678 ) ) ;
#23105=EDGE_CURVE ( 'NONE', #23707, #6993, #3819, .T. ) ;
#23118=CARTESIAN_POINT ( 'NONE',  ( -1.539763995773680838, 29.16712963492463473, -35.94321074656906490 ) ) ;
#23123=CARTESIAN_POINT ( 'NONE',  ( -20.20700224038492721, -16.58740185276692358, 24.51628800869065827 ) ) ;
#23124=EDGE_CURVE ( 'NONE', #27239, #27540, #19351, .T. ) ;
#23125=ORIENTED_EDGE ( 'NONE', *, *, #27365, .F. ) ;
#23126=ORIENTED_EDGE ( 'NONE', *, *, #26808, .F. ) ;
#23140=CARTESIAN_POINT ( 'NONE',  ( -1.155001620486273861, 35.88346938217592452, 28.62773628245626867 ) ) ;
#23142=EDGE_LOOP ( 'NONE', ( #5172, #21913, #25920, #14893 ) ) ;
#23144=CARTESIAN_POINT ( 'NONE',  ( -28.41354790283022069, -21.64275480268742058, 8.345538364877306492 ) ) ;
#23145=ADVANCED_FACE ( 'NONE', ( #61 ), #14415, .F. ) ;
#23147=CIRCLE ( 'NONE', #19443, 53.53553390275978785 ) ;
#23148=CARTESIAN_POINT ( 'NONE',  ( -4.473127245936431073, -31.51789735524165081, 37.94261489385753094 ) ) ;
#23155=CONICAL_SURFACE ( 'NONE', #26794, 34.60786435723138510, 0.8559913436420825139 ) ;
#23160=ORIENTED_EDGE ( 'NONE', *, *, #7829, .T. ) ;
#23161=CARTESIAN_POINT ( 'NONE',  ( -55.25297051322618813, 0.006313402748432478395, 0.01354497706059498707 ) ) ;
#23166=B_SPLINE_CURVE_WITH_KNOTS ( 'NONE', 3,
 ( #20889, #9969, #7812, #16570, #25365, #5639 ),
 .UNSPECIFIED., .F., .F.,
 ( 4, 2, 4 ),
 ( 0.000000000000000000, 0.0004335151646191525506, 0.0008670303292383051011 ),
 .UNSPECIFIED. ) ;
#23169=LINE ( 'NONE', #19238, #10185 ) ;
#23191=CARTESIAN_POINT ( 'NONE',  ( -55.24198130335446422, -0.001391250620101175178, -0.009190321388310287998 ) ) ;
#23192=ORIENTED_EDGE ( 'NONE', *, *, #2468, .T. ) ;
#23195=CARTESIAN_POINT ( 'NONE',  ( -1.045287976400362417, -12.68782741917263657, 44.00138577190661948 ) ) ;
#23201=ORIENTED_EDGE ( 'NONE', *, *, #23852, .T. ) ;
#23204=CARTESIAN_POINT ( 'NONE',  ( -55.24390624410018802, 0.01032895241566708991, 0.001451500391952845713 ) ) ;
#23209=CARTESIAN_POINT ( 'NONE',  ( -1.539763995773683503, 2.469814354917492238, -46.22267697748602444 ) ) ;
#23213=CARTESIAN_POINT ( 'NONE',  ( -20.57838717382308147, 27.96569011373101077, 10.78122205916971055 ) ) ;
#23214=CARTESIAN_POINT ( 'NONE',  ( -1.045287976400379737, -25.66401692420040703, -37.92705037016734337 ) ) ;
#23220=CARTESIAN_POINT ( 'NONE',  ( -4.473127245936434626, -12.17046501147483895, 47.80062405537812964 ) ) ;
#23223=ORIENTED_EDGE ( 'NONE', *, *, #4093, .F. ) ;
#23225=CARTESIAN_POINT ( 'NONE',  ( -8.786685647604890903, 7.199674155858966529, -53.04920435127184675 ) ) ;
#23236=EDGE_CURVE ( 'NONE', #976, #7229, #22824, .T. ) ;
#23244=CARTESIAN_POINT ( 'NONE',  ( -1.619063947482197729, -25.20140673341345305, 38.92136151114934961 ) ) ;
#23251=ORIENTED_EDGE ( 'NONE', *, *, #12265, .T. ) ;
#23255=FACE_OUTER_BOUND ( 'NONE', #27754, .T. ) ;
#23258=( BOUNDED_SURFACE ( )  B_SPLINE_SURFACE ( 3, 1, ( 
 ( #6471, #27010 ),
 ( #11345, #9052 ),
 ( #24752, #265 ),
 ( #24613, #2556 ) ),
 .UNSPECIFIED., .F., .F., .F. ) 
 B_SPLINE_SURFACE_WITH_KNOTS ( ( 4, 4 ),
 ( 2, 2 ),
 ( 0.000000000000000000, 1.000000000000000000 ),
 ( 0.000000000000000000, 1.000000000000000000 ),
 .UNSPECIFIED. ) 
 GEOMETRIC_REPRESENTATION_ITEM ( )  RATIONAL_B_SPLINE_SURFACE ( (
 ( 1.000000000000000000, 1.000000000000000000),
 ( 0.9934239774497837239, 0.8357310067453919133),
 ( 0.9934239774497837239, 0.8357310067453919133),
 ( 1.000000000000000000, 1.000000000000000000) ) ) 
 REPRESENTATION_ITEM ( '' )  SURFACE ( )  );
#23263=CARTESIAN_POINT ( 'NONE',  ( -23.79223135445719706, -16.82181692922836547, -28.60983116549958538 ) ) ;
#23266=ORIENTED_EDGE ( 'NONE', *, *, #22267, .F. ) ;
#23269=CARTESIAN_POINT ( 'NONE',  ( -8.259864102781506290, -46.42816643551554989, -25.58601832199090609 ) ) ;
#23270=CARTESIAN_POINT ( 'NONE',  ( -28.41354790283022069, -5.969609727607868344, 22.41474081378006744 ) ) ;
#23271=CARTESIAN_POINT ( 'NONE',  ( -20.20700224038492365, -8.199606986804534259, -28.44216453106533748 ) ) ;
#23273=CARTESIAN_POINT ( 'NONE',  ( -20.57838717382308147, -16.28767523336102130, 25.16001208503123365 ) ) ;
#23287=CARTESIAN_POINT ( 'NONE',  ( -1.044556982611269058, -44.03203163107536966, -12.57890920527759171 ) ) ;
#23289=CARTESIAN_POINT ( 'NONE',  ( -55.25719721206881729, 0.01115102788683056123, 0.0006290797159205457727 ) ) ;
#23300=ORIENTED_EDGE ( 'NONE', *, *, #10680, .F. ) ;
#23303=CARTESIAN_POINT ( 'NONE',  ( -20.20997486282892552, 3.551351076220724598E-15, -29.60348406988233450 ) ) ;
#23309=( BOUNDED_SURFACE ( )  B_SPLINE_SURFACE ( 3, 1, ( 
 ( #4858, #20393 ),
 ( #16222, #22727 ),
 ( #5283, #7036 ),
 ( #15933, #9332 ) ),
 .UNSPECIFIED., .F., .F., .F. ) 
 B_SPLINE_SURFACE_WITH_KNOTS ( ( 4, 4 ),
 ( 2, 2 ),
 ( 0.000000000000000000, 1.000000000000000000 ),
 ( 0.000000000000000000, 1.000000000000000000 ),
 .UNSPECIFIED. ) 
 GEOMETRIC_REPRESENTATION_ITEM ( )  RATIONAL_B_SPLINE_SURFACE ( (
 ( 1.000000000000000000, 1.000000000000000000),
 ( 0.9934239774497838349, 0.8357310067453913582),
 ( 0.9934239774497838349, 0.8357310067453913582),
 ( 1.000000000000000000, 1.000000000000000000) ) ) 
 REPRESENTATION_ITEM ( '' )  SURFACE ( )  );
#23314=CARTESIAN_POINT ( 'NONE',  ( -1.046935749540012450, 15.35946454248395376, -43.14401153755472507 ) ) ;
#23315=DIRECTION ( 'NONE',  ( -0.7563875759206388771, 0.6531865459554675457, -0.03500244528123232224 ) ) ;
#23316=CARTESIAN_POINT ( 'NONE',  ( -21.41430102051751305, 19.54553566814620069, 23.81424706376344247 ) ) ;
#23318=B_SPLINE_CURVE_WITH_KNOTS ( 'NONE', 3,
 ( #21285, #3999, #27773, #14521, #15063, #12773, #25753, #5900, #23753, #25894 ),
 .UNSPECIFIED., .F., .F.,
 ( 4, 2, 2, 2, 4 ),
 ( 2.799429325053882983E-16, 0.0003346187017559026965, 0.0006692374035115254520, 0.001003856105267148099, 0.001338474807022770963 ),
 .UNSPECIFIED. ) ;
#23320=VERTEX_POINT ( 'NONE', #1295 ) ;
#23326=CARTESIAN_POINT ( 'NONE',  ( -20.20700224038492365, 10.08426345511628597, 27.82980252387807951 ) ) ;
#23327=EDGE_CURVE ( 'NONE', #14914, #10905, #5659, .T. ) ;
#23328=B_SPLINE_CURVE_WITH_KNOTS ( 'NONE', 3,
 ( #14477, #16501, #7892, #12320, #7602, #9899, #18520, #5861, #16804, #10187 ),
 .UNSPECIFIED., .F., .F.,
 ( 4, 2, 2, 2, 4 ),
 ( 2.845980932296679661E-16, 0.0003346187017559042144, 0.0006692374035115238257, 0.001003856105267143329, 0.001338474807022762940 ),
 .UNSPECIFIED. ) ;
#23337=B_SPLINE_CURVE_WITH_KNOTS ( 'NONE', 3,
 ( #16379, #16236, #7475, #18686, #3008, #11924, #27458 ),
 .UNSPECIFIED., .F., .F.,
 ( 4, 3, 4 ),
 ( 0.000000000000000000, 0.006568092053401751972, 0.02506242213020840742 ),
 .UNSPECIFIED. ) ;
#23339=CARTESIAN_POINT ( 'NONE',  ( -1.259920593601966177, -16.33409644610522449, 43.01175804832023886 ) ) ;
#23341=ORIENTED_EDGE ( 'NONE', *, *, #12479, .F. ) ;
#23342=ORIENTED_EDGE ( 'NONE', *, *, #11896, .F. ) ;
#23348=CARTESIAN_POINT ( 'NONE',  ( -4.473127245936434626, 41.70021447285091654, 26.34600523034491815 ) ) ;
#23355=CARTESIAN_POINT ( 'NONE',  ( -12.94347594948481195, 8.691477019903993906, 47.96504705787742040 ) ) ;
#23361=ORIENTED_EDGE ( 'NONE', *, *, #4999, .F. ) ;
#23366=CARTESIAN_POINT ( 'NONE',  ( -55.25297051322618813, -0.01466904165775103838, -0.002853887643042541354 ) ) ;
#23384=ORIENTED_EDGE ( 'NONE', *, *, #8553, .T. ) ;
#23389=ORIENTED_EDGE ( 'NONE', *, *, #27460, .F. ) ;
#23391=VERTEX_POINT ( 'NONE', #5628 ) ;
#23393=ADVANCED_FACE ( 'NONE', ( #19147 ), #7446, .F. ) ;
#23394=( BOUNDED_SURFACE ( )  B_SPLINE_SURFACE ( 3, 1, ( 
 ( #3786, #21044 ),
 ( #8123, #12556 ),
 ( #23100, #1200 ),
 ( #25246, #5514 ) ),
 .UNSPECIFIED., .F., .F., .F. ) 
 B_SPLINE_SURFACE_WITH_KNOTS ( ( 4, 4 ),
 ( 2, 2 ),
 ( 0.000000000000000000, 1.000000000000000000 ),
 ( 0.000000000000000000, 1.000000000000000000 ),
 .UNSPECIFIED. ) 
 GEOMETRIC_REPRESENTATION_ITEM ( )  RATIONAL_B_SPLINE_SURFACE ( (
 ( 1.000000000000000000, 1.000000000000000000),
 ( 0.9593753223639863714, 0.9995975284513187731),
 ( 0.9593753223639863714, 0.9995975284513187731),
 ( 1.000000000000000000, 1.000000000000000000) ) ) 
 REPRESENTATION_ITEM ( '' )  SURFACE ( )  );
#23405=CARTESIAN_POINT ( 'NONE',  ( -25.21435515916025594, 1.749597353048488237E-16, -4.373993382621220594E-17 ) ) ;
#23410=CARTESIAN_POINT ( 'NONE',  ( -4.473127245936434626, -3.196405119334147837, -49.22197550883366546 ) ) ;
#23414=ORIENTED_EDGE ( 'NONE', *, *, #423, .F. ) ;
#23418=VERTEX_POINT ( 'NONE', #4305 ) ;
#23419=EDGE_CURVE ( 'NONE', #27426, #15681, #5947, .T. ) ;
#23425=CARTESIAN_POINT ( 'NONE',  ( -12.82751273423881777, 43.04932478553568842, 23.15139349681263070 ) ) ;
#23427=CARTESIAN_POINT ( 'NONE',  ( -20.20700224038492721, -29.58392382092674211, -0.9908225410477480288 ) ) ;
#23430=CARTESIAN_POINT ( 'NONE',  ( -1.583189561560252701, 44.83405390829673109, -11.94859433442916874 ) ) ;
#23435=ORIENTED_EDGE ( 'NONE', *, *, #15590, .T. ) ;
#23437=CARTESIAN_POINT ( 'NONE',  ( -55.24271866751342941, -0.006671293903667674559, -0.006757859501010194010 ) ) ;
#23441=CARTESIAN_POINT ( 'NONE',  ( -1.019300379054419725, -44.15350047934408195, -12.21833869579447729 ) ) ;
#23444=CARTESIAN_POINT ( 'NONE',  ( -1.155001620486248992, 12.20337535396741124, 44.25209926692296136 ) ) ;
#23445=CARTESIAN_POINT ( 'NONE',  ( -8.786685647604896232, -7.199674155858612146, 53.04920435127190359 ) ) ;
#23452=CARTESIAN_POINT ( 'NONE',  ( -7.078251931573400491, 38.93060825814280435, 34.59014398252872269 ) ) ;
#23468=CARTESIAN_POINT ( 'NONE',  ( -1.049819825607573254, -13.66706894614408618, 43.71263398674766876 ) ) ;
#23472=CARTESIAN_POINT ( 'NONE',  ( -25.21435515916043713, 15.02493970636190745, 31.17620025257570759 ) ) ;
#23483=CARTESIAN_POINT ( 'NONE',  ( -1.044557008772713402, 43.01636061109007159, 15.70482370518772086 ) ) ;
#23488=CARTESIAN_POINT ( 'NONE',  ( -1.048172774974297949, -37.64158596421231096, -26.08722459372772562 ) ) ;
#23494=ORIENTED_EDGE ( 'NONE', *, *, #19775, .T. ) ;
#23497=CARTESIAN_POINT ( 'NONE',  ( -1.050230347360791017, 0.0004630652117437840452, -45.79907861464602092 ) ) ;
#23499=EDGE_CURVE ( 'NONE', #1086, #12213, #1147, .T. ) ;
#23505=CARTESIAN_POINT ( 'NONE',  ( -4.473127245936431073, -18.25038884639838699, 45.82513704981563052 ) ) ;
#23519=ADVANCED_FACE ( 'NONE', ( #10796 ), #23258, .F. ) ;
#23527=VECTOR ( 'NONE', #26410, 1000.000000000000000 ) ;
#23537=CARTESIAN_POINT ( 'NONE',  ( -22.34422965417124018, -26.20925041532873223, -27.39717383755272451 ) ) ;
#23538=AXIS2_PLACEMENT_3D ( 'NONE', #4441, #17956, #15815 ) ;
#23539=CARTESIAN_POINT ( 'NONE',  ( -20.24419206586954090, 27.76448493191444200, -10.37009329716774708 ) ) ;
#23544=( BOUNDED_SURFACE ( )  B_SPLINE_SURFACE ( 3, 1, ( 
 ( #22056, #26652 ),
 ( #2179, #466 ),
 ( #26231, #10989 ),
 ( #9256, #11549 ) ),
 .UNSPECIFIED., .F., .F., .F. ) 
 B_SPLINE_SURFACE_WITH_KNOTS ( ( 4, 4 ),
 ( 2, 2 ),
 ( 0.000000000000000000, 1.000000000000000000 ),
 ( 0.000000000000000000, 1.000000000000000000 ),
 .UNSPECIFIED. ) 
 GEOMETRIC_REPRESENTATION_ITEM ( )  RATIONAL_B_SPLINE_SURFACE ( (
 ( 1.000000000000000000, 1.000000000000000000),
 ( 0.7789835883360578528, 0.9689951854195403280),
 ( 0.7789835883360578528, 0.9689951854195403280),
 ( 1.000000000000000000, 1.000000000000000000) ) ) 
 REPRESENTATION_ITEM ( '' )  SURFACE ( )  );
#23548=PLANE ( 'NONE',  #5044 ) ;
#23549=EDGE_CURVE ( 'NONE', #457, #12820, #9702, .T. ) ;
#23567=EDGE_LOOP ( 'NONE', ( #1123, #15271, #19934, #3407 ) ) ;
#23576=CARTESIAN_POINT ( 'NONE',  ( -1.583189561560252701, 29.24830400313166123, -36.01941156322796900 ) ) ;
#23580=B_SPLINE_CURVE_WITH_KNOTS ( 'NONE', 3,
 ( #21653, #2062, #8284, #8852, #10731, #1924, #23838, #10451 ),
 .UNSPECIFIED., .F., .F.,
 ( 4, 2, 2, 4 ),
 ( 0.000000000000000000, 0.002761524886576656283, 0.005523049773153312567, 0.01104609954630661126 ),
 .UNSPECIFIED. ) ;
#23583=CARTESIAN_POINT ( 'NONE',  ( -1.045287976400365970, -43.05558670614224326, 15.59869763335140469 ) ) ;
#23589=ORIENTED_EDGE ( 'NONE', *, *, #10514, .T. ) ;
#23593=ADVANCED_FACE ( 'NONE', ( #9480 ), #21384, .F. ) ;
#23595=CARTESIAN_POINT ( 'NONE',  ( -1.619063947482201282, -11.94059994246191359, -44.80407745103779860 ) ) ;
#23597=CARTESIAN_POINT ( 'NONE',  ( -25.21435515916043713, -25.00736669481004526, 23.92354251275963861 ) ) ;
#23608=DIRECTION ( 'NONE',  ( -0.7563875759206388771, -0.6104009704506927481, 0.2351350468682887607 ) ) ;
#23614=AXIS2_PLACEMENT_3D ( 'NONE', #12104, #10096, #18863 ) ;
#23615=CARTESIAN_POINT ( 'NONE',  ( -20.24399999263415140, -7.930419334766389383, -28.55700515887716762 ) ) ;
#23618=CARTESIAN_POINT ( 'NONE',  ( -20.20700224038492010, 18.19058640100223556, -23.35150625415664649 ) ) ;
#23619=B_SPLINE_CURVE_WITH_KNOTS ( 'NONE', 3,
 ( #346, #13587, #2208, #26122, #9137, #26681 ),
 .UNSPECIFIED., .F., .F.,
 ( 4, 2, 4 ),
 ( 1.528920360908313465E-16, 0.003570751334075640462, 0.007141502668151127400 ),
 .UNSPECIFIED. ) ;
#23620=CARTESIAN_POINT ( 'NONE',  ( -28.41354790283022069, 23.16239616762931064, 1.249099604787156981 ) ) ;
#23622=B_SPLINE_CURVE_WITH_KNOTS ( 'NONE', 3,
 ( #14501, #5743, #22883, #21112, #25311, #12069 ),
 .UNSPECIFIED., .F., .F.,
 ( 4, 2, 4 ),
 ( 3.467809420226820728E-16, 0.003576372551511154425, 0.007152745103021954098 ),
 .UNSPECIFIED. ) ;
#23623=CARTESIAN_POINT ( 'NONE',  ( -1.323830074806765289, -28.92190886481839129, 35.86387698262947055 ) ) ;
#23631=CARTESIAN_POINT ( 'NONE',  ( -20.24399999263414784, 1.282322917263463813, -29.60996018918694617 ) ) ;
#23637=CARTESIAN_POINT ( 'NONE',  ( -1.048996300304493978, 26.29666317565303046, -37.49570739463894142 ) ) ;
#23645=DIRECTION ( 'NONE',  ( 0.7563875759206388771, -0.6531865459554681008, -0.03500244528122332249 ) ) ;
#23647=CARTESIAN_POINT ( 'NONE',  ( -8.786685647604890903, 37.00619870957935120, -38.68584556812312059 ) ) ;
#23650=ORIENTED_EDGE ( 'NONE', *, *, #4879, .T. ) ;
#23652=( BOUNDED_SURFACE ( )  B_SPLINE_SURFACE ( 3, 1, ( 
 ( #25571, #18650 ),
 ( #5990, #5849 ),
 ( #3111, #20655 ),
 ( #26397, #24115 ) ),
 .UNSPECIFIED., .F., .F., .F. ) 
 B_SPLINE_SURFACE_WITH_KNOTS ( ( 4, 4 ),
 ( 2, 2 ),
 ( 0.000000000000000000, 1.000000000000000000 ),
 ( 0.000000000000000000, 1.000000000000000000 ),
 .UNSPECIFIED. ) 
 GEOMETRIC_REPRESENTATION_ITEM ( )  RATIONAL_B_SPLINE_SURFACE ( (
 ( 1.000000000000000000, 1.000000000000000000),
 ( 0.9934239774497838349, 0.8357310067453913582),
 ( 0.9934239774497838349, 0.8357310067453913582),
 ( 1.000000000000000000, 1.000000000000000000) ) ) 
 REPRESENTATION_ITEM ( '' )  SURFACE ( )  );
#23665=EDGE_CURVE ( 'NONE', #6278, #1423, #21739, .T. ) ;
#23668=CARTESIAN_POINT ( 'NONE',  ( -55.24300891470648622, -0.0003472257464243277253, 0.009812809446890398413 ) ) ;
#23671=CARTESIAN_POINT ( 'NONE',  ( -1.619063947482197729, 29.22875152547757338, -35.99532424477389725 ) ) ;
#23680=VERTEX_POINT ( 'NONE', #5437 ) ;
#23685=B_SPLINE_CURVE_WITH_KNOTS ( 'NONE', 3,
 ( #21595, #8372, #10264, #15240, #1866, #17135, #12530, #6080 ),
 .UNSPECIFIED., .F., .F.,
 ( 4, 2, 2, 4 ),
 ( 2.189053321159284187E-16, 0.002761568181852863766, 0.005523136363705508090, 0.01104627272741077852 ),
 .UNSPECIFIED. ) ;
#23688=CARTESIAN_POINT ( 'NONE',  ( -28.41354790283022069, 5.969609727608021998, -22.41474081378002836 ) ) ;
#23692=B_SPLINE_CURVE_WITH_KNOTS ( 'NONE', 3,
 ( #24460, #19836, #10795, #11344, #6334, #15640, #10928, #21725, #24043, #17255, #4726, #28459, #1995 ),
 .UNSPECIFIED., .F., .F.,
 ( 4, 3, 3, 3, 4 ),
 ( 1.250926888277100303E-17, 0.0007657099931970524301, 0.001531419946797917637, 0.002296279302920158170, 0.003061450627205759400 ),
 .UNSPECIFIED. ) ;
#23706=CARTESIAN_POINT ( 'NONE',  ( -55.24390624410018802, -0.001811362924362171613, 0.01027195578988007209 ) ) ;
#23707=VERTEX_POINT ( 'NONE', #16819 ) ;
#23709=B_SPLINE_CURVE_WITH_KNOTS ( 'NONE', 3,
 ( #17117, #21154, #19146, #25913, #1441, #8212, #10512 ),
 .UNSPECIFIED., .F., .F.,
 ( 4, 3, 4 ),
 ( 0.000000000000000000, 0.006568092053401790135, 0.02506242213020847681 ),
 .UNSPECIFIED. ) ;
#23714=ORIENTED_EDGE ( 'NONE', *, *, #23665, .F. ) ;
#23729=CARTESIAN_POINT ( 'NONE',  ( -55.24300891470650754, -0.007734635432136225362, 0.006048736206179294861 ) ) ;
#23735=CARTESIAN_POINT ( 'NONE',  ( -8.259864102781673267, -52.60025989855198247, 6.590267880897466846 ) ) ;
#23736=CARTESIAN_POINT ( 'NONE',  ( -1.619063947482197729, 25.20140673341430571, 38.92136151114879539 ) ) ;
#23740=VERTEX_POINT ( 'NONE', #7763 ) ;
#23742=ORIENTED_EDGE ( 'NONE', *, *, #1208, .T. ) ;
#23753=CARTESIAN_POINT ( 'NONE',  ( -1.539763995773674177, 38.84665165401067810, -25.17088606276561080 ) ) ;
#23760=CARTESIAN_POINT ( 'NONE',  ( -25.21435515916025594, 1.749597353048488237E-16, -4.373993382621220594E-17 ) ) ;
#23768=ORIENTED_EDGE ( 'NONE', *, *, #9070, .T. ) ;
#23772=B_SPLINE_CURVE_WITH_KNOTS ( 'NONE', 3,
 ( #21495, #1909, #19478, #2047, #28379, #319, #11404, #11269, #20036, #2475, #26513, #15713, #9255 ),
 .UNSPECIFIED., .F., .F.,
 ( 4, 3, 3, 3, 4 ),
 ( 1.040834085586084257E-17, 0.0007657099931970558996, 0.001531419946797916336, 0.002296279302920154267, 0.003061450627205756364 ),
 .UNSPECIFIED. ) ;
#23781=CARTESIAN_POINT ( 'NONE',  ( -1.031422197589711764, -45.78027046666444733, -1.530725436377303073 ) ) ;
#23785=ORIENTED_EDGE ( 'NONE', *, *, #1632, .T. ) ;
#23794=EDGE_CURVE ( 'NONE', #27510, #27064, #17930, .T. ) ;
#23795=CARTESIAN_POINT ( 'NONE',  ( -55.24728320129491266, -0.01402509393918105647, -0.003868537197316873795 ) ) ;
#23805=CARTESIAN_POINT ( 'NONE',  ( -1.323830074806776391, -44.47857376182260936, 12.01461446423248169 ) ) ;
#23810=ORIENTED_EDGE ( 'NONE', *, *, #6443, .F. ) ;
#23811=CARTESIAN_POINT ( 'NONE',  ( -25.21435515916025594, 1.749597353048488237E-16, -4.373993382621220594E-17 ) ) ;
#23815=ORIENTED_EDGE ( 'NONE', *, *, #10307, .F. ) ;
#23817=EDGE_CURVE ( 'NONE', #7509, #17315, #16215, .T. ) ;
#23821=CARTESIAN_POINT ( 'NONE',  ( 14.74894986621300319, 4.490279961725991446E-15, -37.50000000000001421 ) ) ;
#23825=CARTESIAN_POINT ( 'NONE',  ( -1.583189561560255143, 44.83405390829672399, -11.94859433442917762 ) ) ;
#23829=ORIENTED_EDGE ( 'NONE', *, *, #4608, .T. ) ;
#23834=CARTESIAN_POINT ( 'NONE',  ( -55.24390624410018802, 0.001811362924362862900, -0.01027195578988028025 ) ) ;
#23838=CARTESIAN_POINT ( 'NONE',  ( -2.911734481061404534, -30.23325065583388138, -36.84482841982639911 ) ) ;
#23846=CARTESIAN_POINT ( 'NONE',  ( -20.20700224038492010, -10.08426345511570332, 27.82980252387829623 ) ) ;
#23852=EDGE_CURVE ( 'NONE', #5490, #16899, #13014, .T. ) ;
#23857=CARTESIAN_POINT ( 'NONE',  ( -55.24198130335446422, 0.004163123460806185221, -0.008310594958150844397 ) ) ;
#23862=CARTESIAN_POINT ( 'NONE',  ( -1.019300379054419725, 12.21833869579464604, -44.15350047934403221 ) ) ;
#23864=CARTESIAN_POINT ( 'NONE',  ( -1.323439229708139875, 46.01398008004444762, -2.317790194799894010 ) ) ;
#23866=ORIENTED_EDGE ( 'NONE', *, *, #16505, .F. ) ;
#23870=CARTESIAN_POINT ( 'NONE',  ( -12.94347594948482438, 42.93165645342861581, -23.08810053288705078 ) ) ;
#23874=CARTESIAN_POINT ( 'NONE',  ( -20.57838717382308147, -25.16001208503093522, 16.28767523336148315 ) ) ;
#23880=EDGE_CURVE ( 'NONE', #5961, #11177, #6652, .T. ) ;
#23883=EDGE_CURVE ( 'NONE', #18593, #7658, #13455, .T. ) ;
#23893=CARTESIAN_POINT ( 'NONE',  ( -1.259972190295316485, -45.95417440459613090, 2.243354636026243742 ) ) ;
#23899=CARTESIAN_POINT ( 'NONE',  ( -25.21435515916043713, 34.05351380035342146, 6.169479169075106739 ) ) ;
#23905=CARTESIAN_POINT ( 'NONE',  ( -6.574463467970653952, 38.37705091668375701, -34.08059230520056104 ) ) ;
#23906=CARTESIAN_POINT ( 'NONE',  ( -12.94347594948487057, -47.96504705787739198, 8.691477019903814494 ) ) ;
#23907=CARTESIAN_POINT ( 'NONE',  ( -1.031422197589711764, -25.67058493451469303, -37.93675465142463565 ) ) ;
#23909=CARTESIAN_POINT ( 'NONE',  ( -1.050231094221210082, 26.71409683968617799, -37.20185272688468814 ) ) ;
#23912=CARTESIAN_POINT ( 'NONE',  ( -55.24300891470648622, 0.008142823778062486390, -0.005486913146696510354 ) ) ;
#23920=ORIENTED_EDGE ( 'NONE', *, *, #11695, .T. ) ;
#23927=VECTOR ( 'NONE', #1566, 1000.000000000000000 ) ;
#23940=EDGE_CURVE ( 'NONE', #13567, #17941, #21555, .T. ) ;
#23942=ORIENTED_EDGE ( 'NONE', *, *, #2568, .F. ) ;
#23943=ORIENTED_EDGE ( 'NONE', *, *, #27194, .T. ) ;
#23945=VECTOR ( 'NONE', #28057, 999.9999999999998863 ) ;
#23950=VECTOR ( 'NONE', #21981, 999.9999999999998863 ) ;
#23952=B_SPLINE_CURVE_WITH_KNOTS ( 'NONE', 3,
 ( #18340, #7431, #25005, #5257, #20650, #1643, #28119 ),
 .UNSPECIFIED., .F., .F.,
 ( 4, 3, 4 ),
 ( 5.463690523629807176E-17, 0.009512539173626407066, 0.02506242213020838661 ),
 .UNSPECIFIED. ) ;
#23954=CARTESIAN_POINT ( 'NONE',  ( -20.20700224038492721, 28.44216453106548315, 8.199606986804035103 ) ) ;
#23959=CARTESIAN_POINT ( 'NONE',  ( -25.21435515916025594, 34.29329011225976132, 4.655591116594488099 ) ) ;
#23961=CARTESIAN_POINT ( 'NONE',  ( -1.619063947482194177, 35.99532424477422410, 29.22875152547716482 ) ) ;
#23965=CARTESIAN_POINT ( 'NONE',  ( -1.048996300304505747, 27.53442103413745912, 36.59642367107714023 ) ) ;
#23983=EDGE_LOOP ( 'NONE', ( #2064, #2947, #11061, #27808 ) ) ;
#23984=CARTESIAN_POINT ( 'NONE',  ( -28.13707043255157103, 14.07296284901332761, -18.06394523322457957 ) ) ;
#23987=VECTOR ( 'NONE', #19964, 1000.000000000000114 ) ;
#24000=CARTESIAN_POINT ( 'NONE',  ( -1.539760825549688628, -2.469813586483410539, -46.22267384399379608 ) ) ;
#24005=CARTESIAN_POINT ( 'NONE',  ( -1.323830074806759960, 25.17121255494532406, 38.58891736138504314 ) ) ;
#24006=CARTESIAN_POINT ( 'NONE',  ( -25.21435515916043002, 30.48034229288640162, -16.39063784838753790 ) ) ;
#24024=B_SPLINE_CURVE_WITH_KNOTS ( 'NONE', 3,
 ( #16625, #16328, #7719, #27408, #3379, #3236, #25416, #5691, #23118, #14453 ),
 .UNSPECIFIED., .F., .F.,
 ( 4, 2, 2, 2, 4 ),
 ( 2.976962515321448001E-16, 0.0003346187017559152190, 0.0006692374035115327162, 0.001003856105267150267, 0.001338474807022767710 ),
 .UNSPECIFIED. ) ;
#24034=EDGE_CURVE ( 'NONE', #12261, #8723, #1319, .T. ) ;
#24037=CARTESIAN_POINT ( 'NONE',  ( -28.13707043255157103, -21.52861750560944998, -7.802116958608919184 ) ) ;
#24042=EDGE_LOOP ( 'NONE', ( #1625, #14535, #12831, #20859 ) ) ;
#24043=CARTESIAN_POINT ( 'NONE',  ( -1.049817751779876129, -43.71287583013717182, 13.66628317065032583 ) ) ;
#24045=CARTESIAN_POINT ( 'NONE',  ( -4.780792508754314163, -32.07473752860752825, 37.74278713234433269 ) ) ;
#24049=CARTESIAN_POINT ( 'NONE',  ( -1.046935749539993799, 27.93995161054695231, -36.28605774377773230 ) ) ;
#24052=CARTESIAN_POINT ( 'NONE',  ( -55.24390624410018802, 0.007245494385991918876, 0.007503127514281743120 ) ) ;
#24053=DIRECTION ( 'NONE',  ( -0.7637818620346801257, 0.6451161201712179993, -0.02150485345385064542 ) ) ;
#24055=CIRCLE ( 'NONE', #14843, 34.60786435723138510 ) ;
#24057=CONICAL_SURFACE ( 'NONE', #19432, 34.60786435723138510, 0.8559913436420825139 ) ;
#24058=AXIS2_PLACEMENT_3D ( 'NONE', #13152, #15023, #8285 ) ;
#24061=ORIENTED_EDGE ( 'NONE', *, *, #16432, .F. ) ;
#24068=ORIENTED_EDGE ( 'NONE', *, *, #25078, .T. ) ;
#24074=FACE_OUTER_BOUND ( 'NONE', #25957, .T. ) ;
#24075=ADVANCED_FACE ( 'NONE', ( #7956 ), #7631, .F. ) ;
#24076=ADVANCED_BREP_SHAPE_REPRESENTATION ( '', ( #7750, #27263 ), #6137 ) ;
#24081=CARTESIAN_POINT ( 'NONE',  ( -4.473127245936434626, 26.34600523034538355, -41.70021447285062521 ) ) ;
#24082=CARTESIAN_POINT ( 'NONE',  ( -1.031422197589716205, -25.67058493451469658, -37.93675465142464276 ) ) ;
#24083=ORIENTED_EDGE ( 'NONE', *, *, #12738, .T. ) ;
#24089=ORIENTED_EDGE ( 'NONE', *, *, #16432, .T. ) ;
#24097=CIRCLE ( 'NONE', #16749, 34.60786435723138510 ) ;
#24098=DIRECTION ( 'NONE',  ( 1.000000000000000000, -6.938893903907226837E-18, 1.734723475976806709E-18 ) ) ;
#24101=CARTESIAN_POINT ( 'NONE',  ( -25.21435515916043357, 16.39063784838743132, -30.48034229288645136 ) ) ;
#24102=CARTESIAN_POINT ( 'NONE',  ( -55.24728320129491266, -0.003868537197316542463, 0.01402509393918130107 ) ) ;
#24105=ORIENTED_EDGE ( 'NONE', *, *, #1883, .T. ) ;
#24107=CARTESIAN_POINT ( 'NONE',  ( -1.583189561560255143, 2.490696082059864924, -46.33203782964461936 ) ) ;
#24115=CARTESIAN_POINT ( 'NONE',  ( -1.583189561560256253, 2.490696082060512406, 46.33203782964458384 ) ) ;
#24142=CARTESIAN_POINT ( 'NONE',  ( -8.259864102781671491, -47.98931516265581365, 22.52209142944983711 ) ) ;
#24147=CARTESIAN_POINT ( 'NONE',  ( -55.24340739397742084, 0.007744344507855094144, 0.006539691034612383526 ) ) ;
#24158=CARTESIAN_POINT ( 'NONE',  ( -21.81686047589426636, -5.181745222995193245, 38.17230180719262478 ) ) ;
#24161=( LENGTH_UNIT ( ) NAMED_UNIT ( * ) SI_UNIT ( .MILLI., .METRE. ) );
#24172=ORIENTED_EDGE ( 'NONE', *, *, #25964, .F. ) ;
#24173=( BOUNDED_SURFACE ( )  B_SPLINE_SURFACE ( 3, 1, ( 
 ( #23289, #16362 ),
 ( #18667, #16656 ),
 ( #18955, #9903 ),
 ( #25297, #23576 ) ),
 .UNSPECIFIED., .F., .F., .F. ) 
 B_SPLINE_SURFACE_WITH_KNOTS ( ( 4, 4 ),
 ( 2, 2 ),
 ( 0.000000000000000000, 1.000000000000000000 ),
 ( 0.000000000000000000, 1.000000000000000000 ),
 .UNSPECIFIED. ) 
 GEOMETRIC_REPRESENTATION_ITEM ( )  RATIONAL_B_SPLINE_SURFACE ( (
 ( 1.000000000000000000, 1.000000000000000000),
 ( 0.7789835883360578528, 0.9689951854195403280),
 ( 0.7789835883360578528, 0.9689951854195403280),
 ( 1.000000000000000000, 1.000000000000000000) ) ) 
 REPRESENTATION_ITEM ( '' )  SURFACE ( )  );
#24176=CARTESIAN_POINT ( 'NONE',  ( -1.045287976400362417, -28.14015102489855735, -36.12803364096578207 ) ) ;
#24177=CARTESIAN_POINT ( 'NONE',  ( -20.47566262905010603, 1.586617686065558974, -29.82700878811084522 ) ) ;
#24191=ORIENTED_EDGE ( 'NONE', *, *, #1050, .T. ) ;
#24197=ORIENTED_EDGE ( 'NONE', *, *, #26677, .T. ) ;
#24199=EDGE_CURVE ( 'NONE', #3264, #25953, #1968, .T. ) ;
#24204=CARTESIAN_POINT ( 'NONE',  ( -25.21435515916043713, -30.48034229288627017, 16.39063784838775462 ) ) ;
#24211=CARTESIAN_POINT ( 'NONE',  ( -55.24271866751342941, 0.006757859501006707216, 0.006671293903669109175 ) ) ;
#24213=CARTESIAN_POINT ( 'NONE',  ( -55.24340739397742794, 0.0007387096945709508214, 0.01010924026184075245 ) ) ;
#24214=CARTESIAN_POINT ( 'NONE',  ( -10.86508079875781618, -36.95527278096552237, -35.35100740321762913 ) ) ;
#24215=CARTESIAN_POINT ( 'NONE',  ( -20.24419206586952313, -7.929973069813210707, 28.55732805495823712 ) ) ;
#24229=EDGE_CURVE ( 'NONE', #20163, #864, #13504, .T. ) ;
#24241=CARTESIAN_POINT ( 'NONE',  ( -1.048171036023497260, 37.64178826568608116, -26.08692787913882327 ) ) ;
#24254=ORIENTED_EDGE ( 'NONE', *, *, #17212, .F. ) ;
#24264=ORIENTED_EDGE ( 'NONE', *, *, #12479, .T. ) ;
#24265=CARTESIAN_POINT ( 'NONE',  ( -55.24271866751342941, -0.009369360294294061531, 0.001545935011626861600 ) ) ;
#24273=VERTEX_POINT ( 'NONE', #13785 ) ;
#24278=B_SPLINE_CURVE_WITH_KNOTS ( 'NONE', 3,
 ( #16201, #25010, #22850, #9022, #5263, #7016, #14038, #11179, #24581, #22411 ),
 .UNSPECIFIED., .F., .F.,
 ( 4, 2, 2, 2, 4 ),
 ( 2.884421207865724908E-16, 0.0003346187017559065996, 0.0006692374035115252352, 0.001003856105267143979, 0.001338474807022762723 ),
 .UNSPECIFIED. ) ;
#24288=EDGE_CURVE ( 'NONE', #15681, #12261, #11484, .T. ) ;
#24292=CARTESIAN_POINT ( 'NONE',  ( -20.57838717382308147, -29.92853265176830746, 1.611677988432673070 ) ) ;
#24299=DIRECTION ( 'NONE',  ( -1.000000000000000000, 6.938893903907226837E-18, -1.734723475976806709E-18 ) ) ;
#24309=CARTESIAN_POINT ( 'NONE',  ( -4.178947244162628749, 18.28784278438515543, 45.38689110596700260 ) ) ;
#24312=ORIENTED_EDGE ( 'NONE', *, *, #11460, .F. ) ;
#24317=CARTESIAN_POINT ( 'NONE',  ( -20.37983603106074426, -10.62371319148622284, 27.81368274044722000 ) ) ;
#24324=CARTESIAN_POINT ( 'NONE',  ( -8.786685647604890903, -9.545808661480235102, 52.67761315067295413 ) ) ;
#24334=ORIENTED_EDGE ( 'NONE', *, *, #20228, .T. ) ;
#24335=B_SPLINE_CURVE_WITH_KNOTS ( 'NONE', 3,
 ( #6301, #27755, #19245, #6175, #21270, #16948 ),
 .UNSPECIFIED., .F., .F.,
 ( 4, 2, 4 ),
 ( 3.208066105977133993E-16, 0.003576372551511132307, 0.007152745103021943690 ),
 .UNSPECIFIED. ) ;
#24350=CARTESIAN_POINT ( 'NONE',  ( -1.031422197589716205, 44.01264471863865424, 12.69107518035457005 ) ) ;
#24351=CARTESIAN_POINT ( 'NONE',  ( -55.24198130335446422, 0.004276389980776598189, 0.008252882783650057619 ) ) ;
#24354=CARTESIAN_POINT ( 'NONE',  ( -55.24390624410018802, 0.007245494385991800047, -0.007503127514277958821 ) ) ;
#24355=CARTESIAN_POINT ( 'NONE',  ( -25.21435515916043357, -25.00736669481038987, -23.92354251275926558 ) ) ;
#24363=ORIENTED_EDGE ( 'NONE', *, *, #15590, .F. ) ;
#24367=EDGE_LOOP ( 'NONE', ( #8848, #338, #20388, #18241 ) ) ;
#24372=CARTESIAN_POINT ( 'NONE',  ( -55.24340739397742794, 0.005344433640974572026, -0.008612749836242874699 ) ) ;
#24379=CARTESIAN_POINT ( 'NONE',  ( -2.265401668238147259, 43.82493763960408728, 17.02144111536834004 ) ) ;
#24390=DIRECTION ( 'NONE',  ( -0.7563875759206388771, 0.5078650950445624535, -0.4122509917856805317 ) ) ;
#24395=ORIENTED_EDGE ( 'NONE', *, *, #15192, .F. ) ;
#24397=CARTESIAN_POINT ( 'NONE',  ( -20.20700224038492721, -23.35150625415645820, 18.19058640100249491 ) ) ;
#24408=CARTESIAN_POINT ( 'NONE',  ( -1.048172774974290622, -15.11899685083854727, -43.23017713506519755 ) ) ;
#24410=LINE ( 'NONE', #4827, #11538 ) ;
#24412=EDGE_CURVE ( 'NONE', #5523, #20564, #15370, .T. ) ;
#24414=CARTESIAN_POINT ( 'NONE',  ( -7.078251931573400491, -47.71415099571819951, -20.86696228105206075 ) ) ;
#24416=CARTESIAN_POINT ( 'NONE',  ( -55.24271866751342941, -0.004256484107795216812, 0.008488649505342837909 ) ) ;
#24418=EDGE_CURVE ( 'NONE', #6949, #24273, #20525, .T. ) ;
#24421=CARTESIAN_POINT ( 'NONE',  ( -55.24271866751342941, 0.004256484107795918508, -0.008488649505343059953 ) ) ;
#24423=CARTESIAN_POINT ( 'NONE',  ( -20.57838717382308147, -18.89542499756516847, -23.26537097894098594 ) ) ;
#24424=B_SPLINE_CURVE_WITH_KNOTS ( 'NONE', 3,
 ( #13862, #18471, #20340, #7126, #24692, #5515, #3361, #11714 ),
 .UNSPECIFIED., .F., .F.,
 ( 4, 2, 2, 4 ),
 ( 2.225109362706117716E-16, 0.002761568181852862899, 0.005523136363705503753, 0.01104627272741078546 ),
 .UNSPECIFIED. ) ;
#24426=B_SPLINE_CURVE_WITH_KNOTS ( 'NONE', 3,
 ( #10937, #11073, #17540, #131, #9489, #25046 ),
 .UNSPECIFIED., .F., .F.,
 ( 4, 2, 4 ),
 ( 1.504716382203053018E-16, 0.003570751334075636125, 0.007141502668151121329 ),
 .UNSPECIFIED. ) ;
#24434=VERTEX_POINT ( 'NONE', #23445 ) ;
#24436=CARTESIAN_POINT ( 'NONE',  ( -20.57838717382308502, 23.26537097894105699, -18.89542499756508320 ) ) ;
#24447=CARTESIAN_POINT ( 'NONE',  ( -25.21435515916043357, -15.02493970636125198, 31.17620025257602379 ) ) ;
#24450=EDGE_LOOP ( 'NONE', ( #17151, #21208, #5625, #289 ) ) ;
#24452=CARTESIAN_POINT ( 'NONE',  ( -7.078251931573406708, -44.92740138729184451, -26.33626633876207634 ) ) ;
#24457=ORIENTED_EDGE ( 'NONE', *, *, #18152, .F. ) ;
#24458=VERTEX_POINT ( 'NONE', #19248 ) ;
#24460=CARTESIAN_POINT ( 'NONE',  ( -1.045287976400365970, -43.05558670614224326, 15.59869763335140469 ) ) ;
#24462=FACE_OUTER_BOUND ( 'NONE', #25086, .T. ) ;
#24465=CARTESIAN_POINT ( 'NONE',  ( -6.588769196390767746, -51.10255870850473769, -4.956336548259470121 ) ) ;
#24467=ORIENTED_EDGE ( 'NONE', *, *, #15550, .T. ) ;
#24471=( BOUNDED_SURFACE ( )  B_SPLINE_SURFACE ( 3, 1, ( 
 ( #18533, #20678 ),
 ( #23161, #12057 ),
 ( #25301, #10047 ),
 ( #14631, #23430 ) ),
 .UNSPECIFIED., .F., .F., .F. ) 
 B_SPLINE_SURFACE_WITH_KNOTS ( ( 4, 4 ),
 ( 2, 2 ),
 ( 0.000000000000000000, 1.000000000000000000 ),
 ( 0.000000000000000000, 1.000000000000000000 ),
 .UNSPECIFIED. ) 
 GEOMETRIC_REPRESENTATION_ITEM ( )  RATIONAL_B_SPLINE_SURFACE ( (
 ( 1.000000000000000000, 1.000000000000000000),
 ( 0.7789835883360578528, 0.9689951854195403280),
 ( 0.7789835883360578528, 0.9689951854195403280),
 ( 1.000000000000000000, 1.000000000000000000) ) ) 
 REPRESENTATION_ITEM ( '' )  SURFACE ( )  );
#24475=CARTESIAN_POINT ( 'NONE',  ( -20.47566338032518019, 29.82700953060488303, -1.586617869343990739 ) ) ;
#24478=AXIS2_PLACEMENT_3D ( 'NONE', #10343, #9908, #23011 ) ;
#24487=EDGE_CURVE ( 'NONE', #24434, #7787, #16249, .T. ) ;
#24492=ORIENTED_EDGE ( 'NONE', *, *, #10168, .T. ) ;
#24497=CARTESIAN_POINT ( 'NONE',  ( -5.986830583229489022, -4.559539818181495896, -50.53158596890440180 ) ) ;
#24502=CARTESIAN_POINT ( 'NONE',  ( -55.25297051322618813, -0.01093108995495129139, -0.01019003092403723831 ) ) ;
#24504=CARTESIAN_POINT ( 'NONE',  ( -23.77929240705206837, -32.66578242509734054, 15.74261278740706338 ) ) ;
#24505=DIRECTION ( 'NONE',  ( 0.000000000000000000, 5.223019709708233256E-21, -1.000000000000000000 ) ) ;
#24507=CARTESIAN_POINT ( 'NONE',  ( -25.21435515916043713, 4.655591116594827383, 34.29329011225949841 ) ) ;
#24509=ORIENTED_EDGE ( 'NONE', *, *, #24288, .T. ) ;
#24510=CARTESIAN_POINT ( 'NONE',  ( -20.21097721712958517, -9.464413111084555297, 28.05863618200118381 ) ) ;
#24517=CARTESIAN_POINT ( 'NONE',  ( -1.045287976400365970, 45.76855895860943235, -1.530335034934267258 ) ) ;
#24523=FACE_OUTER_BOUND ( 'NONE', #24873, .T. ) ;
#24528=CARTESIAN_POINT ( 'NONE',  ( -55.24300891470648622, 0.006048736206180948920, -0.007734635432132875611 ) ) ;
#24530=EDGE_CURVE ( 'NONE', #23418, #11824, #25659, .T. ) ;
#24531=FACE_OUTER_BOUND ( 'NONE', #23983, .T. ) ;
#24538=CARTESIAN_POINT ( 'NONE',  ( -55.24340739397742794, -0.009842732675348539115, -0.002421372372456522849 ) ) ;
#24539=VERTEX_POINT ( 'NONE', #9120 ) ;
#24543=CARTESIAN_POINT ( 'NONE',  ( -1.046935749539994465, -37.78548154587976882, 25.87617179820957602 ) ) ;
#24544=CARTESIAN_POINT ( 'NONE',  ( -20.20700224038492721, 29.58392382092673500, 0.9908225410479544193 ) ) ;
#24551=CARTESIAN_POINT ( 'NONE',  ( -20.38016308990357217, -23.16952666206571365, 18.69911008768360361 ) ) ;
#24553=VECTOR ( 'NONE', #11813, 1000.000000000000114 ) ;
#24554=ORIENTED_EDGE ( 'NONE', *, *, #18959, .F. ) ;
#24556=ORIENTED_EDGE ( 'NONE', *, *, #11967, .F. ) ;
#24559=B_SPLINE_CURVE_WITH_KNOTS ( 'NONE', 3,
 ( #4400, #22259, #19793, #20080, #87, #26696 ),
 .UNSPECIFIED., .F., .F.,
 ( 4, 2, 4 ),
 ( 0.000000000000000000, 0.003570751334075647834, 0.007141502668151295669 ),
 .UNSPECIFIED. ) ;
#24560=ADVANCED_FACE ( 'NONE', ( #16164 ), #17877, .T. ) ;
#24561=CARTESIAN_POINT ( 'NONE',  ( -55.24390624410018802, -0.009209468562452135382, -0.004896917417131697002 ) ) ;
#24569=DIRECTION ( 'NONE',  ( 0.000000000000000000, -5.223019709708116647E-21, 1.000000000000000000 ) ) ;
#24576=CARTESIAN_POINT ( 'NONE',  ( -2.904412668506660467, 11.97478724945576545, 46.12477647685262383 ) ) ;
#24577=CARTESIAN_POINT ( 'NONE',  ( -1.049819825607597235, -26.50610175068240792, 37.34982882986871999 ) ) ;
#24578=CARTESIAN_POINT ( 'NONE',  ( -22.23226125620943705, -20.31044300692189708, -24.24619897613468211 ) ) ;
#24581=CARTESIAN_POINT ( 'NONE',  ( -1.539763995773691940, 46.22267697748604576, 2.469814354917652999 ) ) ;
#24582=CARTESIAN_POINT ( 'NONE',  ( -1.044557008772710516, -37.98985164565307571, 25.56990300677022177 ) ) ;
#24589=CARTESIAN_POINT ( 'NONE',  ( -1.045287976400365970, -36.12803364096568259, 28.14015102489869591 ) ) ;
#24590=EDGE_CURVE ( 'NONE', #20894, #25218, #11561, .T. ) ;
#24598=DIRECTION ( 'NONE',  ( 0.000000000000000000, 0.000000000000000000, 1.000000000000000000 ) ) ;
#24599=CARTESIAN_POINT ( 'NONE',  ( -20.57838717382308147, -18.89542499756482741, 23.26537097894125594 ) ) ;
#24602=LINE ( 'NONE', #27406, #14945 ) ;
#24612=FACE_OUTER_BOUND ( 'NONE', #27345, .T. ) ;
#24613=CARTESIAN_POINT ( 'NONE',  ( -55.24271866751342941, -0.008433070970613520956, 0.004365563123935277227 ) ) ;
#24616=CARTESIAN_POINT ( 'NONE',  ( -20.90916690077944295, 39.20864005633548999, -5.322316104228152156 ) ) ;
#24622=CARTESIAN_POINT ( 'NONE',  ( -6.574463467970653952, -11.01561683920017387, 50.12924290857549181 ) ) ;
#24624=FACE_OUTER_BOUND ( 'NONE', #5482, .T. ) ;
#24635=ORIENTED_EDGE ( 'NONE', *, *, #7530, .F. ) ;
#24640=CARTESIAN_POINT ( 'NONE',  ( -23.79248802219722592, -32.40806545715335574, -7.157555990716774730 ) ) ;
#24648=CARTESIAN_POINT ( 'NONE',  ( -22.23342874802667879, 31.55488258420089664, 2.180636882146622657 ) ) ;
#24651=CARTESIAN_POINT ( 'NONE',  ( -25.21435515916043713, 34.05351380035342146, 6.169479169075106739 ) ) ;
#24652=CARTESIAN_POINT ( 'NONE',  ( -12.94347594948480484, 43.91326021875542551, 21.16159467081307710 ) ) ;
#24656=CARTESIAN_POINT ( 'NONE',  ( -20.20612092514784308, -8.058517256680906016, 28.48192215759674184 ) ) ;
#24660=CARTESIAN_POINT ( 'NONE',  ( -22.34422965417127216, -5.100074259622869199, -37.57019010019544680 ) ) ;
#24665=ORIENTED_EDGE ( 'NONE', *, *, #13679, .F. ) ;
#24669=EDGE_CURVE ( 'NONE', #6550, #15305, #18615, .T. ) ;
#24670=VERTEX_POINT ( 'NONE', #22956 ) ;
#24676=CARTESIAN_POINT ( 'NONE',  ( -1.583189561560256253, 46.33203782964461936, -2.490696082060027017 ) ) ;
#24692=CARTESIAN_POINT ( 'NONE',  ( -4.780792508754325709, -11.68149851467495637, -48.13366140756553335 ) ) ;
#24698=DIRECTION ( 'NONE',  ( 0.000000000000000000, 5.223019709708233256E-21, -1.000000000000000000 ) ) ;
#24703=ORIENTED_EDGE ( 'NONE', *, *, #2413, .T. ) ;
#24706=B_SPLINE_CURVE_WITH_KNOTS ( 'NONE', 3,
 ( #17330, #21658, #19502, #2205, #26119, #12356 ),
 .UNSPECIFIED., .F., .F.,
 ( 4, 2, 4 ),
 ( 4.114075111014854645E-16, 0.003576372551511222079, 0.007152745103022032161 ),
 .UNSPECIFIED. ) ;
#24710=CARTESIAN_POINT ( 'NONE',  ( -55.24271866751342941, -0.008488649505345847654, 0.004256484107793125603 ) ) ;
#24711=CARTESIAN_POINT ( 'NONE',  ( -8.786685647604889127, 9.545808661480615243, -52.67761315067287597 ) ) ;
#24724=CARTESIAN_POINT ( 'NONE',  ( -21.41427618760447160, -29.81030852927061758, 7.777551129310369404 ) ) ;
#24726=LINE ( 'NONE', #7157, #6496 ) ;
#24730=VERTEX_POINT ( 'NONE', #18569 ) ;
#24732=EDGE_CURVE ( 'NONE', #22719, #654, #6411, .T. ) ;
#24735=CARTESIAN_POINT ( 'NONE',  ( -1.239374126674604337, 35.79060836339814955, -28.97829083655452820 ) ) ;
#24739=EDGE_LOOP ( 'NONE', ( #7484, #19853, #6696, #18621 ) ) ;
#24749=EDGE_LOOP ( 'NONE', ( #22461, #22709, #22852, #21509 ) ) ;
#24752=CARTESIAN_POINT ( 'NONE',  ( -55.24300891470648622, -0.008142823778061756071, 0.005486913146696262289 ) ) ;
#24754=CARTESIAN_POINT ( 'NONE',  ( -25.21435515916042647, 15.02493970636146692, -31.17620025257592786 ) ) ;
#24758=VERTEX_POINT ( 'NONE', #13526 ) ;
#24764=DIRECTION ( 'NONE',  ( -1.000000000000000000, 6.938893903907227607E-18, -1.734723475976806902E-18 ) ) ;
#24770=CARTESIAN_POINT ( 'NONE',  ( -8.786685647604885574, 6.096987947571466530E-17, -1.524246986892866633E-17 ) ) ;
#24777=VECTOR ( 'NONE', #17985, 1000.000000000000114 ) ;
#24778=CARTESIAN_POINT ( 'NONE',  ( -8.786685647604896232, 23.24040270374459993, 48.22796981442743913 ) ) ;
#24788=CARTESIAN_POINT ( 'NONE',  ( -2.904412668506668460, 47.56768199507434502, 2.864640348250799828 ) ) ;
#24795=EDGE_CURVE ( 'NONE', #5592, #17694, #28365, .T. ) ;
#24803=EDGE_CURVE ( 'NONE', #27648, #12565, #20435, .T. ) ;
#24823=CARTESIAN_POINT ( 'NONE',  ( -20.20700224038492721, -24.51628800869059432, -16.58740185276701951 ) ) ;
#24824=FACE_OUTER_BOUND ( 'NONE', #21814, .T. ) ;
#24831=CARTESIAN_POINT ( 'NONE',  ( -1.019300379054419947, 35.83762006677442002, 28.53917295602858673 ) ) ;
#24833=ORIENTED_EDGE ( 'NONE', *, *, #8265, .F. ) ;
#24841=CARTESIAN_POINT ( 'NONE',  ( -1.619063947482201282, 11.94059994246159384, -44.80407745103787676 ) ) ;
#24849=CARTESIAN_POINT ( 'NONE',  ( -1.031422197589716205, 44.01264471863849082, -12.69107518035517046 ) ) ;
#24853=CARTESIAN_POINT ( 'NONE',  ( -25.21435515916043713, -34.29329011225952684, 4.655591116594705703 ) ) ;
#24859=EDGE_LOOP ( 'NONE', ( #4375, #8014, #15412, #4459 ) ) ;
#24863=VECTOR ( 'NONE', #20299, 1000.000000000000114 ) ;
#24871=B_SPLINE_CURVE_WITH_KNOTS ( 'NONE', 3,
 ( #21424, #14803, #28307, #19541, #25896, #24158, #1700 ),
 .UNSPECIFIED., .F., .F.,
 ( 4, 3, 4 ),
 ( 1.114146325429624918E-17, 0.009512539173626377575, 0.02506242213020845946 ),
 .UNSPECIFIED. ) ;
#24873=EDGE_LOOP ( 'NONE', ( #9099, #3023, #11478, #21618 ) ) ;
#24874=( NAMED_UNIT ( * ) SI_UNIT ( $, .STERADIAN. ) SOLID_ANGLE_UNIT ( ) );
#24876=EDGE_CURVE ( 'NONE', #23391, #9533, #16735, .T. ) ;
#24878=DIRECTION ( 'NONE',  ( 0.000000000000000000, 5.223019709707975211E-21, -1.000000000000000000 ) ) ;
#24879=CARTESIAN_POINT ( 'NONE',  ( -22.23226125620929139, -2.179935373562669643, -31.55376588768476509 ) ) ;
#24880=B_SPLINE_CURVE_WITH_KNOTS ( 'NONE', 3,
 ( #26002, #24000, #7005, #2964, #3100, #3241, #506, #15761, #11737, #26840 ),
 .UNSPECIFIED., .F., .F.,
 ( 4, 2, 2, 2, 4 ),
 ( 1.563658610346375379E-18, 0.0003346267210630954943, 0.0006692534421261893624, 0.001003880163189283230, 0.001338506884252377207 ),
 .UNSPECIFIED. ) ;
#24891=CARTESIAN_POINT ( 'NONE',  ( -19.53423201713129842, 1.353948732986041533E-16, 28.92774122539760384 ) ) ;
#24897=CARTESIAN_POINT ( 'NONE',  ( -25.21435515916025594, 1.749597353048488237E-16, -4.373993382621220594E-17 ) ) ;
#24901=DIRECTION ( 'NONE',  ( 1.000000000000000000, -6.938893903907226837E-18, -5.541455922705464902E-20 ) ) ;
#24903=CARTESIAN_POINT ( 'NONE',  ( -25.21435515916043002, 34.05351380035335040, -6.169479169075572145 ) ) ;
#24905=LINE ( 'NONE', #22896, #2930 ) ;
#24909=ORIENTED_EDGE ( 'NONE', *, *, #8433, .T. ) ;
#24912=AXIS2_PLACEMENT_3D ( 'NONE', #24770, #25332, #23039 ) ;
#24923=ORIENTED_EDGE ( 'NONE', *, *, #6771, .F. ) ;
#24926=CARTESIAN_POINT ( 'NONE',  ( -6.574463467970651287, -5.014313797967385966, -51.07975593197902953 ) ) ;
#24931=CARTESIAN_POINT ( 'NONE',  ( -1.056502255334264895, 13.66916755949850604, -43.72121397317227576 ) ) ;
#24933=B_SPLINE_CURVE_WITH_KNOTS ( 'NONE', 3,
 ( #11373, #19722, #26621, #8948, #26483, #7614 ),
 .UNSPECIFIED., .F., .F.,
 ( 4, 2, 4 ),
 ( 0.000000000000000000, 0.0004335151646191504364, 0.0008670303292383008727 ),
 .UNSPECIFIED. ) ;
#24937=ORIENTED_EDGE ( 'NONE', *, *, #4879, .F. ) ;
#24938=AXIS2_PLACEMENT_3D ( 'NONE', #7830, #896, #3203 ) ;
#24943=B_SPLINE_CURVE_WITH_KNOTS ( 'NONE', 3,
 ( #723, #9513, #27042, #7352, #28185, #4152, #14948, #5916, #16851, #25909 ),
 .UNSPECIFIED., .F., .F.,
 ( 4, 2, 2, 2, 4 ),
 ( 2.884421207865725401E-16, 0.0003346187017559067080, 0.0006692374035115243678, 0.001003856105267142028, 0.001338474807022759687 ),
 .UNSPECIFIED. ) ;
#24947=B_SPLINE_CURVE_WITH_KNOTS ( 'NONE', 3,
 ( #10994, #8982, #19907, #2631, #9115, #4497, #8686, #4651 ),
 .UNSPECIFIED., .F., .F.,
 ( 4, 2, 2, 4 ),
 ( 2.251264292202123005E-16, 0.002761568181852872006, 0.005523136363705519365, 0.01104627272741081322 ),
 .UNSPECIFIED. ) ;
#24948=EDGE_CURVE ( 'NONE', #4790, #22518, #898, .T. ) ;
#24949=CARTESIAN_POINT ( 'NONE',  ( -1.056502255334265339, -43.40574022158784118, -14.64009593116085739 ) ) ;
#24950=ADVANCED_FACE ( 'NONE', ( #14939 ), #23155, .T. ) ;
#24955=CARTESIAN_POINT ( 'NONE',  ( -10.86508079875801691, 6.877801422380844798, -50.67624451685624365 ) ) ;
#24960=CARTESIAN_POINT ( 'NONE',  ( -10.86508079875781263, 9.118642906269942117, 50.32133009257457701 ) ) ;
#24993=CARTESIAN_POINT ( 'NONE',  ( -1.239374126674604337, 16.50008610789298302, -42.99367564261284258 ) ) ;
#24997=CARTESIAN_POINT ( 'NONE',  ( -1.050230347699842692, 1.897926697972695375E-16, 45.79907861674080749 ) ) ;
#25001=CARTESIAN_POINT ( 'NONE',  ( -28.41354790283022069, -8.345538364876929904, 21.64275480268756269 ) ) ;
#25002=VECTOR ( 'NONE', #16269, 999.9999999999998863 ) ;
#25005=CARTESIAN_POINT ( 'NONE',  ( -12.94347594948484392, -8.691477019903656398, -47.96504705787742040 ) ) ;
#25007=CARTESIAN_POINT ( 'NONE',  ( -25.21435515916043713, 25.00736669481056751, 23.92354251275909505 ) ) ;
#25010=CARTESIAN_POINT ( 'NONE',  ( -1.044557008772710072, 45.76404748504490527, 1.643388457098048372 ) ) ;
#25011=CARTESIAN_POINT ( 'NONE',  ( -1.113548883309548376, -38.22628252420791739, 25.34012683631596374 ) ) ;
#25022=VERTEX_POINT ( 'NONE', #5139 ) ;
#25026=CARTESIAN_POINT ( 'NONE',  ( -20.38016308990359349, -10.62413300761005353, -27.81387210821418776 ) ) ;
#25027=CARTESIAN_POINT ( 'NONE',  ( -20.21097721712959938, -17.13687106192361398, -24.14932359587282917 ) ) ;
#25029=CARTESIAN_POINT ( 'NONE',  ( -55.25719721206881729, 0.01079965405819919254, 0.002847566758682530588 ) ) ;
#25032=CARTESIAN_POINT ( 'NONE',  ( -20.20700224038492721, 0.9908225410478516126, -29.58392382092673145 ) ) ;
#25034=ORIENTED_EDGE ( 'NONE', *, *, #9941, .F. ) ;
#25036=ORIENTED_EDGE ( 'NONE', *, *, #26328, .T. ) ;
#25046=CARTESIAN_POINT ( 'NONE',  ( -25.21435515916043713, 30.48034229288662544, 16.39063784838709736 ) ) ;
#25059=CARTESIAN_POINT ( 'NONE',  ( -4.162674018437130030, -18.33413805792406492, 45.34593312138898824 ) ) ;
#25063=CARTESIAN_POINT ( 'NONE',  ( -20.37983603106073716, 23.16947629293390065, 18.69865230096500852 ) ) ;
#25064=CARTESIAN_POINT ( 'NONE',  ( -1.619063947482197729, -25.20140673341401438, -38.92136151114898723 ) ) ;
#25073=( BOUNDED_SURFACE ( )  B_SPLINE_SURFACE ( 3, 1, ( 
 ( #3855, #21117 ),
 ( #10061, #19385 ),
 ( #10355, #8460 ),
 ( #3985, #27595 ) ),
 .UNSPECIFIED., .F., .F., .F. ) 
 B_SPLINE_SURFACE_WITH_KNOTS ( ( 4, 4 ),
 ( 2, 2 ),
 ( 0.000000000000000000, 1.000000000000000000 ),
 ( 0.000000000000000000, 1.000000000000000000 ),
 .UNSPECIFIED. ) 
 GEOMETRIC_REPRESENTATION_ITEM ( )  RATIONAL_B_SPLINE_SURFACE ( (
 ( 1.000000000000000000, 1.000000000000000000),
 ( 0.9934239774497838349, 0.8357310067453913582),
 ( 0.9934239774497838349, 0.8357310067453913582),
 ( 1.000000000000000000, 1.000000000000000000) ) ) 
 REPRESENTATION_ITEM ( '' )  SURFACE ( )  );
#25076=CARTESIAN_POINT ( 'NONE',  ( -1.050230347699842248, -0.2550051351976088121, -45.79907861674080749 ) ) ;
#25077=CARTESIAN_POINT ( 'NONE',  ( -1.619063947482197729, -25.20140673341401438, -38.92136151114898723 ) ) ;
#25078=EDGE_CURVE ( 'NONE', #22323, #15612, #19402, .T. ) ;
#25081=DIRECTION ( 'NONE',  ( 1.000000000000000000, -6.938893903907226837E-18, 1.734723475976806709E-18 ) ) ;
#25086=EDGE_LOOP ( 'NONE', ( #18068, #12593, #13407, #7733 ) ) ;
#25097=CARTESIAN_POINT ( 'NONE',  ( -20.57838717382308502, 25.16001208503106668, -16.28767523336130196 ) ) ;
#25107=ORIENTED_EDGE ( 'NONE', *, *, #8167, .F. ) ;
#25115=EDGE_LOOP ( 'NONE', ( #6956, #25768, #27193, #23125 ) ) ;
#25116=EDGE_LOOP ( 'NONE', ( #16436, #23300, #28341, #14837 ) ) ;
#25125=CARTESIAN_POINT ( 'NONE',  ( -20.21097721650786738, 17.67178726257392896, 23.76068422213738529 ) ) ;
#25129=ORIENTED_EDGE ( 'NONE', *, *, #24288, .F. ) ;
#25137=ORIENTED_EDGE ( 'NONE', *, *, #12265, .F. ) ;
#25139=CARTESIAN_POINT ( 'NONE',  ( -1.323830074806772394, 35.86387698262958423, 28.92190886481825274 ) ) ;
#25159=ADVANCED_FACE ( 'NONE', ( #7897 ), #24173, .F. ) ;
#25165=VERTEX_POINT ( 'NONE', #27440 ) ;
#25167=CARTESIAN_POINT ( 'NONE',  ( -7.078251931573406708, -50.86685171665420313, -11.16394717458656949 ) ) ;
#25174=CARTESIAN_POINT ( 'NONE',  ( -20.24419206586952313, -18.44224248888889051, -23.20105925399719382 ) ) ;
#25181=CARTESIAN_POINT ( 'NONE',  ( -1.045287976400365970, -45.76855895860942525, 1.530335034934587002 ) ) ;
#25183=ORIENTED_EDGE ( 'NONE', *, *, #5496, .T. ) ;
#25188=ORIENTED_EDGE ( 'NONE', *, *, #17337, .F. ) ;
#25189=CARTESIAN_POINT ( 'NONE',  ( -1.048171036023513025, 45.78635789057865679, 1.020520027229292470 ) ) ;
#25190=CARTESIAN_POINT ( 'NONE',  ( -1.046936909428682450, -43.93225665392624535, -12.93351869073256388 ) ) ;
#25198=CARTESIAN_POINT ( 'NONE',  ( -28.13707043255157103, 18.96624908365864925, 12.83104814250432923 ) ) ;
#25199=ORIENTED_EDGE ( 'NONE', *, *, #25638, .F. ) ;
#25207=CARTESIAN_POINT ( 'NONE',  ( -1.619063947482197729, 2.489035965910159298, -46.30105812165548684 ) ) ;
#25210=DIRECTION ( 'NONE',  ( -0.7563875759206388771, -0.2351350468682952832, -0.6104009704506900835 ) ) ;
#25218=VERTEX_POINT ( 'NONE', #8169 ) ;
#25221=CIRCLE ( 'NONE', #27018, 34.60786435723138510 ) ;
#25225=EDGE_CURVE ( 'NONE', #25959, #6949, #1245, .T. ) ;
#25233=EDGE_CURVE ( 'NONE', #12213, #25254, #25944, .T. ) ;
#25239=CARTESIAN_POINT ( 'NONE',  ( -25.21435515916043002, 31.17620025257588523, -15.02493970636157705 ) ) ;
#25240=CARTESIAN_POINT ( 'NONE',  ( -25.21435515916043713, 16.39063784838786475, 30.48034229288620622 ) ) ;
#25245=CARTESIAN_POINT ( 'NONE',  ( -28.13707043255157103, -7.802116958609158992, -21.52861750560936471 ) ) ;
#25246=CARTESIAN_POINT ( 'NONE',  ( -55.24271866751342941, 0.008433070970614320663, 0.004365563123939306990 ) ) ;
#25253=DIRECTION ( 'NONE',  ( 0.000000000000000000, 5.223019709708116647E-21, -1.000000000000000000 ) ) ;
#25254=VERTEX_POINT ( 'NONE', #15320 ) ;
#25267=CARTESIAN_POINT ( 'NONE',  ( -55.24340739397742794, 0.003826481709800397344, 0.009386184976285138343 ) ) ;
#25272=ORIENTED_EDGE ( 'NONE', *, *, #12188, .T. ) ;
#25275=CARTESIAN_POINT ( 'NONE',  ( -24.53237795827023859, 6.738475012720130941, -33.25734978085264260 ) ) ;
#25278=CARTESIAN_POINT ( 'NONE',  ( -1.113548883309550153, -35.91246368318222437, -28.52482525634933097 ) ) ;
#25281=CARTESIAN_POINT ( 'NONE',  ( -8.786685647604887350, 53.04920435127183254, 7.199674155859139724 ) ) ;
#25283=ORIENTED_EDGE ( 'NONE', *, *, #17705, .T. ) ;
#25290=CARTESIAN_POINT ( 'NONE',  ( -20.20700224038492010, 18.19058640100223556, -23.35150625415664649 ) ) ;
#25295=CARTESIAN_POINT ( 'NONE',  ( -1.113427685306998649, -44.18561238466747199, -12.28784199929917875 ) ) ;
#25297=CARTESIAN_POINT ( 'NONE',  ( -55.24390624410018802, 0.001811362924359719581, 0.01027195578987765215 ) ) ;
#25299=ADVANCED_FACE ( 'NONE', ( #8575 ), #3404, .F. ) ;
#25301=CARTESIAN_POINT ( 'NONE',  ( -55.24728320129491266, 0.0006547948648740692726, 0.01453410071985259712 ) ) ;
#25305=VERTEX_POINT ( 'NONE', #19509 ) ;
#25306=ORIENTED_EDGE ( 'NONE', *, *, #6891, .F. ) ;
#25308=CARTESIAN_POINT ( 'NONE',  ( -6.574463467970653952, -51.07975593197902953, 5.014313797967556496 ) ) ;
#25311=CARTESIAN_POINT ( 'NONE',  ( -21.41427618760447515, -7.777551129310266376, -29.81030852927063890 ) ) ;
#25314=VERTEX_POINT ( 'NONE', #13032 ) ;
#25321=CARTESIAN_POINT ( 'NONE',  ( -1.049817751779893227, 14.63752841325048237, -43.39729912094385611 ) ) ;
#25327=VECTOR ( 'NONE', #14268, 1000.000000000000000 ) ;
#25332=DIRECTION ( 'NONE',  ( 1.000000000000000000, -6.938893903907226837E-18, 1.734723475976806709E-18 ) ) ;
#25333=CARTESIAN_POINT ( 'NONE',  ( -55.24728320129491266, 0.0006547948648751116246, -0.01453410071985669280 ) ) ;
#25336=CARTESIAN_POINT ( 'NONE',  ( -1.056502255334264895, 14.64009593116162478, 43.40574022158757828 ) ) ;
#25340=CARTESIAN_POINT ( 'NONE',  ( -1.050229599974477068, 45.79907399707867199, 0.2556477501661113538 ) ) ;
#25341=CARTESIAN_POINT ( 'NONE',  ( -1.050231094221214301, -43.63617436699747287, -13.91061116148175536 ) ) ;
#25342=CARTESIAN_POINT ( 'NONE',  ( -25.21435515916043002, 4.655591116594353984, -34.29329011225956947 ) ) ;
#25346=LINE ( 'NONE', #23620, #27342 ) ;
#25348=B_SPLINE_CURVE_WITH_KNOTS ( 'NONE', 3,
 ( #14820, #15085, #8361, #23905, #22001, #4022, #15369, #25915 ),
 .UNSPECIFIED., .F., .F.,
 ( 4, 2, 2, 4 ),
 ( 0.000000000000000000, 0.002761524886576646742, 0.005523049773153293485, 0.01104609954630660605 ),
 .UNSPECIFIED. ) ;
#25365=CARTESIAN_POINT ( 'NONE',  ( -20.20612091757427109, -16.46550228026411844, -24.59769958242381094 ) ) ;
#25366=ORIENTED_EDGE ( 'NONE', *, *, #6372, .T. ) ;
#25392=CARTESIAN_POINT ( 'NONE',  ( -7.078251931573406708, -26.33626633876190937, 44.92740138729193689 ) ) ;
#25398=EDGE_CURVE ( 'NONE', #10905, #23680, #5340, .T. ) ;
#25400=CARTESIAN_POINT ( 'NONE',  ( -20.20612091757424622, 8.058516044219587116, 28.48192249925577357 ) ) ;
#25405=ORIENTED_EDGE ( 'NONE', *, *, #17825, .F. ) ;
#25416=CARTESIAN_POINT ( 'NONE',  ( -1.323830074806772172, 28.92190886481864709, -35.86387698262922186 ) ) ;
#25419=CARTESIAN_POINT ( 'NONE',  ( -20.24419206586952669, 10.37009329716804196, 27.76448493191432476 ) ) ;
#25425=FACE_OUTER_BOUND ( 'NONE', #28458, .T. ) ;
#25426=LINE ( 'NONE', #23270, #27033 ) ;
#25436=VERTEX_POINT ( 'NONE', #16773 ) ;
#25439=CARTESIAN_POINT ( 'NONE',  ( -1.045287976400365970, -37.92705037016778391, -25.66401692419976399 ) ) ;
#25450=VECTOR ( 'NONE', #21287, 1000.000000000000000 ) ;
#25457=ORIENTED_EDGE ( 'NONE', *, *, #24412, .F. ) ;
#25458=B_SPLINE_CURVE_WITH_KNOTS ( 'NONE', 3,
 ( #6363, #27950, #1746, #10545, #14571, #21141, #855, #25340, #25493, #20574, #25189, #5765, #3163 ),
 .UNSPECIFIED., .F., .F.,
 ( 4, 3, 3, 3, 4 ),
 ( 1.084202172485504434E-17, 0.0007657099931970561164, 0.001531419946797918721, 0.002296279302920154267, 0.003061450627205758099 ),
 .UNSPECIFIED. ) ;
#25459=B_SPLINE_CURVE_WITH_KNOTS ( 'NONE', 3,
 ( #22485, #24656, #24215, #11384, #15261, #15690 ),
 .UNSPECIFIED., .F., .F.,
 ( 4, 2, 4 ),
 ( 1.734723475976807094E-18, 0.0004335184443140216969, 0.0008670368886280416590 ),
 .UNSPECIFIED. ) ;
#25471=CARTESIAN_POINT ( 'NONE',  ( -1.463510566862832762, -11.94877850058534285, -44.64091840826485935 ) ) ;
#25491=CARTESIAN_POINT ( 'NONE',  ( -1.619063947482197729, -2.489035965909835557, 46.30105812165550816 ) ) ;
#25493=CARTESIAN_POINT ( 'NONE',  ( -1.049817751779888786, 45.79652915392415480, 0.5106138415328438374 ) ) ;
#25499=CARTESIAN_POINT ( 'NONE',  ( -1.619063947482197729, -29.22875152547730337, 35.99532424477411041 ) ) ;
#25506=PRODUCT_DEFINITION ( 'UNKNOWN', '', #6152, #1042 ) ;
#25512=ORIENTED_EDGE ( 'NONE', *, *, #19177, .T. ) ;
#25515=DIRECTION ( 'NONE',  ( 0.7563875759206387661, 0.6320336713238499105, -0.1685564395263362270 ) ) ;
#25521=CARTESIAN_POINT ( 'NONE',  ( -1.259972190295293393, -28.82609802125285015, -35.85909728507041194 ) ) ;
#25526=DIRECTION ( 'NONE',  ( 1.000000000000000000, -6.938893903907226837E-18, 1.734723475976806709E-18 ) ) ;
#25534=CARTESIAN_POINT ( 'NONE',  ( -25.21435515916043357, -15.02493970636125198, 31.17620025257602379 ) ) ;
#25536=EDGE_CURVE ( 'NONE', #11759, #6633, #108, .T. ) ;
#25538=EDGE_CURVE ( 'NONE', #8126, #21801, #9839, .T. ) ;
#25541=CARTESIAN_POINT ( 'NONE',  ( -19.53423201713130197, 1.355459634611817678E-16, -3.388649086529544194E-17 ) ) ;
#25545=CARTESIAN_POINT ( 'NONE',  ( -1.464342487929852998, 25.15873223207692178, -38.76467504336592640 ) ) ;
#25546=ORIENTED_EDGE ( 'NONE', *, *, #4414, .F. ) ;
#25547=CARTESIAN_POINT ( 'NONE',  ( -1.050230346682676785, 43.55772679531850855, -14.15203301556446647 ) ) ;
#25552=CARTESIAN_POINT ( 'NONE',  ( -20.24419206586952313, 16.36655224501367911, -24.70913649113835930 ) ) ;
#25554=EDGE_CURVE ( 'NONE', #12534, #27588, #24933, .T. ) ;
#25566=CARTESIAN_POINT ( 'NONE',  ( -6.574463467970464770, -44.27173031830730565, -25.96726214983177528 ) ) ;
#25571=CARTESIAN_POINT ( 'NONE',  ( -55.24271866751342941, 0.004365563123939763222, -0.008433070970614044842 ) ) ;
#25573=EDGE_LOOP ( 'NONE', ( #15824, #9159, #7305, #11040 ) ) ;
#25592=EDGE_LOOP ( 'NONE', ( #14923, #5399, #12836, #17981 ) ) ;
#25593=DIRECTION ( 'NONE',  ( 0.000000000000000000, 5.223019709707975211E-21, -1.000000000000000000 ) ) ;
#25600=CARTESIAN_POINT ( 'NONE',  ( -1.239374126674604337, -2.406737988131443906, -45.98822239537607715 ) ) ;
#25602=CARTESIAN_POINT ( 'NONE',  ( -20.20700224038492721, 28.44216453106548315, 8.199606986804035103 ) ) ;
#25606=VERTEX_POINT ( 'NONE', #20007 ) ;
#25607=CARTESIAN_POINT ( 'NONE',  ( -23.79223135445719350, -28.60983116549952143, 16.82181692922848626 ) ) ;
#25615=B_SPLINE_CURVE_WITH_KNOTS ( 'NONE', 3,
 ( #17321, #19491, #10218, #6397, #1134, #6543, #10066, #27598 ),
 .UNSPECIFIED., .F., .F.,
 ( 4, 2, 2, 4 ),
 ( 2.211348276820754320E-16, 0.002761568181852864200, 0.005523136363705507222, 0.01104627272741079066 ),
 .UNSPECIFIED. ) ;
#25617=CARTESIAN_POINT ( 'NONE',  ( -25.21435515916025594, 1.749597353048488237E-16, -4.373993382621220594E-17 ) ) ;
#25621=( BOUNDED_SURFACE ( )  B_SPLINE_SURFACE ( 3, 1, ( 
 ( #26599, #26462 ),
 ( #19988, #19700 ),
 ( #6624, #4876 ),
 ( #11353, #19845 ) ),
 .UNSPECIFIED., .F., .F., .F. ) 
 B_SPLINE_SURFACE_WITH_KNOTS ( ( 4, 4 ),
 ( 2, 2 ),
 ( 0.000000000000000000, 1.000000000000000000 ),
 ( 0.000000000000000000, 1.000000000000000000 ),
 .UNSPECIFIED. ) 
 GEOMETRIC_REPRESENTATION_ITEM ( )  RATIONAL_B_SPLINE_SURFACE ( (
 ( 1.000000000000000000, 1.000000000000000000),
 ( 0.7789835883360578528, 0.9689951854195403280),
 ( 0.7789835883360578528, 0.9689951854195403280),
 ( 1.000000000000000000, 1.000000000000000000) ) ) 
 REPRESENTATION_ITEM ( '' )  SURFACE ( )  );
#25622=CARTESIAN_POINT ( 'NONE',  ( -5.986830583229487246, 49.46736940480273859, 11.27873876172089851 ) ) ;
#25628=CARTESIAN_POINT ( 'NONE',  ( -55.24198130335446422, 0.001516807524708540730, -0.009170435128245290474 ) ) ;
#25638=EDGE_CURVE ( 'NONE', #7509, #4222, #20779, .T. ) ;
#25644=CARTESIAN_POINT ( 'NONE',  ( -55.24300891470648622, 0.009225237711098475957, 0.003362556190414738716 ) ) ;
#25646=CARTESIAN_POINT ( 'NONE',  ( -20.57838717382308147, -23.26537097894118133, -18.89542499756491978 ) ) ;
#25649=CARTESIAN_POINT ( 'NONE',  ( -55.24271866751342941, 0.006757859501010503658, -0.006671293903668132526 ) ) ;
#25654=ORIENTED_EDGE ( 'NONE', *, *, #3303, .T. ) ;
#25659=B_SPLINE_CURVE_WITH_KNOTS ( 'NONE', 3,
 ( #4806, #766, #26663, #22666, #22812, #9549, #15729, #2935, #11712, #18306, #27087, #24543, #7396 ),
 .UNSPECIFIED., .F., .F.,
 ( 4, 3, 3, 3, 4 ),
 ( 1.551583845779545699E-17, 0.0007657099931970551407, 0.001531419946797920239, 0.002296279302920158170, 0.003061450627205758099 ),
 .UNSPECIFIED. ) ;
#25665=CARTESIAN_POINT ( 'NONE',  ( -9.156249394959706578, -24.29252099376457608, 48.78605533024762764 ) ) ;
#25668=CARTESIAN_POINT ( 'NONE',  ( -15.02187109954785527, 32.04062513125116141, -33.49412687891580021 ) ) ;
#25678=CARTESIAN_POINT ( 'NONE',  ( -24.53239521893651442, 16.68574937151015192, 29.54733954334095358 ) ) ;
#25680=CARTESIAN_POINT ( 'NONE',  ( -20.21097721712958872, -28.05863618200116250, -9.464413111084637009 ) ) ;
#25681=CARTESIAN_POINT ( 'NONE',  ( -1.058197053496177764, -44.07533330186778642, 12.47644286888561105 ) ) ;
#25693=CARTESIAN_POINT ( 'NONE',  ( -20.57838717382308147, 16.28767523336121315, -25.16001208503110931 ) ) ;
#25696=CARTESIAN_POINT ( 'NONE',  ( -20.24419206586952313, 7.929973069813410547, -28.55732805495818383 ) ) ;
#25708=CARTESIAN_POINT ( 'NONE',  ( -55.24728320129491266, -0.01402509393918509838, 0.003868537197316900683 ) ) ;
#25709=DIRECTION ( 'NONE',  ( -0.7563875759206388771, -0.6320336713238522419, -0.1685564395263275950 ) ) ;
#25730=CARTESIAN_POINT ( 'NONE',  ( -20.57838717382308147, -25.16001208503117326, -16.28767523336112433 ) ) ;
#25733=CARTESIAN_POINT ( 'NONE',  ( -1.583189561560256253, -2.490696082060189109, -46.33203782964460515 ) ) ;
#25739=FACE_OUTER_BOUND ( 'NONE', #56, .T. ) ;
#25753=CARTESIAN_POINT ( 'NONE',  ( -1.323830074806772839, 38.58891736138533446, -25.17121255494489418 ) ) ;
#25755=ORIENTED_EDGE ( 'NONE', *, *, #13698, .T. ) ;
#25758=CARTESIAN_POINT ( 'NONE',  ( -20.37983603106074426, -7.753708011498764208, -28.74620395171560006 ) ) ;
#25761=CARTESIAN_POINT ( 'NONE',  ( -55.24198130335446422, -0.001516807524703878444, -0.009170435128245257514 ) ) ;
#25762=CARTESIAN_POINT ( 'NONE',  ( -20.57838717382308147, 18.89542499756500149, -23.26537097894111383 ) ) ;
#25763=CARTESIAN_POINT ( 'NONE',  ( -1.583189561560252701, 38.94740041318296164, -25.21827308671245760 ) ) ;
#25765=CARTESIAN_POINT ( 'NONE',  ( -1.113548883309548376, -28.52482525634917820, 35.91246368318234516 ) ) ;
#25768=ORIENTED_EDGE ( 'NONE', *, *, #19090, .F. ) ;
#25772=CARTESIAN_POINT ( 'NONE',  ( -1.044556982611269502, 15.70482750345296452, 43.01635920718332784 ) ) ;
#25774=VECTOR ( 'NONE', #9720, 999.9999999999998863 ) ;
#25776=CARTESIAN_POINT ( 'NONE',  ( -1.259920593601965066, 43.01175804832032412, 16.33409644610508238 ) ) ;
#25785=ORIENTED_EDGE ( 'NONE', *, *, #20372, .F. ) ;
#25789=EDGE_CURVE ( 'NONE', #27426, #8723, #28419, .T. ) ;
#25790=ORIENTED_EDGE ( 'NONE', *, *, #14257, .T. ) ;
#25792=ADVANCED_FACE ( 'NONE', ( #17901 ), #2632, .F. ) ;
#25796=CARTESIAN_POINT ( 'NONE',  ( -55.25719721206881729, 0.01079965405819524257, -0.002847566758684156023 ) ) ;
#25798=ORIENTED_EDGE ( 'NONE', *, *, #23852, .F. ) ;
#25802=B_SPLINE_CURVE_WITH_KNOTS ( 'NONE', 3,
 ( #10854, #27977, #17312, #27843, #28246, #8141 ),
 .UNSPECIFIED., .F., .F.,
 ( 4, 2, 4 ),
 ( 4.679414566804424472E-16, 0.003576372551511269784, 0.007152745103022071192 ),
 .UNSPECIFIED. ) ;
#25810=CARTESIAN_POINT ( 'NONE',  ( -21.41430102051752016, 28.68859753627394582, -11.22990201072285466 ) ) ;
#25819=( BOUNDED_SURFACE ( )  B_SPLINE_SURFACE ( 3, 1, ( 
 ( #12183, #20666 ),
 ( #5565, #5132 ),
 ( #9746, #24735 ),
 ( #7599, #18516 ) ),
 .UNSPECIFIED., .F., .F., .F. ) 
 B_SPLINE_SURFACE_WITH_KNOTS ( ( 4, 4 ),
 ( 2, 2 ),
 ( 0.000000000000000000, 1.000000000000000000 ),
 ( 0.000000000000000000, 1.000000000000000000 ),
 .UNSPECIFIED. ) 
 GEOMETRIC_REPRESENTATION_ITEM ( )  RATIONAL_B_SPLINE_SURFACE ( (
 ( 1.000000000000000000, 1.000000000000000000),
 ( 0.9934239774497838349, 0.8357310067453913582),
 ( 0.9934239774497838349, 0.8357310067453913582),
 ( 1.000000000000000000, 1.000000000000000000) ) ) 
 REPRESENTATION_ITEM ( '' )  SURFACE ( )  );
#25821=ORIENTED_EDGE ( 'NONE', *, *, #1018, .T. ) ;
#25823=EDGE_CURVE ( 'NONE', #14162, #7747, #21075, .T. ) ;
#25826=CARTESIAN_POINT ( 'NONE',  ( -20.90916690077961704, -27.35210456531395451, -28.59207721780137135 ) ) ;
#25828=CARTESIAN_POINT ( 'NONE',  ( -20.38016308990359349, 27.81387210821422329, -10.62413300760995583 ) ) ;
#25831=EDGE_CURVE ( 'NONE', #11014, #1503, #3605, .T. ) ;
#25841=CARTESIAN_POINT ( 'NONE',  ( -4.473127245936434626, 31.51789735524247504, 37.94261489385684882 ) ) ;
#25842=EDGE_CURVE ( 'NONE', #14776, #14092, #1863, .T. ) ;
#25847=ORIENTED_EDGE ( 'NONE', *, *, #28266, .T. ) ;
#25852=ORIENTED_EDGE ( 'NONE', *, *, #4443, .T. ) ;
#25854=ORIENTED_EDGE ( 'NONE', *, *, #8850, .F. ) ;
#25857=CARTESIAN_POINT ( 'NONE',  ( -23.77929240705206482, 31.93650644494365309, 17.17389748746929001 ) ) ;
#25858=LINE ( 'NONE', #2212, #13838 ) ;
#25859=CARTESIAN_POINT ( 'NONE',  ( -1.048994561756786625, 13.42228657661184954, 43.78680886990926524 ) ) ;
#25864=CARTESIAN_POINT ( 'NONE',  ( -55.24271866751342941, -0.006757859501009785483, 0.006671293903667892267 ) ) ;
#25865=CARTESIAN_POINT ( 'NONE',  ( -1.045287976400365970, 45.76855895860943235, -1.530335034934267258 ) ) ;
#25875=ORIENTED_EDGE ( 'NONE', *, *, #25831, .T. ) ;
#25887=ORIENTED_EDGE ( 'NONE', *, *, #6372, .F. ) ;
#25890=CONICAL_SURFACE ( 'NONE', #21738, 34.60786435723138510, 0.8559913436420825139 ) ;
#25894=CARTESIAN_POINT ( 'NONE',  ( -1.619063947482201282, 38.92136151114908671, -25.20140673341387227 ) ) ;
#25896=CARTESIAN_POINT ( 'NONE',  ( -18.41936578851710493, -5.707900577127883679, 42.05131332928132082 ) ) ;
#25900=CARTESIAN_POINT ( 'NONE',  ( -8.786685647604890903, -47.14957014837335691, 25.35688121747554291 ) ) ;
#25905=CARTESIAN_POINT ( 'NONE',  ( -4.473127245936434626, 45.82513704981544578, -18.25038884639885950 ) ) ;
#25909=CARTESIAN_POINT ( 'NONE',  ( -1.619063947482197729, -46.30105812165550105, -2.489035965909997206 ) ) ;
#25913=CARTESIAN_POINT ( 'NONE',  ( -20.90916690077961348, 38.93431874629082756, 7.054312691028585824 ) ) ;
#25915=CARTESIAN_POINT ( 'NONE',  ( -1.619063947482201282, 35.99532424477380488, -29.22875152547769062 ) ) ;
#25917=CARTESIAN_POINT ( 'NONE',  ( -8.786685647604887350, 53.04920435127183254, -7.199674155859138835 ) ) ;
#25920=ORIENTED_EDGE ( 'NONE', *, *, #17666, .T. ) ;
#25923=VECTOR ( 'NONE', #24390, 1000.000000000000000 ) ;
#25924=CARTESIAN_POINT ( 'NONE',  ( -1.046935749539995353, -36.28605774377782467, -27.93995161054682441 ) ) ;
#25926=CARTESIAN_POINT ( 'NONE',  ( -20.20700224038492721, -28.44216453106542986, -8.199606986804219844 ) ) ;
#25941=B_SPLINE_CURVE_WITH_KNOTS ( 'NONE', 3,
 ( #4275, #26569, #2383, #6871, #15616, #9162, #20091, #6448, #17921, #24589 ),
 .UNSPECIFIED., .F., .F.,
 ( 4, 2, 2, 2, 4 ),
 ( 0.000000000000000000, 0.0003346267210630928380, 0.0006692534421261856761, 0.001003880163189278460, 0.001338506884252371352 ),
 .UNSPECIFIED. ) ;
#25944=B_SPLINE_CURVE_WITH_KNOTS ( 'NONE', 3,
 ( #14767, #7607, #967, #9754, #5424, #14187, #3273, #19367, #28001, #25859, #2214, #17484, #21526 ),
 .UNSPECIFIED., .F., .F.,
 ( 4, 3, 3, 3, 4 ),
 ( 1.868354362588067661E-17, 0.0007657099931970537312, 0.001531419946797914168, 0.002296279302920151665, 0.003061450627205758099 ),
 .UNSPECIFIED. ) ;
#25945=CARTESIAN_POINT ( 'NONE',  ( -1.583189561560253589, -29.24830400313191348, -36.01941156322777005 ) ) ;
#25947=CARTESIAN_POINT ( 'NONE',  ( -4.178947244162647401, 41.47292084251672151, 25.96944194166747621 ) ) ;
#25949=EDGE_CURVE ( 'NONE', #14622, #12565, #6015, .T. ) ;
#25951=CARTESIAN_POINT ( 'NONE',  ( -22.23226125620943705, 29.33577758406451252, -11.82389163795220455 ) ) ;
#25953=VERTEX_POINT ( 'NONE', #901 ) ;
#25957=EDGE_LOOP ( 'NONE', ( #27757, #6838 ) ) ;
#25959=VERTEX_POINT ( 'NONE', #18750 ) ;
#25960=ORIENTED_EDGE ( 'NONE', *, *, #8578, .F. ) ;
#25964=EDGE_CURVE ( 'NONE', #16059, #457, #15556, .T. ) ;
#25966=CARTESIAN_POINT ( 'NONE',  ( -55.24390624410018802, -0.004572280736702649152, 0.009374879212966917563 ) ) ;
#25973=DIRECTION ( 'NONE',  ( 5.541455922705464902E-20, -5.223019709708320524E-21, 1.000000000000000000 ) ) ;
#25986=ORIENTED_EDGE ( 'NONE', *, *, #4413, .T. ) ;
#25990=CARTESIAN_POINT ( 'NONE',  ( -6.574463467970655728, 34.08059230520098737, 38.37705091668339463 ) ) ;
#26002=CARTESIAN_POINT ( 'NONE',  ( -1.619063947482197729, -2.489035965910479486, -46.30105812165547974 ) ) ;
#26003=EDGE_CURVE ( 'NONE', #14092, #987, #3915, .T. ) ;
#26008=CARTESIAN_POINT ( 'NONE',  ( -10.86508079875781263, 45.04061326950873223, -24.22249093393315533 ) ) ;
#26010=B_SPLINE_CURVE_WITH_KNOTS ( 'NONE', 3,
 ( #13003, #15427, #19906, #19753, #21642, #1915, #45, #19483, #21499, #17447, #24241, #4496, #15010 ),
 .UNSPECIFIED., .F., .F.,
 ( 4, 3, 3, 3, 4 ),
 ( 1.250926888277100149E-17, 0.0007657099931970565501, 0.001531419946797910915, 0.002296279302920149062, 0.003061450627205762869 ),
 .UNSPECIFIED. ) ;
#26013=CARTESIAN_POINT ( 'NONE',  ( -22.23342874802668234, -26.81018246605525590, 16.78332232459670337 ) ) ;
#26020=ORIENTED_EDGE ( 'NONE', *, *, #992, .T. ) ;
#26022=CARTESIAN_POINT ( 'NONE',  ( -8.259864102781675044, 52.06232470801727885, 9.986657004933084281 ) ) ;
#26027=DIRECTION ( 'NONE',  ( 0.000000000000000000, 5.223019709707975211E-21, -1.000000000000000000 ) ) ;
#26028=CARTESIAN_POINT ( 'NONE',  ( -7.762687761849950397E-17, 3.022826910523253725E-17, 44.74884827092600403 ) ) ;
#26035=CARTESIAN_POINT ( 'NONE',  ( -1.050230347360791017, -0.0004630652115286125773, 45.79907861464602092 ) ) ;
#26043=ORIENTED_EDGE ( 'NONE', *, *, #8167, .T. ) ;
#26046=CARTESIAN_POINT ( 'NONE',  ( -20.37983603106073716, 1.508851015062576462, -29.73529213200292176 ) ) ;
#26048=CARTESIAN_POINT ( 'NONE',  ( -1.045287976400351981, 43.05558670614237116, -15.59869763335110449 ) ) ;
#26060=B_SPLINE_CURVE_WITH_KNOTS ( 'NONE', 3,
 ( #27178, #7487, #16251, #5166, #13943, #14083 ),
 .UNSPECIFIED., .F., .F.,
 ( 4, 2, 4 ),
 ( 0.000000000000000000, 0.0004335151646191536890, 0.0008670303292383073780 ),
 .UNSPECIFIED. ) ;
#26062=ORIENTED_EDGE ( 'NONE', *, *, #13679, .T. ) ;
#26067=ADVANCED_FACE ( 'NONE', ( #20801 ), #6350, .F. ) ;
#26069=CARTESIAN_POINT ( 'NONE',  ( -55.24340739397742794, -0.008612749836242414997, -0.005344433640974251970 ) ) ;
#26072=CARTESIAN_POINT ( 'NONE',  ( -55.24198130335446422, 0.001391250620101877958, 0.009190321388310107587 ) ) ;
#26086=ORIENTED_EDGE ( 'NONE', *, *, #1632, .F. ) ;
#26088=EDGE_CURVE ( 'NONE', #10527, #12534, #5656, .T. ) ;
#26092=CARTESIAN_POINT ( 'NONE',  ( 14.74894986621300141, -1.023413983156987271E-16, 2.558534957892468177E-17 ) ) ;
#26099=CARTESIAN_POINT ( 'NONE',  ( -18.41936578851706230, 42.05131332928132082, 5.707900577128324215 ) ) ;
#26100=CARTESIAN_POINT ( 'NONE',  ( -20.90916690077963125, 18.74041620980169043, -34.84883504600955462 ) ) ;
#26103=CIRCLE ( 'NONE', #6824, 53.53553390275978785 ) ;
#26117=ORIENTED_EDGE ( 'NONE', *, *, #15791, .T. ) ;
#26119=CARTESIAN_POINT ( 'NONE',  ( -21.41427618760446094, -1.815001260755626733, 30.75468365310880259 ) ) ;
#26121=EDGE_CURVE ( 'NONE', #20961, #17579, #7028, .T. ) ;
#26122=CARTESIAN_POINT ( 'NONE',  ( -23.79248802219730052, 16.82188324679482605, -28.61009539422389381 ) ) ;
#26123=CIRCLE ( 'NONE', #8234, 34.60786435723138510 ) ;
#26151=FACE_OUTER_BOUND ( 'NONE', #17295, .T. ) ;
#26158=ORIENTED_EDGE ( 'NONE', *, *, #17337, .T. ) ;
#26163=ADVANCED_FACE ( 'NONE', ( #25425 ), #5640, .T. ) ;
#26164=CARTESIAN_POINT ( 'NONE',  ( -1.539760825549682632, -11.93465943778483584, 44.72358953107743673 ) ) ;
#26170=CARTESIAN_POINT ( 'NONE',  ( -1.050230347699840694, -0.0002315326057593219944, 45.79907861674081460 ) ) ;
#26172=CARTESIAN_POINT ( 'NONE',  ( -23.77929240705206126, -6.464423883190137055, 35.68044874544703049 ) ) ;
#26178=CARTESIAN_POINT ( 'NONE',  ( -20.20612092514784308, -29.57813644637189299, 1.137292630518367265 ) ) ;
#26184=CARTESIAN_POINT ( 'NONE',  ( -1.048994561756802391, 27.53485040342894408, -36.59609844253136401 ) ) ;
#26189=CARTESIAN_POINT ( 'NONE',  ( -20.21097721650788159, -28.26295598655178765, -8.835581399095051580 ) ) ;
#26191=EDGE_CURVE ( 'NONE', #20564, #12449, #22481, .T. ) ;
#26192=EDGE_LOOP ( 'NONE', ( #11261, #4179, #13635, #9365 ) ) ;
#26200=CARTESIAN_POINT ( 'NONE',  ( -9.156249394959706578, -8.027840202793560920, 53.90509764945136340 ) ) ;
#26201=CARTESIAN_POINT ( 'NONE',  ( -4.473127245936431073, -37.94261489385741015, -31.51789735524179648 ) ) ;
#26207=CARTESIAN_POINT ( 'NONE',  ( -55.24390624410018802, -0.001811362924362171613, 0.01027195578988007209 ) ) ;
#26215=ORIENTED_EDGE ( 'NONE', *, *, #9009, .T. ) ;
#26225=CIRCLE ( 'NONE', #13817, 53.53553390275978785 ) ;
#26230=DIRECTION ( 'NONE',  ( 0.000000000000000000, 5.223019709708233256E-21, -1.000000000000000000 ) ) ;
#26231=CARTESIAN_POINT ( 'NONE',  ( -55.24728320129491266, 0.01402509393918179546, 0.003868537197316780987 ) ) ;
#26232=CIRCLE ( 'NONE', #15637, 53.53553390275978785 ) ;
#26235=CARTESIAN_POINT ( 'NONE',  ( -55.25719721206881729, 0.006045473558784881206, 0.009391134844728978373 ) ) ;
#26246=CARTESIAN_POINT ( 'NONE',  ( -20.47566262905010248, -29.82700878811085232, -1.586617686065453725 ) ) ;
#26252=CARTESIAN_POINT ( 'NONE',  ( -6.574463467970649511, 25.96726214983191383, -44.27173031830743355 ) ) ;
#26259=DIRECTION ( 'NONE',  ( 0.7637818620346800147, 0.3965875333584841234, -0.5092696688508654423 ) ) ;
#26260=ORIENTED_EDGE ( 'NONE', *, *, #23549, .F. ) ;
#26263=CARTESIAN_POINT ( 'NONE',  ( -1.031422197589711987, 43.06660437151308685, -15.60268798220652720 ) ) ;
#26279=B_SPLINE_CURVE_WITH_KNOTS ( 'NONE', 3,
 ( #8136, #16900, #25552, #1494, #10561, #25693 ),
 .UNSPECIFIED., .F., .F.,
 ( 4, 2, 4 ),
 ( 0.000000000000000000, 0.0004335184443140274431, 0.0008670368886280548863 ),
 .UNSPECIFIED. ) ;
#26282=CARTESIAN_POINT ( 'NONE',  ( -1.048171036023500369, -27.73816396939538009, 36.44209502233739073 ) ) ;
#26288=CIRCLE ( 'NONE', #16178, 53.53553390275978785 ) ;
#26289=EDGE_CURVE ( 'NONE', #5379, #1423, #2055, .T. ) ;
#26295=( BOUNDED_SURFACE ( )  B_SPLINE_SURFACE ( 3, 1, ( 
 ( #25864, #13168 ),
 ( #23729, #23862 ),
 ( #21958, #3974 ),
 ( #8447, #83 ) ),
 .UNSPECIFIED., .F., .F., .F. ) 
 B_SPLINE_SURFACE_WITH_KNOTS ( ( 4, 4 ),
 ( 2, 2 ),
 ( 0.000000000000000000, 1.000000000000000000 ),
 ( 0.000000000000000000, 1.000000000000000000 ),
 .UNSPECIFIED. ) 
 GEOMETRIC_REPRESENTATION_ITEM ( )  RATIONAL_B_SPLINE_SURFACE ( (
 ( 1.000000000000000000, 1.000000000000000000),
 ( 0.9934239774497838349, 0.8357310067453913582),
 ( 0.9934239774497838349, 0.8357310067453913582),
 ( 1.000000000000000000, 1.000000000000000000) ) ) 
 REPRESENTATION_ITEM ( '' )  SURFACE ( )  );
#26300=DIRECTION ( 'NONE',  ( 0.000000000000000000, 5.223019709708116647E-21, -1.000000000000000000 ) ) ;
#26304=CIRCLE ( 'NONE', #7964, 28.92774122539760384 ) ;
#26314=ORIENTED_EDGE ( 'NONE', *, *, #19090, .T. ) ;
#26316=CARTESIAN_POINT ( 'NONE',  ( -20.20700224038492721, 0.9908225410478516126, -29.58392382092673145 ) ) ;
#26317=ADVANCED_FACE ( 'NONE', ( #9117 ), #11415, .F. ) ;
#26322=ORIENTED_EDGE ( 'NONE', *, *, #8267, .T. ) ;
#26324=CARTESIAN_POINT ( 'NONE',  ( -1.583189561560253589, -46.33203782964459805, 2.490696082060356531 ) ) ;
#26327=ADVANCED_FACE ( 'NONE', ( #15726 ), #24057, .T. ) ;
#26328=EDGE_CURVE ( 'NONE', #11017, #5935, #4592, .T. ) ;
#26330=AXIS2_PLACEMENT_3D ( 'NONE', #20462, #11539, #608 ) ;
#26332=CARTESIAN_POINT ( 'NONE',  ( -20.20700224038492721, 29.58392382092673500, -0.9908225410479557516 ) ) ;
#26342=ORIENTED_EDGE ( 'NONE', *, *, #5092, .F. ) ;
#26343=CARTESIAN_POINT ( 'NONE',  ( -28.41354790283022069, 8.345538364877077342, -21.64275480268750940 ) ) ;
#26348=ORIENTED_EDGE ( 'NONE', *, *, #12357, .F. ) ;
#26352=CARTESIAN_POINT ( 'NONE',  ( -55.24271866751342941, 0.009369360294296127586, 0.001545935011630553526 ) ) ;
#26354=CARTESIAN_POINT ( 'NONE',  ( -7.078251931573406708, 5.101176922831390570, 51.82710018979469879 ) ) ;
#26358=CARTESIAN_POINT ( 'NONE',  ( -55.24198130335446422, 0.006617369590169233477, 0.006527480770975859110 ) ) ;
#26367=CARTESIAN_POINT ( 'NONE',  ( -20.20700224038492010, -0.9908225410480588913, -29.58392382092672435 ) ) ;
#26373=CARTESIAN_POINT ( 'NONE',  ( -55.24340739397742084, -0.002421372372453905585, -0.009842732675352267036 ) ) ;
#26397=CARTESIAN_POINT ( 'NONE',  ( -55.24390624410018802, 0.007503127514282199352, -0.007245494385991655198 ) ) ;
#26402=ORIENTED_EDGE ( 'NONE', *, *, #4999, .T. ) ;
#26404=ORIENTED_EDGE ( 'NONE', *, *, #13341, .T. ) ;
#26406=LINE ( 'NONE', #13022, #21604 ) ;
#26410=DIRECTION ( 'NONE',  ( -0.7637818620346801257, -0.3965875333584914508, -0.5092696688508597802 ) ) ;
#26417=FACE_OUTER_BOUND ( 'NONE', #9854, .T. ) ;
#26418=( BOUNDED_SURFACE ( )  B_SPLINE_SURFACE ( 3, 1, ( 
 ( #16087, #20409 ),
 ( #693, #26733 ),
 ( #13929, #11920 ),
 ( #12339, #18682 ) ),
 .UNSPECIFIED., .F., .F., .F. ) 
 B_SPLINE_SURFACE_WITH_KNOTS ( ( 4, 4 ),
 ( 2, 2 ),
 ( 0.000000000000000000, 1.000000000000000000 ),
 ( 0.000000000000000000, 1.000000000000000000 ),
 .UNSPECIFIED. ) 
 GEOMETRIC_REPRESENTATION_ITEM ( )  RATIONAL_B_SPLINE_SURFACE ( (
 ( 1.000000000000000000, 1.000000000000000000),
 ( 0.9593753223639863714, 0.9995975284513187731),
 ( 0.9593753223639863714, 0.9995975284513187731),
 ( 1.000000000000000000, 1.000000000000000000) ) ) 
 REPRESENTATION_ITEM ( '' )  SURFACE ( )  );
#26421=CARTESIAN_POINT ( 'NONE',  ( -1.045287976400386842, -28.14015102489780062, 36.12803364096639314 ) ) ;
#26422=CARTESIAN_POINT ( 'NONE',  ( -21.41430102051751305, -19.54553566814603016, -23.81424706376357392 ) ) ;
#26430=ORIENTED_EDGE ( 'NONE', *, *, #25789, .F. ) ;
#26432=CARTESIAN_POINT ( 'NONE',  ( -25.21435515916043713, -34.29329011225952684, 4.655591116594705703 ) ) ;
#26437=EDGE_CURVE ( 'NONE', #414, #2795, #14068, .T. ) ;
#26441=CARTESIAN_POINT ( 'NONE',  ( -20.38016308990357928, 28.74660391518355951, 7.753479680700641197 ) ) ;
#26443=CARTESIAN_POINT ( 'NONE',  ( -1.619063947482197729, 43.26576862488456499, 16.67502769180516964 ) ) ;
#26452=ORIENTED_EDGE ( 'NONE', *, *, #491, .T. ) ;
#26453=VERTEX_POINT ( 'NONE', #5587 ) ;
#26455=CARTESIAN_POINT ( 'NONE',  ( -55.25297051322618813, -0.01019003092403448357, -0.01093108995494832154 ) ) ;
#26461=CARTESIAN_POINT ( 'NONE',  ( -8.259864102781671491, 52.60025989855203221, -6.590267880897108022 ) ) ;
#26462=CARTESIAN_POINT ( 'NONE',  ( -9.156249394959706578, -53.74753343182696597, 9.022661520478342467 ) ) ;
#26476=CARTESIAN_POINT ( 'NONE',  ( -55.24271866751342941, 0.009369360294294836952, -0.001545935011626992572 ) ) ;
#26480=CARTESIAN_POINT ( 'NONE',  ( -15.02187109954798316, -40.82269973458204504, 21.95370994985608704 ) ) ;
#26483=CARTESIAN_POINT ( 'NONE',  ( -20.20612091757421069, 10.22177757278315191, -27.77903622052259536 ) ) ;
#26487=FACE_OUTER_BOUND ( 'NONE', #13434, .T. ) ;
#26490=CARTESIAN_POINT ( 'NONE',  ( -9.156249394959706578, -53.90509764945135629, -8.027840202793747437 ) ) ;
#26492=CARTESIAN_POINT ( 'NONE',  ( -1.583189561560253589, -43.29471907393730135, 16.68617981233748537 ) ) ;
#26494=CARTESIAN_POINT ( 'NONE',  ( -8.786685647604885574, 6.096987947571466530E-17, -1.524246986892866633E-17 ) ) ;
#26495=CARTESIAN_POINT ( 'NONE',  ( -23.77929240705206482, -4.877832571065186862, -35.93174012244169546 ) ) ;
#26497=ORIENTED_EDGE ( 'NONE', *, *, #28261, .T. ) ;
#26500=CARTESIAN_POINT ( 'NONE',  ( -55.24390624410018802, -0.001811362924359030029, -0.01027195578987783083 ) ) ;
#26501=ORIENTED_EDGE ( 'NONE', *, *, #3720, .T. ) ;
#26502=ORIENTED_EDGE ( 'NONE', *, *, #12036, .T. ) ;
#26505=CARTESIAN_POINT ( 'NONE',  ( -20.47566338032517663, -1.586617869344095322, -29.82700953060487592 ) ) ;
#26513=CARTESIAN_POINT ( 'NONE',  ( -1.048171036023507474, 43.23005599774320729, 15.11933492062782847 ) ) ;
#26516=CARTESIAN_POINT ( 'NONE',  ( -1.619063947482197729, 43.26576862488456499, 16.67502769180516964 ) ) ;
#26519=EDGE_LOOP ( 'NONE', ( #20890, #8961, #9911, #3281, #17064, #23866, #881, #2368, #27936, #26158, #14815, #10020, #25875, #14378, #24068, #9827, #26680, #13004, #18344, #865, #24105, #10391, #2037, #22632, #23829, #1344, #19022, #5558, #13329, #16196, #27249, #19890, #641, #950, #13012, #20836, #9561, #17700, #13769, #4566, #10164, #20712, #10912, #26404, #3337, #6687, #5278, #7075, #16874, #17929, #9887, #9906, #15222, #27303, #8640, #27855, #23251, #4654, #202, #5988, #18209, #20531, #23650, #4155 ) ) ;
#26521=B_SPLINE_CURVE_WITH_KNOTS ( 'NONE', 3,
 ( #12777, #2542, #17932, #9467, #20240, #24599 ),
 .UNSPECIFIED., .F., .F.,
 ( 4, 2, 4 ),
 ( 4.055692965608002806E-16, 0.003576372551511211671, 0.007152745103022018283 ),
 .UNSPECIFIED. ) ;
#26523=CARTESIAN_POINT ( 'NONE',  ( -1.031422197589716205, 37.93675465142474224, -25.67058493451456513 ) ) ;
#26524=CARTESIAN_POINT ( 'NONE',  ( -1.031422197589716205, 1.530725436377464499, -45.78027046666444733 ) ) ;
#26529=VERTEX_POINT ( 'NONE', #8181 ) ;
#26531=ORIENTED_EDGE ( 'NONE', *, *, #23940, .F. ) ;
#26533=CARTESIAN_POINT ( 'NONE',  ( -20.20612092514791058, -23.26073121129628873, 18.30568145913871447 ) ) ;
#26539=ORIENTED_EDGE ( 'NONE', *, *, #8382, .T. ) ;
#26549=CARTESIAN_POINT ( 'NONE',  ( -1.045287976400351981, 12.68782741917293855, -44.00138577190654132 ) ) ;
#26552=B_SPLINE_CURVE_WITH_KNOTS ( 'NONE', 3,
 ( #13172, #11174, #19654, #17907, #24577, #11447, #28427, #4540, #8726, #2666, #26282, #11032, #26421 ),
 .UNSPECIFIED., .F., .F.,
 ( 4, 3, 3, 3, 4 ),
 ( 9.813077866773594792E-18, 0.0007657099931970698858, 0.001531419946797932816, 0.002296279302920152098, 0.003061450627205747257 ),
 .UNSPECIFIED. ) ;
#26553=ORIENTED_EDGE ( 'NONE', *, *, #7675, .F. ) ;
#26554=DIRECTION ( 'NONE',  ( 0.7637818620346800147, -0.6201872550346642088, 0.1788995134688892708 ) ) ;
#26555=CARTESIAN_POINT ( 'NONE',  ( -20.20700224038492721, -29.58392382092674211, -0.9908225410477480288 ) ) ;
#26569=CARTESIAN_POINT ( 'NONE',  ( -1.539760825549681966, -35.94320866319468166, 29.16712717142800670 ) ) ;
#26570=ORIENTED_EDGE ( 'NONE', *, *, #5204, .T. ) ;
#26579=DIRECTION ( 'NONE',  ( 1.000000000000000000, -6.938893903907226837E-18, 1.734723475976806709E-18 ) ) ;
#26594=CARTESIAN_POINT ( 'NONE',  ( -16.86833981943413363, 43.82216161736224791, -5.948101187261743306 ) ) ;
#26599=CARTESIAN_POINT ( 'NONE',  ( -55.25719721206881729, -0.008651607285659737578, -0.007063345920777289004 ) ) ;
#26601=EDGE_CURVE ( 'NONE', #14777, #6545, #13873, .T. ) ;
#26607=CARTESIAN_POINT ( 'NONE',  ( -20.24419206586953379, 29.61012937815439372, -1.282847120831333898 ) ) ;
#26611=EDGE_CURVE ( 'NONE', #4663, #8780, #16612, .T. ) ;
#26614=B_SPLINE_CURVE_WITH_KNOTS ( 'NONE', 3,
 ( #21414, #8192, #12219, #10487, #7927, #18984, #6039 ),
 .UNSPECIFIED., .F., .F.,
 ( 4, 3, 4 ),
 ( 2.453269466693398621E-17, 0.009512539173626417474, 0.02506242213020847681 ),
 .UNSPECIFIED. ) ;
#26619=CARTESIAN_POINT ( 'NONE',  ( -55.24390624410018802, -0.01027195578987978239, -0.001811362924362686826 ) ) ;
#26621=CARTESIAN_POINT ( 'NONE',  ( -20.37983603106074426, 10.62371319148641291, -27.81368274044714539 ) ) ;
#26629=CARTESIAN_POINT ( 'NONE',  ( -7.733045908741331687, -25.81515396910893045, -45.70676731105710644 ) ) ;
#26631=ADVANCED_FACE ( 'NONE', ( #9303 ), #8824, .F. ) ;
#26632=CARTESIAN_POINT ( 'NONE',  ( -22.34422965417125795, -34.15536449444077505, 16.46028608106144731 ) ) ;
#26650=CARTESIAN_POINT ( 'NONE',  ( -20.57838717382308147, -28.96176188950213870, 7.715628353033985753 ) ) ;
#26651=ORIENTED_EDGE ( 'NONE', *, *, #2945, .F. ) ;
#26652=CARTESIAN_POINT ( 'NONE',  ( -9.156249394959706578, 8.027840202793937507, -53.90509764945131366 ) ) ;
#26658=CARTESIAN_POINT ( 'NONE',  ( -55.24271866751342941, 0.004365563123935787236, 0.008433070970613791573 ) ) ;
#26660=EDGE_CURVE ( 'NONE', #17270, #5961, #4691, .T. ) ;
#26663=CARTESIAN_POINT ( 'NONE',  ( -1.048172774974294619, -36.44231470008696760, 27.73787987941047817 ) ) ;
#26664=CARTESIAN_POINT ( 'NONE',  ( -20.37983603106074426, 29.73529213200291821, 1.508851015062683487 ) ) ;
#26668=CARTESIAN_POINT ( 'NONE',  ( -1.045287976400362417, -12.68782741917263657, 44.00138577190661948 ) ) ;
#26676=ORIENTED_EDGE ( 'NONE', *, *, #8471, .T. ) ;
#26677=EDGE_CURVE ( 'NONE', #18316, #22163, #26552, .T. ) ;
#26679=CARTESIAN_POINT ( 'NONE',  ( -12.82751273423876803, -48.09651489336695107, -8.715310691360061313 ) ) ;
#26680=ORIENTED_EDGE ( 'NONE', *, *, #10823, .T. ) ;
#26681=CARTESIAN_POINT ( 'NONE',  ( -25.21435515916043357, 16.39063784838743132, -30.48034229288645136 ) ) ;
#26682=AXIS2_PLACEMENT_3D ( 'NONE', #23811, #15267, #8128 ) ;
#26687=VECTOR ( 'NONE', #5867, 1000.000000000000114 ) ;
#26695=CARTESIAN_POINT ( 'NONE',  ( -2.265401668238146815, 11.98901689611106036, 45.46007138824028004 ) ) ;
#26696=CARTESIAN_POINT ( 'NONE',  ( -25.21435515916025594, 34.29329011225976842, -4.655591116594504086 ) ) ;
#26697=EDGE_CURVE ( 'NONE', #27443, #15365, #24559, .T. ) ;
#26704=CARTESIAN_POINT ( 'NONE',  ( -1.259920593601971062, -38.49623866863331045, 25.19630221849093488 ) ) ;
#26709=CARTESIAN_POINT ( 'NONE',  ( -21.41430102051744200, -30.75470819672111134, 1.815007301162295805 ) ) ;
#26714=CARTESIAN_POINT ( 'NONE',  ( -25.21435515916043713, -31.17620025257576799, 15.02493970636179377 ) ) ;
#26720=FACE_OUTER_BOUND ( 'NONE', #26519, .T. ) ;
#26722=EDGE_CURVE ( 'NONE', #17500, #21826, #14182, .T. ) ;
#26723=CARTESIAN_POINT ( 'NONE',  ( -25.21435515916043357, -6.169479169075226643, 34.05351380035340014 ) ) ;
#26726=ORIENTED_EDGE ( 'NONE', *, *, #7671, .F. ) ;
#26733=CARTESIAN_POINT ( 'NONE',  ( -1.056502255334265339, 36.75727364034771938, 27.33667001641128991 ) ) ;
#26737=CARTESIAN_POINT ( 'NONE',  ( -20.20700224038492365, 23.35150625415685255, 18.19058640100197977 ) ) ;
#26741=CARTESIAN_POINT ( 'NONE',  ( -7.078251931573406708, -51.82710018979472721, 5.101176922831208493 ) ) ;
#26755=CARTESIAN_POINT ( 'NONE',  ( -55.24271866751342941, -0.008433070970613520956, 0.004365563123935277227 ) ) ;
#26758=ADVANCED_FACE ( 'NONE', ( #20604 ), #1512, .T. ) ;
#26770=CARTESIAN_POINT ( 'NONE',  ( -8.786685647604898008, 48.22796981442802178, 23.24040270374343464 ) ) ;
#26772=CARTESIAN_POINT ( 'NONE',  ( -55.25297051322618813, -0.001818774723749082148, -0.01483298743814642773 ) ) ;
#26775=CARTESIAN_POINT ( 'NONE',  ( -15.02187109954785704, -33.49412687891593521, -32.04062513125103351 ) ) ;
#26776=CARTESIAN_POINT ( 'NONE',  ( -4.780792508754313275, -25.98388465890110410, -42.16805077400949386 ) ) ;
#26781=CARTESIAN_POINT ( 'NONE',  ( -1.619063947482197729, 38.92136151114943488, 25.20140673341330739 ) ) ;
#26786=VERTEX_POINT ( 'NONE', #24517 ) ;
#26787=ORIENTED_EDGE ( 'NONE', *, *, #1268, .F. ) ;
#26788=AXIS2_PLACEMENT_3D ( 'NONE', #7775, #16682, #10725 ) ;
#26794=AXIS2_PLACEMENT_3D ( 'NONE', #23760, #21985, #17107 ) ;
#26797=CARTESIAN_POINT ( 'NONE',  ( -55.24340739397742084, -0.007744344507854280558, -0.006539691034612628989 ) ) ;
#26798=B_SPLINE_CURVE_WITH_KNOTS ( 'NONE', 3,
 ( #28446, #14663, #25758, #23615, #28036, #17101 ),
 .UNSPECIFIED., .F., .F.,
 ( 4, 2, 4 ),
 ( 0.000000000000000000, 0.0004335151646191514122, 0.0008670303292383013064 ),
 .UNSPECIFIED. ) ;
#26807=CARTESIAN_POINT ( 'NONE',  ( -20.20700224038492010, -18.19058640100240254, -23.35150625415651859 ) ) ;
#26808=EDGE_CURVE ( 'NONE', #1423, #8797, #820, .T. ) ;
#26811=CARTESIAN_POINT ( 'NONE',  ( -1.239374126674604337, 25.08410696974298304, 38.61989855450910625 ) ) ;
#26813=CARTESIAN_POINT ( 'NONE',  ( -15.02187109954782507, 8.264310930413024892, 45.60876405941875333 ) ) ;
#26814=CARTESIAN_POINT ( 'NONE',  ( -5.986830583229487246, -49.46736940480267464, -11.27873876172122181 ) ) ;
#26823=CARTESIAN_POINT ( 'NONE',  ( -55.24300891470648622, -0.009812809446890113918, -0.0003472257464246985225 ) ) ;
#26824=ORIENTED_EDGE ( 'NONE', *, *, #13546, .F. ) ;
#26825=CARTESIAN_POINT ( 'NONE',  ( -1.113427685306992876, -28.52429901637193410, -35.91272432484649357 ) ) ;
#26834=DIRECTION ( 'NONE',  ( 1.000000000000000000, -6.938893903907226837E-18, 1.734723475976806709E-18 ) ) ;
#26835=ADVANCED_FACE ( 'NONE', ( #3233 ), #15592, .F. ) ;
#26840=CARTESIAN_POINT ( 'NONE',  ( -1.045287976400362417, -1.530335034934427574, -45.76855895860943235 ) ) ;
#26842=CARTESIAN_POINT ( 'NONE',  ( -1.031422197589711764, -1.530725436377143867, 45.78027046666444022 ) ) ;
#26858=VECTOR ( 'NONE', #16112, 999.9999999999998863 ) ;
#26863=VERTEX_POINT ( 'NONE', #18326 ) ;
#26865=CARTESIAN_POINT ( 'NONE',  ( -20.57838717382308147, -10.78122205917020437, -27.96569011373082603 ) ) ;
#26877=VERTEX_POINT ( 'NONE', #28108 ) ;
#26883=CARTESIAN_POINT ( 'NONE',  ( -23.77929240705188008, 35.93174012244194415, -4.877832571065094491 ) ) ;
#26884=CARTESIAN_POINT ( 'NONE',  ( -20.90916690077961704, -28.59207721780126477, 27.35210456531406109 ) ) ;
#26890=CARTESIAN_POINT ( 'NONE',  ( -25.21435515916043713, 4.655591116594827383, 34.29329011225949841 ) ) ;
#26894=( BOUNDED_SURFACE ( )  B_SPLINE_SURFACE ( 3, 1, ( 
 ( #13282, #26524 ),
 ( #329, #11560 ),
 ( #20337, #6829 ),
 ( #629, #17747 ) ),
 .UNSPECIFIED., .F., .F., .F. ) 
 B_SPLINE_SURFACE_WITH_KNOTS ( ( 4, 4 ),
 ( 2, 2 ),
 ( 0.000000000000000000, 1.000000000000000000 ),
 ( 0.000000000000000000, 1.000000000000000000 ),
 .UNSPECIFIED. ) 
 GEOMETRIC_REPRESENTATION_ITEM ( )  RATIONAL_B_SPLINE_SURFACE ( (
 ( 1.000000000000000000, 1.000000000000000000),
 ( 0.9593753223639863714, 0.9995975284513187731),
 ( 0.9593753223639863714, 0.9995975284513187731),
 ( 1.000000000000000000, 1.000000000000000000) ) ) 
 REPRESENTATION_ITEM ( '' )  SURFACE ( )  );
#26895=ORIENTED_EDGE ( 'NONE', *, *, #31, .F. ) ;
#26918=CARTESIAN_POINT ( 'NONE',  ( -20.57838717382308147, -18.89542499756482741, 23.26537097894125594 ) ) ;
#26921=CARTESIAN_POINT ( 'NONE',  ( -8.786685647604890903, -47.14957014837335691, 25.35688121747554291 ) ) ;
#26933=EDGE_CURVE ( 'NONE', #20203, #6666, #1830, .T. ) ;
#26935=CARTESIAN_POINT ( 'NONE',  ( -1.031422197589716205, -44.01264471863856897, -12.69107518035485782 ) ) ;
#26943=CARTESIAN_POINT ( 'NONE',  ( -21.41427618760457818, -16.60878262545437778, -25.94789270595500597 ) ) ;
#26945=ORIENTED_EDGE ( 'NONE', *, *, #8433, .F. ) ;
#26946=B_SPLINE_CURVE_WITH_KNOTS ( 'NONE', 3,
 ( #4440, #26461, #17262, #12943, #15232, #130, #9058, #15651 ),
 .UNSPECIFIED., .F., .F.,
 ( 4, 2, 2, 4 ),
 ( 0.000000000000000000, 0.002761524886576650645, 0.005523049773153301291, 0.01104609954630661299 ),
 .UNSPECIFIED. ) ;
#26947=VECTOR ( 'NONE', #20440, 999.9999999999998863 ) ;
#26950=CARTESIAN_POINT ( 'NONE',  ( -28.41354790283022069, -18.00456980371888704, 14.62505768302820464 ) ) ;
#26964=CARTESIAN_POINT ( 'NONE',  ( -8.786685647604896232, 25.35688121747570278, 47.14957014837326454 ) ) ;
#26966=CARTESIAN_POINT ( 'NONE',  ( -1.583189561560252701, 25.21827308671288392, 38.94740041318267032 ) ) ;
#26971=CARTESIAN_POINT ( 'NONE',  ( -20.20700224038492010, 8.199606986804733211, 28.44216453106527709 ) ) ;
#26973=CARTESIAN_POINT ( 'NONE',  ( -1.046936909428682005, 1.275306677858881743, 45.77873603877004882 ) ) ;
#26980=CARTESIAN_POINT ( 'NONE',  ( -24.53239521893653219, 24.99972072650176713, 22.94500969220215580 ) ) ;
#26986=DIRECTION ( 'NONE',  ( 0.000000000000000000, 5.223019709707975211E-21, -1.000000000000000000 ) ) ;
#26994=FACE_OUTER_BOUND ( 'NONE', #5746, .T. ) ;
#26997=ORIENTED_EDGE ( 'NONE', *, *, #10680, .T. ) ;
#27010=CARTESIAN_POINT ( 'NONE',  ( -1.583189561560255143, 46.33203782964461936, 2.490696082060026573 ) ) ;
#27016=DIRECTION ( 'NONE',  ( 1.000000000000000000, -6.938893903907226837E-18, 1.734723475976806709E-18 ) ) ;
#27018=AXIS2_PLACEMENT_3D ( 'NONE', #24897, #11641, #3293 ) ;
#27020=CARTESIAN_POINT ( 'NONE',  ( -15.02187109954783928, 20.12219089991090115, -41.75590530176315696 ) ) ;
#27024=ORIENTED_EDGE ( 'NONE', *, *, #23079, .F. ) ;
#27026=CARTESIAN_POINT ( 'NONE',  ( -22.23342874802668234, 7.677086057585391643, 30.68433055777672180 ) ) ;
#27028=CARTESIAN_POINT ( 'NONE',  ( -9.156249394959713683, 53.74753343182715781, 9.022661520477214481 ) ) ;
#27033=VECTOR ( 'NONE', #16336, 1000.000000000000114 ) ;
#27042=CARTESIAN_POINT ( 'NONE',  ( -1.058197053496169548, -45.77356582045592859, -1.754224732379389362 ) ) ;
#27045=CARTESIAN_POINT ( 'NONE',  ( -12.94347594948481195, -43.91326021875530472, -21.16159467081338263 ) ) ;
#27047=CARTESIAN_POINT ( 'NONE',  ( -4.162674018437141576, 48.79210541969627712, 3.424137510345119484 ) ) ;
#27048=CARTESIAN_POINT ( 'NONE',  ( -55.25297051322618813, -0.01306918787467559705, 0.007247191603131494450 ) ) ;
#27054=ORIENTED_EDGE ( 'NONE', *, *, #25078, .F. ) ;
#27058=ADVANCED_FACE ( 'NONE', ( #13135 ), #23544, .F. ) ;
#27062=CARTESIAN_POINT ( 'NONE',  ( -23.79248802219722947, 3.207402715357613676, 33.03370827286725842 ) ) ;
#27064=VERTEX_POINT ( 'NONE', #19749 ) ;
#27067=EDGE_LOOP ( 'NONE', ( #14694, #13615, #25129, #11445 ) ) ;
#27069=CARTESIAN_POINT ( 'NONE',  ( -1.045287976400362417, -1.530335034933495653, 45.76855895860946788 ) ) ;
#27071=CARTESIAN_POINT ( 'NONE',  ( -21.81686047589424859, -38.17230180719262478, -5.181745222995322919 ) ) ;
#27077=DIRECTION ( 'NONE',  ( -1.000000000000000000, 6.938893903907227607E-18, -1.734723475976806902E-18 ) ) ;
#27080=CARTESIAN_POINT ( 'NONE',  ( -12.94347594948485103, 23.08810053288751263, 42.93165645342833869 ) ) ;
#27087=CARTESIAN_POINT ( 'NONE',  ( -1.048171036023494596, -37.64178826568587510, 26.08692787913908617 ) ) ;
#27088=CARTESIAN_POINT ( 'NONE',  ( -20.57838717382308147, 29.92853265176831812, 1.611677988432465014 ) ) ;
#27096=EDGE_LOOP ( 'NONE', ( #3553, #5009, #26402, #2292 ) ) ;
#27098=B_SPLINE_CURVE_WITH_KNOTS ( 'NONE', 3,
 ( #27389, #9997, #25545, #7995, #23104, #5517, #3364, #18759, #7702, #12149 ),
 .UNSPECIFIED., .F., .F.,
 ( 4, 2, 2, 2, 4 ),
 ( 2.602085213965210642E-18, 0.0003346267210630942475, 0.0006692534421261858929, 0.001003880163189277593, 0.001338506884252369184 ),
 .UNSPECIFIED. ) ;
#27103=CARTESIAN_POINT ( 'NONE',  ( -4.473127245936431073, 26.34600523034598396, 41.70021447285024863 ) ) ;
#27110=CARTESIAN_POINT ( 'NONE',  ( -55.24271866751342941, 0.001545935011627245191, 0.009369360294294363373 ) ) ;
#27118=EDGE_LOOP ( 'NONE', ( #8907, #19816, #12933, #8418 ) ) ;
#27120=CARTESIAN_POINT ( 'NONE',  ( -55.24198130335446422, -0.008252882783649790471, 0.004276389980776089048 ) ) ;
#27121=CARTESIAN_POINT ( 'NONE',  ( -1.031422197589711764, -36.13727897780146492, -28.14735071801730726 ) ) ;
#27122=CARTESIAN_POINT ( 'NONE',  ( -23.79248802219724368, 7.157555990716900851, -32.40806545715334153 ) ) ;
#27127=EDGE_CURVE ( 'NONE', #20942, #16924, #3224, .T. ) ;
#27129=CARTESIAN_POINT ( 'NONE',  ( -23.79223135445718995, -32.40779366744830270, 7.157574570129486169 ) ) ;
#27131=CARTESIAN_POINT ( 'NONE',  ( -1.045287976400379737, -37.92705037016725100, 25.66401692420055269 ) ) ;
#27136=( BOUNDED_SURFACE ( )  B_SPLINE_SURFACE ( 3, 1, ( 
 ( #16582, #25665 ),
 ( #23366, #5942 ),
 ( #14697, #23505 ),
 ( #10949, #8943 ) ),
 .UNSPECIFIED., .F., .F., .F. ) 
 B_SPLINE_SURFACE_WITH_KNOTS ( ( 4, 4 ),
 ( 2, 2 ),
 ( 0.000000000000000000, 1.000000000000000000 ),
 ( 0.000000000000000000, 1.000000000000000000 ),
 .UNSPECIFIED. ) 
 GEOMETRIC_REPRESENTATION_ITEM ( )  RATIONAL_B_SPLINE_SURFACE ( (
 ( 1.000000000000000000, 1.000000000000000000),
 ( 0.7789835883360578528, 0.9689951854195403280),
 ( 0.7789835883360578528, 0.9689951854195403280),
 ( 1.000000000000000000, 1.000000000000000000) ) ) 
 REPRESENTATION_ITEM ( '' )  SURFACE ( )  );
#27141=CARTESIAN_POINT ( 'NONE',  ( -55.25297051322618813, -0.01306918787467238607, -0.007247191603129069307 ) ) ;
#27143=VERTEX_POINT ( 'NONE', #9541 ) ;
#27144=CARTESIAN_POINT ( 'NONE',  ( -22.23226125620944771, -16.78323347921898900, 26.80886670319655707 ) ) ;
#27145=VERTEX_POINT ( 'NONE', #27911 ) ;
#27146=CARTESIAN_POINT ( 'NONE',  ( -8.786685647604885574, 6.096987947571466530E-17, -1.524246986892866633E-17 ) ) ;
#27150=CARTESIAN_POINT ( 'NONE',  ( -24.53237795827023859, -3.868415699415882258, -33.71192251888856362 ) ) ;
#27158=ORIENTED_EDGE ( 'NONE', *, *, #25398, .T. ) ;
#27160=CARTESIAN_POINT ( 'NONE',  ( -55.25297051322618813, -0.006313402748432862636, 0.01354497706059893877 ) ) ;
#27166=CARTESIAN_POINT ( 'NONE',  ( -1.019300379054419725, -12.21833869579434761, 44.15350047934410327 ) ) ;
#27178=CARTESIAN_POINT ( 'NONE',  ( -20.57838717382308147, 16.28767523336157552, 25.16001208503087838 ) ) ;
#27187=CARTESIAN_POINT ( 'NONE',  ( -6.588769196390770411, 50.13301368233300082, -11.07780292579711556 ) ) ;
#27193=ORIENTED_EDGE ( 'NONE', *, *, #27284, .F. ) ;
#27194=EDGE_CURVE ( 'NONE', #24539, #28478, #589, .T. ) ;
#27196=CARTESIAN_POINT ( 'NONE',  ( -1.619063947482197729, -35.99532424477357750, 29.22875152547795707 ) ) ;
#27204=ORIENTED_EDGE ( 'NONE', *, *, #8972, .T. ) ;
#27214=ORIENTED_EDGE ( 'NONE', *, *, #15791, .F. ) ;
#27217=FACE_OUTER_BOUND ( 'NONE', #5110, .T. ) ;
#27232=CARTESIAN_POINT ( 'NONE',  ( -23.79223135445719350, -13.25822371132274924, 30.42557260166825017 ) ) ;
#27233=CARTESIAN_POINT ( 'NONE',  ( -1.113427685306994652, -25.34053733836502431, 38.22586258295222450 ) ) ;
#27239=VERTEX_POINT ( 'NONE', #15077 ) ;
#27247=AXIS2_PLACEMENT_3D ( 'NONE', #13075, #1990, #10789 ) ;
#27249=ORIENTED_EDGE ( 'NONE', *, *, #2514, .T. ) ;
#27257=CARTESIAN_POINT ( 'NONE',  ( -4.178947244162622532, 45.38689110596718734, -18.28784278438465805 ) ) ;
#27263=AXIS2_PLACEMENT_3D ( 'NONE', #6878, #24598, #15623 ) ;
#27265=CARTESIAN_POINT ( 'NONE',  ( -1.583189561560252701, -43.29471907393753582, -16.68617981233686365 ) ) ;
#27269=ORIENTED_EDGE ( 'NONE', *, *, #7675, .T. ) ;
#27271=CARTESIAN_POINT ( 'NONE',  ( -55.24198130335446422, -0.009190321388309828296, 0.001391250620101365347 ) ) ;
#27276=LINE ( 'NONE', #7732, #18771 ) ;
#27277=ORIENTED_EDGE ( 'NONE', *, *, #22943, .T. ) ;
#27284=EDGE_CURVE ( 'NONE', #21028, #7787, #20346, .T. ) ;
#27292=PRODUCT_CONTEXT ( 'NONE', #5692, 'mechanical' ) ;
#27293=CARTESIAN_POINT ( 'NONE',  ( -1.464342487929844783, -44.64187261869788870, -11.94843286121900228 ) ) ;
#27294=B_SPLINE_CURVE_WITH_KNOTS ( 'NONE', 3,
 ( #1998, #15086, #23906, #4436, #17535, #19839, #10657 ),
 .UNSPECIFIED., .F., .F.,
 ( 4, 3, 4 ),
 ( 9.299800619644450092E-17, 0.009512539173626386249, 0.02506242213020836232 ),
 .UNSPECIFIED. ) ;
#27298=ORIENTED_EDGE ( 'NONE', *, *, #11998, .T. ) ;
#27299=VECTOR ( 'NONE', #19217, 1000.000000000000114 ) ;
#27303=ORIENTED_EDGE ( 'NONE', *, *, #3714, .F. ) ;
#27306=CARTESIAN_POINT ( 'NONE',  ( -55.24390624410018802, 0.004572280736702236288, 0.009374879212970765180 ) ) ;
#27312=CARTESIAN_POINT ( 'NONE',  ( -20.57838717382308147, -18.89542499756516847, -23.26537097894098594 ) ) ;
#27320=CARTESIAN_POINT ( 'NONE',  ( -4.473127245936431073, 37.94261489385763753, 31.51789735524151226 ) ) ;
#27328=EDGE_CURVE ( 'NONE', #11014, #12154, #11166, .T. ) ;
#27331=EDGE_LOOP ( 'NONE', ( #23025, #26651, #17693, #14367 ) ) ;
#27333=CARTESIAN_POINT ( 'NONE',  ( -1.031422197589716205, 25.67058493451444079, -37.93675465142481329 ) ) ;
#27334=CARTESIAN_POINT ( 'NONE',  ( -1.046935749539996685, -43.14401153755477480, -15.35946454248379034 ) ) ;
#27336=CARTESIAN_POINT ( 'NONE',  ( -1.045287976400362417, -15.59869763335038506, 43.05558670614261985 ) ) ;
#27342=VECTOR ( 'NONE', #12647, 999.9999999999998863 ) ;
#27345=EDGE_LOOP ( 'NONE', ( #2697, #10315, #25034, #22349 ) ) ;
#27347=CARTESIAN_POINT ( 'NONE',  ( -55.25297051322618813, 0.01093108995494865114, -0.01019003092403491552 ) ) ;
#27351=CARTESIAN_POINT ( 'NONE',  ( -1.045287976400365970, 1.530335034933814731, -45.76855895860946788 ) ) ;
#27353=EDGE_LOOP ( 'NONE', ( #4439, #20185, #936, #10263 ) ) ;
#27356=( BOUNDED_SURFACE ( )  B_SPLINE_SURFACE ( 3, 1, ( 
 ( #9185, #17947 ),
 ( #7189, #4728 ),
 ( #2707, #13500 ),
 ( #2263, #11634 ) ),
 .UNSPECIFIED., .F., .F., .F. ) 
 B_SPLINE_SURFACE_WITH_KNOTS ( ( 4, 4 ),
 ( 2, 2 ),
 ( 0.000000000000000000, 1.000000000000000000 ),
 ( 0.000000000000000000, 1.000000000000000000 ),
 .UNSPECIFIED. ) 
 GEOMETRIC_REPRESENTATION_ITEM ( )  RATIONAL_B_SPLINE_SURFACE ( (
 ( 1.000000000000000000, 1.000000000000000000),
 ( 0.7789835883360576307, 0.9689951854195403280),
 ( 0.7789835883360576307, 0.9689951854195403280),
 ( 1.000000000000000000, 1.000000000000000000) ) ) 
 REPRESENTATION_ITEM ( '' )  SURFACE ( )  );
#27357=CARTESIAN_POINT ( 'NONE',  ( -1.155001620486248770, -25.28075036143248866, -38.31519699443491334 ) ) ;
#27365=EDGE_CURVE ( 'NONE', #16671, #21028, #14549, .T. ) ;
#27370=ADVANCED_FACE ( 'NONE', ( #6887 ), #28138, .F. ) ;
#27373=B_SPLINE_CURVE_WITH_KNOTS ( 'NONE', 3,
 ( #19662, #8322, #28023, #15191, #2098, #6586, #13050, #21835 ),
 .UNSPECIFIED., .F., .F.,
 ( 4, 2, 2, 4 ),
 ( 2.211348276820754320E-16, 0.002761568181852866368, 0.005523136363705511559, 0.01104627272741080107 ),
 .UNSPECIFIED. ) ;
#27376=CARTESIAN_POINT ( 'NONE',  ( -20.20612091757422490, -28.48192249925583752, 8.058516044219494745 ) ) ;
#27379=CARTESIAN_POINT ( 'NONE',  ( -28.13707043255157103, -0.7675454997505393173, 22.88591869784691468 ) ) ;
#27382=CARTESIAN_POINT ( 'NONE',  ( -1.619063947482197729, -25.20140673341345305, 38.92136151114934961 ) ) ;
#27389=CARTESIAN_POINT ( 'NONE',  ( -1.619063947482194177, 25.20140673341374438, -38.92136151114915066 ) ) ;
#27390=ORIENTED_EDGE ( 'NONE', *, *, #2906, .T. ) ;
#27403=CARTESIAN_POINT ( 'NONE',  ( -22.23226125620944060, -26.80886670319648246, -16.78323347921907427 ) ) ;
#27406=CARTESIAN_POINT ( 'NONE',  ( -28.13707043255157103, -14.07296284901319439, 18.06394523322468615 ) ) ;
#27407=CARTESIAN_POINT ( 'NONE',  ( -1.056502255334264895, 27.33667001641221717, 36.75727364034702305 ) ) ;
#27408=CARTESIAN_POINT ( 'NONE',  ( -1.113548883309550153, 28.52482525634944821, -35.91246368318211069 ) ) ;
#27416=CARTESIAN_POINT ( 'NONE',  ( -55.24300891470648622, 0.009812809446890878931, 0.0003472257464245802360 ) ) ;
#27418=CARTESIAN_POINT ( 'NONE',  ( -20.21097721712959938, -24.14932359587277233, 17.13687106192370280 ) ) ;
#27419=CARTESIAN_POINT ( 'NONE',  ( -8.786685647604892679, -53.04920435127177569, 7.199674155859498548 ) ) ;
#27420=ORIENTED_EDGE ( 'NONE', *, *, #1976, .F. ) ;
#27425=LINE ( 'NONE', #12727, #1069 ) ;
#27426=VERTEX_POINT ( 'NONE', #7040 ) ;
#27433=( BOUNDED_SURFACE ( )  B_SPLINE_SURFACE ( 3, 1, ( 
 ( #17127, #3897 ),
 ( #8502, #19155 ),
 ( #1592, #10256 ),
 ( #1723, #27926 ) ),
 .UNSPECIFIED., .F., .F., .F. ) 
 B_SPLINE_SURFACE_WITH_KNOTS ( ( 4, 4 ),
 ( 2, 2 ),
 ( 0.000000000000000000, 1.000000000000000000 ),
 ( 0.000000000000000000, 1.000000000000000000 ),
 .UNSPECIFIED. ) 
 GEOMETRIC_REPRESENTATION_ITEM ( )  RATIONAL_B_SPLINE_SURFACE ( (
 ( 1.000000000000000000, 1.000000000000000000),
 ( 0.9934239774497838349, 0.8357310067453913582),
 ( 0.9934239774497838349, 0.8357310067453913582),
 ( 1.000000000000000000, 1.000000000000000000) ) ) 
 REPRESENTATION_ITEM ( '' )  SURFACE ( )  );
#27440=CARTESIAN_POINT ( 'NONE',  ( -1.619063947482201282, -16.67502769180592992, -43.26576862488428077 ) ) ;
#27442=CARTESIAN_POINT ( 'NONE',  ( -28.13707043255157103, -14.07296284901345551, -18.06394523322448009 ) ) ;
#27443=VERTEX_POINT ( 'NONE', #5286 ) ;
#27447=CARTESIAN_POINT ( 'NONE',  ( -23.79223135445720771, 28.60983116549966354, -16.82181692922826599 ) ) ;
#27448=ORIENTED_EDGE ( 'NONE', *, *, #19384, .F. ) ;
#27451=CARTESIAN_POINT ( 'NONE',  ( -1.619063947482194177, -46.30105812165547974, 2.489035965910640247 ) ) ;
#27456=DIRECTION ( 'NONE',  ( 0.000000000000000000, 5.223019709707975211E-21, -1.000000000000000000 ) ) ;
#27458=CARTESIAN_POINT ( 'NONE',  ( -8.786685647604898008, 48.22796981442765940, -23.24040270374399952 ) ) ;
#27460=EDGE_CURVE ( 'NONE', #20961, #20579, #7613, .T. ) ;
#27462=CARTESIAN_POINT ( 'NONE',  ( -55.24340739397742084, 0.002421372372454598174, 0.009842732675352095298 ) ) ;
#27463=CARTESIAN_POINT ( 'NONE',  ( -1.048172774974287291, 13.17853518375297739, -43.86067135048624266 ) ) ;
#27465=ADVANCED_FACE ( 'NONE', ( #5429 ), #1972, .T. ) ;
#27467=DIRECTION ( 'NONE',  ( 0.000000000000000000, 5.223019709707975211E-21, -1.000000000000000000 ) ) ;
#27468=CARTESIAN_POINT ( 'NONE',  ( -22.23342874802668234, 30.68433055777684970, -7.677086057585063017 ) ) ;
#27469=ORIENTED_EDGE ( 'NONE', *, *, #18279, .T. ) ;
#27474=B_SPLINE_CURVE_WITH_KNOTS ( 'NONE', 3,
 ( #22174, #13107, #6355, #26480, #8795, #6785, #24204 ),
 .UNSPECIFIED., .F., .F.,
 ( 4, 3, 4 ),
 ( 2.695974601917670536E-16, 0.009512539173626363698, 0.02506242213020817844 ),
 .UNSPECIFIED. ) ;
#27483=CARTESIAN_POINT ( 'NONE',  ( -7.078251931573406708, 51.82710018979476985, -5.101176922830847893 ) ) ;
#27501=ADVANCED_FACE ( 'NONE', ( #3276 ), #24471, .F. ) ;
#27509=CIRCLE ( 'NONE', #18770, 53.53553390275978785 ) ;
#27510=VERTEX_POINT ( 'NONE', #21256 ) ;
#27513=CARTESIAN_POINT ( 'NONE',  ( -1.619063947482197729, -16.67502769180532596, 43.26576862488450104 ) ) ;
#27515=DIRECTION ( 'NONE',  ( -0.7637818620346801257, -0.5092696688508642211, 0.3965875333584858997 ) ) ;
#27525=CARTESIAN_POINT ( 'NONE',  ( -20.21097721712959583, -8.835581498567664838, -28.26295595852182529 ) ) ;
#27527=CARTESIAN_POINT ( 'NONE',  ( -20.20997486282892552, 1.395963739018065216E-16, 29.60348406988233450 ) ) ;
#27528=CARTESIAN_POINT ( 'NONE',  ( -1.045287976400362417, -44.00138577190658395, -12.68782741917276446 ) ) ;
#27538=CARTESIAN_POINT ( 'NONE',  ( -1.045287976400379737, 44.00138577190644185, -12.68782741917337198 ) ) ;
#27540=VERTEX_POINT ( 'NONE', #17072 ) ;
#27551=CARTESIAN_POINT ( 'NONE',  ( -8.786685647604890903, -48.22796981442785835, -23.24040270374372952 ) ) ;
#27561=ORIENTED_EDGE ( 'NONE', *, *, #58, .F. ) ;
#27568=CARTESIAN_POINT ( 'NONE',  ( -1.619063947482197729, -38.92136151114925724, -25.20140673341360227 ) ) ;
#27572=CARTESIAN_POINT ( 'NONE',  ( -5.986830583229479252, 33.39046620690970002, 38.20088153919464702 ) ) ;
#27574=CARTESIAN_POINT ( 'NONE',  ( -55.24300891470650754, 0.002702093572893664395, -0.009439835024159005245 ) ) ;
#27588=VERTEX_POINT ( 'NONE', #10602 ) ;
#27595=CARTESIAN_POINT ( 'NONE',  ( -1.583189561560256253, -43.29471907393730135, 16.68617981233747827 ) ) ;
#27598=CARTESIAN_POINT ( 'NONE',  ( -8.786685647604890903, 47.14957014837354876, -25.35688121747519119 ) ) ;
#27604=CARTESIAN_POINT ( 'NONE',  ( -1.045287976400362417, -28.14015102489855735, -36.12803364096578207 ) ) ;
#27606=AXIS2_PLACEMENT_3D ( 'NONE', #11195, #679, #15794 ) ;
#27607=ORIENTED_EDGE ( 'NONE', *, *, #12996, .F. ) ;
#27612=CARTESIAN_POINT ( 'NONE',  ( -8.786685647604896232, 52.67761315067299677, 9.545808661480061019 ) ) ;
#27614=CARTESIAN_POINT ( 'NONE',  ( -1.155001620486251879, -2.068551059060010022, 45.85729774065939779 ) ) ;
#27620=CARTESIAN_POINT ( 'NONE',  ( -22.23342874802668234, 2.180636882146512079, -31.55488258420089664 ) ) ;
#27621=ADVANCED_FACE ( 'NONE', ( #6570 ), #26295, .F. ) ;
#27644=FACE_OUTER_BOUND ( 'NONE', #1, .T. ) ;
#27648=VERTEX_POINT ( 'NONE', #23583 ) ;
#27650=VECTOR ( 'NONE', #26259, 1000.000000000000114 ) ;
#27674=DIRECTION ( 'NONE',  ( 0.7563875759206388771, -0.6104009704506944134, -0.2351350468682844030 ) ) ;
#27694=CARTESIAN_POINT ( 'NONE',  ( 60.46576798286869803, -4.195655488513964285E-16, 1.048913872128491071E-16 ) ) ;
#27700=CARTESIAN_POINT ( 'NONE',  ( -55.24271866751342941, -0.001425019990778747699, -0.009388511352200236415 ) ) ;
#27707=ORIENTED_EDGE ( 'NONE', *, *, #19856, .T. ) ;
#27716=DIRECTION ( 'NONE',  ( -0.7637818620346801257, 0.5092696688508612235, -0.3965875333584896190 ) ) ;
#27718=CARTESIAN_POINT ( 'NONE',  ( -1.044557008772710960, 36.05793264791386576, 28.22896138707331204 ) ) ;
#27723=VERTEX_POINT ( 'NONE', #26549 ) ;
#27724=B_SPLINE_CURVE_WITH_KNOTS ( 'NONE', 3,
 ( #4987, #530, #13759, #22720, #17928, #26714 ),
 .UNSPECIFIED., .F., .F.,
 ( 4, 2, 4 ),
 ( 1.499206600309199041E-16, 0.003570751334075636992, 0.007141502668151123931 ),
 .UNSPECIFIED. ) ;
#27735=B_SPLINE_CURVE_WITH_KNOTS ( 'NONE', 3,
 ( #12809, #6345, #23497, #8638, #6220, #2010, #3763, #16993, #4174, #21316 ),
 .UNSPECIFIED., .F., .F.,
 ( 4, 3, 3, 4 ),
 ( 0.001530725384384652287, 0.001531419946797919589, 0.002296279302920155134, 0.003061450627205758099 ),
 .UNSPECIFIED. ) ;
#27739=DIRECTION ( 'NONE',  ( -0.7637818620346801257, -0.02150485345385289709, -0.6451161201712178883 ) ) ;
#27740=VERTEX_POINT ( 'NONE', #20076 ) ;
#27748=CARTESIAN_POINT ( 'NONE',  ( -1.031422197589711987, -1.530725436377782467, -45.78027046666441890 ) ) ;
#27753=CARTESIAN_POINT ( 'NONE',  ( -25.21435515916025594, 1.749597353048488237E-16, -4.373993382621220594E-17 ) ) ;
#27754=EDGE_LOOP ( 'NONE', ( #5475, #14190, #3174, #6487 ) ) ;
#27755=CARTESIAN_POINT ( 'NONE',  ( -24.53239521893645048, 22.94500969220232633, -24.99972072650149713 ) ) ;
#27757=ORIENTED_EDGE ( 'NONE', *, *, #27194, .F. ) ;
#27763=APPLICATION_CONTEXT ( 'automotive_design' ) ;
#27769=CARTESIAN_POINT ( 'NONE',  ( -28.41354790283022069, 21.64275480268748453, -8.345538364877153725 ) ) ;
#27772=VERTEX_POINT ( 'NONE', #26971 ) ;
#27773=CARTESIAN_POINT ( 'NONE',  ( -1.058197053496169548, 38.06270006878853707, -25.48582931365482906 ) ) ;
#27777=CARTESIAN_POINT ( 'NONE',  ( -1.050229599974462413, -45.79907399707869331, -0.2556477501657915541 ) ) ;
#27779=CARTESIAN_POINT ( 'NONE',  ( -1.048996300304477769, -13.42280206896947092, 43.78665266739852058 ) ) ;
#27798=FACE_OUTER_BOUND ( 'NONE', #24042, .T. ) ;
#27808=ORIENTED_EDGE ( 'NONE', *, *, #24732, .F. ) ;
#27809=ORIENTED_EDGE ( 'NONE', *, *, #28375, .F. ) ;
#27813=CARTESIAN_POINT ( 'NONE',  ( -1.583189561560255143, 11.94859433442965546, 44.83405390829658188 ) ) ;
#27816=CARTESIAN_POINT ( 'NONE',  ( -24.53237795827026346, 24.99972053297905461, -22.94498492516348520 ) ) ;
#27820=CARTESIAN_POINT ( 'NONE',  ( -28.41354790283022069, -21.64275480268754137, -8.345538364876993853 ) ) ;
#27841=CARTESIAN_POINT ( 'NONE',  ( -1.045287976400365970, 45.76855895860946077, 1.530335034933974381 ) ) ;
#27843=CARTESIAN_POINT ( 'NONE',  ( -22.23342874802668234, 29.33662284748876914, 11.82490389046284029 ) ) ;
#27845=CARTESIAN_POINT ( 'NONE',  ( -8.786685647604890903, -9.545808661480235102, 52.67761315067295413 ) ) ;
#27848=EDGE_LOOP ( 'NONE', ( #4483, #19485, #25457, #4420 ) ) ;
#27850=EDGE_CURVE ( 'NONE', #15703, #7068, #4176, .T. ) ;
#27851=CARTESIAN_POINT ( 'NONE',  ( -1.058473599757817185, 28.32531354681336566, 35.99997772736180224 ) ) ;
#27855=ORIENTED_EDGE ( 'NONE', *, *, #23549, .T. ) ;
#27869=B_SPLINE_CURVE_WITH_KNOTS ( 'NONE', 3,
 ( #17175, #5973, #23539, #25828, #14874, #15005 ),
 .UNSPECIFIED., .F., .F.,
 ( 4, 2, 4 ),
 ( 0.000000000000000000, 0.0004335184443140232147, 0.0008670368886280464295 ),
 .UNSPECIFIED. ) ;
#27874=DIRECTION ( 'NONE',  ( -1.000000000000000000, 6.938893903907227607E-18, -1.734723475976806902E-18 ) ) ;
#27879=ORIENTED_EDGE ( 'NONE', *, *, #12637, .T. ) ;
#27880=ORIENTED_EDGE ( 'NONE', *, *, #10894, .F. ) ;
#27888=CARTESIAN_POINT ( 'NONE',  ( -12.82751273423879113, -21.21958768041828947, -44.03362901247000138 ) ) ;
#27894=EDGE_CURVE ( 'NONE', #7710, #18844, #25802, .T. ) ;
#27906=CARTESIAN_POINT ( 'NONE',  ( -1.048172774974286403, -43.86067135048628529, -13.17853518375281041 ) ) ;
#27911=CARTESIAN_POINT ( 'NONE',  ( -25.21435515916043713, -23.92354251275954979, -25.00736669481013053 ) ) ;
#27920=CARTESIAN_POINT ( 'NONE',  ( -1.058473599757823180, 12.47539220917862934, -44.07591602137159725 ) ) ;
#27921=CARTESIAN_POINT ( 'NONE',  ( -1.155031165708874985, 42.97366960678603931, -16.13806347973012834 ) ) ;
#27926=CARTESIAN_POINT ( 'NONE',  ( -1.583189561560256253, 29.24830400313217282, 36.01941156322756399 ) ) ;
#27931=VERTEX_POINT ( 'NONE', #28385 ) ;
#27936=ORIENTED_EDGE ( 'NONE', *, *, #28101, .T. ) ;
#27938=ADVANCED_FACE ( 'NONE', ( #21641 ), #21346, .F. ) ;
#27942=FACE_OUTER_BOUND ( 'NONE', #8579, .T. ) ;
#27943=ORIENTED_EDGE ( 'NONE', *, *, #18737, .T. ) ;
#27949=ADVANCED_FACE ( 'NONE', ( #19482 ), #4602, .F. ) ;
#27950=CARTESIAN_POINT ( 'NONE',  ( -1.046936909428679119, 45.77873603877006303, -1.275306677858401905 ) ) ;
#27963=ORIENTED_EDGE ( 'NONE', *, *, #20905, .F. ) ;
#27977=CARTESIAN_POINT ( 'NONE',  ( -24.53239521893653929, 30.86654523348686041, 14.09666242510765954 ) ) ;
#27983=CARTESIAN_POINT ( 'NONE',  ( -28.13707043255157103, -22.00298671236744497, -6.342158660426917116 ) ) ;
#27991=ORIENTED_EDGE ( 'NONE', *, *, #12642, .T. ) ;
#27992=CARTESIAN_POINT ( 'NONE',  ( -25.21435515916025594, 1.749597353048488237E-16, -4.373993382621220594E-17 ) ) ;
#27998=CARTESIAN_POINT ( 'NONE',  ( -8.786685647604931759, 47.14957014837394667, 25.35688121747446999 ) ) ;
#28001=CARTESIAN_POINT ( 'NONE',  ( -1.049817751779873021, 13.66628317065048392, 43.71287583013712208 ) ) ;
#28009=ORIENTED_EDGE ( 'NONE', *, *, #15521, .F. ) ;
#28010=DIRECTION ( 'NONE',  ( -0.7563875759206388771, 0.6320336713238511317, 0.1685564395263317583 ) ) ;
#28012=CARTESIAN_POINT ( 'NONE',  ( -25.21435515916043713, -23.92354251275918031, 25.00736669481048224 ) ) ;
#28023=CARTESIAN_POINT ( 'NONE',  ( -2.904412668506668016, 25.64203923793632356, 40.16685646686180178 ) ) ;
#28026=CARTESIAN_POINT ( 'NONE',  ( -20.24399999263415140, -1.282322917263260198, 29.60996018918694617 ) ) ;
#28030=CARTESIAN_POINT ( 'NONE',  ( -9.156249394959706578, -9.022661520478157726, -53.74753343182698728 ) ) ;
#28036=CARTESIAN_POINT ( 'NONE',  ( -20.20612091757416451, -8.058516044219402374, -28.48192249925589792 ) ) ;
#28057=DIRECTION ( 'NONE',  ( -0.7563875759206388771, -0.6531865459554678788, 0.03500244528122777032 ) ) ;
#28063=CARTESIAN_POINT ( 'NONE',  ( -55.24198130335446422, 0.004276389980780370345, -0.008252882783649044540 ) ) ;
#28073=AXIS2_PLACEMENT_3D ( 'NONE', #6836, #20055, #17754 ) ;
#28078=EDGE_CURVE ( 'NONE', #11177, #28126, #17224, .T. ) ;
#28083=ORIENTED_EDGE ( 'NONE', *, *, #3714, .T. ) ;
#28086=CARTESIAN_POINT ( 'NONE',  ( -8.259864102781710571, 46.42816643551610412, 25.58601832199028436 ) ) ;
#28088=VECTOR ( 'NONE', #1115, 1000.000000000000000 ) ;
#28094=VECTOR ( 'NONE', #21081, 1000.000000000000000 ) ;
#28101=EDGE_CURVE ( 'NONE', #10864, #5699, #10710, .T. ) ;
#28103=CIRCLE ( 'NONE', #19825, 37.50000000000001421 ) ;
#28106=AXIS2_PLACEMENT_3D ( 'NONE', #17421, #13111, #6503 ) ;
#28108=CARTESIAN_POINT ( 'NONE',  ( -20.57838717382308502, 25.16001208503106668, -16.28767523336130196 ) ) ;
#28109=CARTESIAN_POINT ( 'NONE',  ( -23.77929240705204705, 26.20227034809557054, -25.06639637888430272 ) ) ;
#28111=CARTESIAN_POINT ( 'NONE',  ( -4.162674018437137136, 45.34593312138912324, 18.33413805792392992 ) ) ;
#28112=CARTESIAN_POINT ( 'NONE',  ( -55.24271866751342941, -0.006671293903668846365, 0.006757859501006202411 ) ) ;
#28117=CARTESIAN_POINT ( 'NONE',  ( -1.259972190295307382, 28.82609802125311660, 35.85909728507018457 ) ) ;
#28119=CARTESIAN_POINT ( 'NONE',  ( -25.21435515916043713, -6.169479169075696490, -34.05351380035330777 ) ) ;
#28120=CARTESIAN_POINT ( 'NONE',  ( -28.41354790283022069, 12.60397206714860729, 19.47297445639535596 ) ) ;
#28121=CARTESIAN_POINT ( 'NONE',  ( -7.078251931573406708, 34.59014398252973166, 38.93060825814192327 ) ) ;
#28124=CARTESIAN_POINT ( 'NONE',  ( -4.178947244162629637, 25.96944194166794162, -41.47292084251642308 ) ) ;
#28126=VERTEX_POINT ( 'NONE', #23090 ) ;
#28134=EDGE_CURVE ( 'NONE', #26877, #18004, #18917, .T. ) ;
#28137=VERTEX_POINT ( 'NONE', #25239 ) ;
#28138=( BOUNDED_SURFACE ( )  B_SPLINE_SURFACE ( 3, 1, ( 
 ( #5143, #15632 ),
 ( #18229, #2699 ),
 ( #395, #24452 ),
 ( #15800, #4719 ) ),
 .UNSPECIFIED., .F., .F., .F. ) 
 B_SPLINE_SURFACE_WITH_KNOTS ( ( 4, 4 ),
 ( 2, 2 ),
 ( 0.000000000000000000, 1.000000000000000000 ),
 ( 0.000000000000000000, 1.000000000000000000 ),
 .UNSPECIFIED. ) 
 GEOMETRIC_REPRESENTATION_ITEM ( )  RATIONAL_B_SPLINE_SURFACE ( (
 ( 1.000000000000000000, 1.000000000000000000),
 ( 0.7789835883360576307, 0.9689951854195403280),
 ( 0.7789835883360576307, 0.9689951854195403280),
 ( 1.000000000000000000, 1.000000000000000000) ) ) 
 REPRESENTATION_ITEM ( '' )  SURFACE ( )  );
#28145=( BOUNDED_SURFACE ( )  B_SPLINE_SURFACE ( 3, 1, ( 
 ( #1128, #21113 ),
 ( #3143, #23441 ),
 ( #5590, #14201 ),
 ( #14502, #3429 ) ),
 .UNSPECIFIED., .F., .F., .F. ) 
 B_SPLINE_SURFACE_WITH_KNOTS ( ( 4, 4 ),
 ( 2, 2 ),
 ( 0.000000000000000000, 1.000000000000000000 ),
 ( 0.000000000000000000, 1.000000000000000000 ),
 .UNSPECIFIED. ) 
 GEOMETRIC_REPRESENTATION_ITEM ( )  RATIONAL_B_SPLINE_SURFACE ( (
 ( 1.000000000000000000, 1.000000000000000000),
 ( 0.9934239774497838349, 0.8357310067453913582),
 ( 0.9934239774497838349, 0.8357310067453913582),
 ( 1.000000000000000000, 1.000000000000000000) ) ) 
 REPRESENTATION_ITEM ( '' )  SURFACE ( )  );
#28148=CARTESIAN_POINT ( 'NONE',  ( -20.21097721650787804, 23.76068422213757714, -17.67178726257366606 ) ) ;
#28150=VERTEX_POINT ( 'NONE', #14269 ) ;
#28155=CARTESIAN_POINT ( 'NONE',  ( -1.619063947482197729, -43.26576862488421682, 16.67502769180607203 ) ) ;
#28183=CARTESIAN_POINT ( 'NONE',  ( -25.21435515916043357, -6.169479169075226643, 34.05351380035340014 ) ) ;
#28184=DIRECTION ( 'NONE',  ( 0.7637818620346800147, -0.6068965246771045319, -0.2198041754873859832 ) ) ;
#28185=CARTESIAN_POINT ( 'NONE',  ( -1.155001620486255209, -45.85729774065936937, -2.068551059060163677 ) ) ;
#28188=ORIENTED_EDGE ( 'NONE', *, *, #7108, .F. ) ;
#28191=CARTESIAN_POINT ( 'NONE',  ( -1.259972190295300054, 16.33417789844434509, 43.01178231151312303 ) ) ;
#28192=CARTESIAN_POINT ( 'NONE',  ( -2.265401668238146371, -29.73100299756539755, 36.42007794497283157 ) ) ;
#28205=CARTESIAN_POINT ( 'NONE',  ( -20.38016308990358638, -28.74660391518349911, -7.753479680700832155 ) ) ;
#28208=CARTESIAN_POINT ( 'NONE',  ( -4.780792508754314163, 32.07473752860781246, -37.74278713234406979 ) ) ;
#28211=VERTEX_POINT ( 'NONE', #17288 ) ;
#28216=CARTESIAN_POINT ( 'NONE',  ( -1.056502255334265339, -36.75727364034752043, -27.33667001641156702 ) ) ;
#28221=CARTESIAN_POINT ( 'NONE',  ( -1.583189561560256253, -29.24830400313190637, -36.01941156322777715 ) ) ;
#28222=CARTESIAN_POINT ( 'NONE',  ( -1.031422197589716205, -15.60268798220668174, -43.06660437151303711 ) ) ;
#28225=CARTESIAN_POINT ( 'NONE',  ( -20.90916690077960638, 7.054312691028996163, -38.93431874629079203 ) ) ;
#28235=EDGE_CURVE ( 'NONE', #26786, #20356, #25458, .T. ) ;
#28246=CARTESIAN_POINT ( 'NONE',  ( -21.41427618760457818, 28.68857606049983744, 11.22988868156155640 ) ) ;
#28248=EDGE_LOOP ( 'NONE', ( #23943, #11688, #14213, #3080 ) ) ;
#28252=ADVANCED_FACE ( 'NONE', ( #5906 ), #19317, .F. ) ;
#28254=CARTESIAN_POINT ( 'NONE',  ( -55.24271866751342941, 0.004256484107795918508, -0.008488649505343059953 ) ) ;
#28257=EDGE_LOOP ( 'NONE', ( #16464, #12393, #9098, #19107 ) ) ;
#28260=CARTESIAN_POINT ( 'NONE',  ( -28.13707043255157103, -12.83104814250467562, -18.96624908365841478 ) ) ;
#28261=EDGE_CURVE ( 'NONE', #4663, #1581, #21755, .T. ) ;
#28265=B_SPLINE_CURVE_WITH_KNOTS ( 'NONE', 3,
 ( #27088, #1059, #26664, #15731, #22516, #24544 ),
 .UNSPECIFIED., .F., .F.,
 ( 4, 2, 4 ),
 ( 6.505213034913026604E-19, 0.0004335151646191484848, 0.0008670303292382963191 ),
 .UNSPECIFIED. ) ;
#28266=EDGE_CURVE ( 'NONE', #22518, #2726, #19927, .T. ) ;
#28267=DIRECTION ( 'NONE',  ( 0.000000000000000000, -1.000000000000000000, 0.000000000000000000 ) ) ;
#28269=LINE ( 'NONE', #23984, #27650 ) ;
#28273=CARTESIAN_POINT ( 'NONE',  ( -1.239374126674604337, 16.50008610789360119, 42.99367564261261521 ) ) ;
#28283=CARTESIAN_POINT ( 'NONE',  ( -1.464342487929856995, 46.14921266389555399, -2.431462367721493045 ) ) ;
#28287=LINE ( 'NONE', #17637, #10625 ) ;
#28291=CARTESIAN_POINT ( 'NONE',  ( -2.911734481061399205, -44.38410240830292963, 17.36785190846027049 ) ) ;
#28292=CARTESIAN_POINT ( 'NONE',  ( -8.786685647604890903, 7.199674155858966529, -53.04920435127184675 ) ) ;
#28299=CARTESIAN_POINT ( 'NONE',  ( -9.156249394959706578, 9.022661520478530761, 53.74753343182691623 ) ) ;
#28300=VERTEX_POINT ( 'NONE', #16401 ) ;
#28301=CARTESIAN_POINT ( 'NONE',  ( -20.20700224038492721, 29.58392382092673500, -0.9908225410479557516 ) ) ;
#28303=DIRECTION ( 'NONE',  ( 0.000000000000000000, 5.223019709708233256E-21, -1.000000000000000000 ) ) ;
#28306=EDGE_LOOP ( 'NONE', ( #8586, #5516, #6230, #1396 ) ) ;
#28307=CARTESIAN_POINT ( 'NONE',  ( -12.94347594948482794, -6.555928820868979656, 48.30328466416770539 ) ) ;
#28312=( BOUNDED_SURFACE ( )  B_SPLINE_SURFACE ( 3, 1, ( 
 ( #28254, #21798 ),
 ( #15574, #15149 ),
 ( #17606, #2488 ),
 ( #4659, #2339 ) ),
 .UNSPECIFIED., .F., .F., .F. ) 
 B_SPLINE_SURFACE_WITH_KNOTS ( ( 4, 4 ),
 ( 2, 2 ),
 ( 0.000000000000000000, 1.000000000000000000 ),
 ( 0.000000000000000000, 1.000000000000000000 ),
 .UNSPECIFIED. ) 
 GEOMETRIC_REPRESENTATION_ITEM ( )  RATIONAL_B_SPLINE_SURFACE ( (
 ( 1.000000000000000000, 1.000000000000000000),
 ( 0.9593753223639863714, 0.9995975284513187731),
 ( 0.9593753223639863714, 0.9995975284513187731),
 ( 1.000000000000000000, 1.000000000000000000) ) ) 
 REPRESENTATION_ITEM ( '' )  SURFACE ( )  );
#28315=CARTESIAN_POINT ( 'NONE',  ( -1.044556982611275053, -45.76404732357875815, 1.643392503293194862 ) ) ;
#28318=CARTESIAN_POINT ( 'NONE',  ( -1.050230346682677007, -0.0006945978172492803249, 45.79907861045643358 ) ) ;
#28319=B_SPLINE_CURVE_WITH_KNOTS ( 'NONE', 3,
 ( #1013, #7797, #12240, #2888, #9806, #5032 ),
 .UNSPECIFIED., .F., .F.,
 ( 4, 2, 4 ),
 ( 0.000000000000000000, 0.0004335151646191517374, 0.0008670303292383034748 ),
 .UNSPECIFIED. ) ;
#28321=EDGE_CURVE ( 'NONE', #16924, #20693, #8264, .T. ) ;
#28328=CARTESIAN_POINT ( 'NONE',  ( -1.619063947482197729, 16.67502769180622835, 43.26576862488415287 ) ) ;
#28331=CARTESIAN_POINT ( 'NONE',  ( -1.019300379054419947, -25.26451264419671361, -38.21680004809154241 ) ) ;
#28332=CARTESIAN_POINT ( 'NONE',  ( -55.25297051322618813, 0.01019003092403740832, -0.01093108995495187946 ) ) ;
#28333=CARTESIAN_POINT ( 'NONE',  ( -1.048172774974286847, 26.08722459372787128, -37.64158596421222569 ) ) ;
#28341=ORIENTED_EDGE ( 'NONE', *, *, #22568, .F. ) ;
#28350=EDGE_CURVE ( 'NONE', #18844, #13567, #10635, .T. ) ;
#28351=CARTESIAN_POINT ( 'NONE',  ( -9.156249394959706578, -38.89149400288433611, -38.17928057391977603 ) ) ;
#28365=B_SPLINE_CURVE_WITH_KNOTS ( 'NONE', 3,
 ( #9372, #22765, #18127, #7215, #7347, #18259, #24778 ),
 .UNSPECIFIED., .F., .F.,
 ( 4, 3, 4 ),
 ( 0.000000000000000000, 0.006568092053401836973, 0.02506242213020846987 ),
 .UNSPECIFIED. ) ;
#28373=B_SPLINE_CURVE_WITH_KNOTS ( 'NONE', 3,
 ( #27612, #26022, #8332, #21133, #25622, #16693, #4136, #10492 ),
 .UNSPECIFIED., .F., .F.,
 ( 4, 2, 2, 4 ),
 ( 0.000000000000000000, 0.002761524886576655416, 0.005523049773153310832, 0.01104609954630662166 ),
 .UNSPECIFIED. ) ;
#28375=EDGE_CURVE ( 'NONE', #25436, #6634, #21707, .T. ) ;
#28379=CARTESIAN_POINT ( 'NONE',  ( -1.049819825607592794, 43.71263398674771139, 13.66706894614392986 ) ) ;
#28385=CARTESIAN_POINT ( 'NONE',  ( -20.57838717382308147, -29.92853265176830746, 1.611677988432673070 ) ) ;
#28390=CARTESIAN_POINT ( 'NONE',  ( -55.24271866751342941, -0.009388511352199774979, 0.001425019990778933097 ) ) ;
#28396=ORIENTED_EDGE ( 'NONE', *, *, #23236, .T. ) ;
#28408=ORIENTED_EDGE ( 'NONE', *, *, #23817, .F. ) ;
#28410=EDGE_CURVE ( 'NONE', #15835, #19755, #3107, .T. ) ;
#28413=EDGE_CURVE ( 'NONE', #21724, #414, #15297, .T. ) ;
#28417=EDGE_CURVE ( 'NONE', #13229, #10864, #26798, .T. ) ;
#28419=LINE ( 'NONE', #504, #12970 ) ;
#28422=( BOUNDED_SURFACE ( )  B_SPLINE_SURFACE ( 3, 1, ( 
 ( #7230, #13826 ),
 ( #16426, #3327 ),
 ( #11825, #24931 ),
 ( #5045, #22633 ) ),
 .UNSPECIFIED., .F., .F., .F. ) 
 B_SPLINE_SURFACE_WITH_KNOTS ( ( 4, 4 ),
 ( 2, 2 ),
 ( 0.000000000000000000, 1.000000000000000000 ),
 ( 0.000000000000000000, 1.000000000000000000 ),
 .UNSPECIFIED. ) 
 GEOMETRIC_REPRESENTATION_ITEM ( )  RATIONAL_B_SPLINE_SURFACE ( (
 ( 1.000000000000000000, 1.000000000000000000),
 ( 0.9593753223639863714, 0.9995975284513187731),
 ( 0.9593753223639863714, 0.9995975284513187731),
 ( 1.000000000000000000, 1.000000000000000000) ) ) 
 REPRESENTATION_ITEM ( '' )  SURFACE ( )  );
#28427=CARTESIAN_POINT ( 'NONE',  ( -1.050230346682680560, -26.92058491724839797, 37.05182464822011923 ) ) ;
#28440=ORIENTED_EDGE ( 'NONE', *, *, #9070, .F. ) ;
#28446=CARTESIAN_POINT ( 'NONE',  ( -20.57838717382308147, -7.715628353033886278, -28.96176188950215646 ) ) ;
#28455=CARTESIAN_POINT ( 'NONE',  ( -8.786685647604896232, 23.24040270374459993, 48.22796981442743913 ) ) ;
#28457=ORIENTED_EDGE ( 'NONE', *, *, #1208, .F. ) ;
#28458=EDGE_LOOP ( 'NONE', ( #23810, #27390, #204, #19296 ) ) ;
#28459=CARTESIAN_POINT ( 'NONE',  ( -1.046935749539998906, -43.93230528057173956, 12.93334586714225054 ) ) ;
#28462=CARTESIAN_POINT ( 'NONE',  ( -2.265401668238148591, -46.93990709177548837, -2.645701981445641504 ) ) ;
#28464=CARTESIAN_POINT ( 'NONE',  ( -25.21435515916043357, -25.00736669481038987, -23.92354251275926558 ) ) ;
#28467=CARTESIAN_POINT ( 'NONE',  ( -55.25719721206881729, -0.006045473558784038998, 0.009391134844733136505 ) ) ;
#28478=VERTEX_POINT ( 'NONE', #7173 ) ;
#28494=COLOUR_RGB('Light Blue',0.38,0.62,0.78);
#28495=FILL_AREA_STYLE_COLOUR('',#28494);
#28496=FILL_AREA_STYLE('',(#28495));
#28497=SURFACE_STYLE_FILL_AREA(#28496);
#28498=SURFACE_SIDE_STYLE('',(#28497));
#28499=SURFACE_STYLE_USAGE(.BOTH.,#28498);
#28500=PRESENTATION_STYLE_ASSIGNMENT((#28499));
ENDSEC;
END-ISO-10303-21;
